ISO-10303-21;
HEADER;
FILE_DESCRIPTION (('STEP AP214'),
    '1' );
FILE_NAME ('square bolt.step',
    '2026-10-26T19:46:16',
    ( '' ),
    ( '' ),
    'SwSTEP 2.0',
    'SolidWorks 2025',
    '' );
FILE_SCHEMA (( 'AUTOMOTIVE_DESIGN' ));
ENDSEC;

DATA;
#1=CARTESIAN_POINT ( 'NONE',  ( 7.204075437095966983, 7.204075437095967871, 116.9687500020483810 ) ) ;
#5=CARTESIAN_POINT ( 'NONE',  ( -6.238412754330611322E-16, 10.18810118749999916, 71.78125000204838102 ) ) ;
#35=( NAMED_UNIT ( * ) PLANE_ANGLE_UNIT ( ) SI_UNIT ( $, .RADIAN. ) );
#37=EDGE_CURVE ( 'NONE', #72225, #25230, #72296, .T. ) ;
#42=CARTESIAN_POINT ( 'NONE',  ( -7.204075437095967871, 7.204075437095967871, 89.96875000204838102 ) ) ;
#43=CARTESIAN_POINT ( 'NONE',  ( -10.99999999999989342, 4.556349186104152515, 92.40625000000000000 ) ) ;
#45=CARTESIAN_POINT ( 'NONE',  ( 11.00000000000000000, 4.556349186104045934, 99.34375000000000000 ) ) ;
#79=CARTESIAN_POINT ( 'NONE',  ( 7.778174593052023411, -7.778174593052021635, 93.25000000409677625 ) ) ;
#81=EDGE_CURVE ( 'NONE', #73625, #45401, #67113, .T. ) ;
#93=ORIENTED_EDGE ( 'NONE', *, *, #56073, .F. ) ;
#101=CARTESIAN_POINT ( 'NONE',  ( -4.220049686691937474, -10.18810118749999738, 95.31250000204838102 ) ) ;
#109=CARTESIAN_POINT ( 'NONE',  ( 10.18810118749999916, 1.247682550866122264E-15, 105.9062500020483810 ) ) ;
#118=CARTESIAN_POINT ( 'NONE',  ( 7.204075437095968759, -7.204075437095966983, 106.0937500020483810 ) ) ;
#123=EDGE_CURVE ( 'NONE', #13669, #16043, #62099, .T. ) ;
#135=CARTESIAN_POINT ( 'NONE',  ( -6.238412754330611322E-16, 10.18810118749999916, 112.2812500020483810 ) ) ;
#150=CARTESIAN_POINT ( 'NONE',  ( -11.00000000000000000, 0.000000000000000000, 77.49999999999998579 ) ) ;
#154=CARTESIAN_POINT ( 'NONE',  ( -10.18810118749999916, 4.220049686691934809, 67.93750000204838102 ) ) ;
#160=ORIENTED_EDGE ( 'NONE', *, *, #64767, .F. ) ;
#163=CARTESIAN_POINT ( 'NONE',  ( -7.778174593052023411, 7.778174593052023411, 109.0000000040967763 ) ) ;
#171=( BOUNDED_CURVE ( )  B_SPLINE_CURVE ( 2, ( #47416, #64413, #24036, #1427, #24411, #35019, #22928, #63283, #6340 ),
 .UNSPECIFIED., .F., .F. ) 
 B_SPLINE_CURVE_WITH_KNOTS ( ( 3, 2, 2, 2, 3 ),
 ( 0.4558823529411764608, 0.4595588235294117418, 0.4632352941176470784, 0.4669117647058824150, 0.4705882352941176960 ),
 .UNSPECIFIED. ) 
 CURVE ( )  GEOMETRIC_REPRESENTATION_ITEM ( )  RATIONAL_B_SPLINE_CURVE ( ( 1.000000000000000000, 0.9238795325112867385, 1.000000000000000000, 0.9238795325112867385, 1.000000000000000000, 0.9238795325112867385, 1.000000000000000000, 0.9238795325112856283, 1.000000000000001110 ) ) 
 REPRESENTATION_ITEM ( '' )  );
#182=CARTESIAN_POINT ( 'NONE',  ( -4.556349186104045934, 11.00000000000000000, 104.2187500000000000 ) ) ;
#186=CARTESIAN_POINT ( 'NONE',  ( 7.204075437095968759, -7.204075437095966983, 81.71875000204836681 ) ) ;
#190=CARTESIAN_POINT ( 'NONE',  ( 1.871523826299183495E-15, -10.18810118749999916, 116.4062500020483810 ) ) ;
#198=CARTESIAN_POINT ( 'NONE',  ( -7.204075437095967871, 7.204075437095967871, 75.34375000204838102 ) ) ;
#205=CONICAL_SURFACE ( 'NONE', #29092, 10.49999999999998224, 0.7853981633974378429 ) ;
#212=CARTESIAN_POINT ( 'NONE',  ( -6.238412754330611322E-16, 10.18810118749999916, 71.78125000204838102 ) ) ;
#250=CARTESIAN_POINT ( 'NONE',  ( -4.556349186104045934, 11.00000000000000000, 84.90625000409676204 ) ) ;
#273=CARTESIAN_POINT ( 'NONE',  ( -6.238412754330611322E-16, 10.18810118749999916, 103.2812500020483810 ) ) ;
#276=CARTESIAN_POINT ( 'NONE',  ( 4.556349186104052151, -10.99999999999999822, 68.96875000000000000 ) ) ;
#291=CARTESIAN_POINT ( 'NONE',  ( 10.18810118750000093, -4.220049686691933033, 95.68750000204838102 ) ) ;
#293=ORIENTED_EDGE ( 'NONE', *, *, #58065, .F. ) ;
#303=CARTESIAN_POINT ( 'NONE',  ( -6.238412754330611322E-16, 10.18810118749999916, 86.78125000204836681 ) ) ;
#313=VECTOR ( 'NONE', #22146, 1000.000000000000000 ) ;
#315=CARTESIAN_POINT ( 'NONE',  ( 1.871523826299183495E-15, -10.18810118749999916, 77.40625000204836681 ) ) ;
#331=CARTESIAN_POINT ( 'NONE',  ( 1.871523826299183495E-15, -10.18810118749999916, 69.53125000204838102 ) ) ;
#334=CARTESIAN_POINT ( 'NONE',  ( -7.778174593052023411, 7.778174593052023411, 84.81249999999998579 ) ) ;
#359=CARTESIAN_POINT ( 'NONE',  ( -4.556349186104048599, -10.99999999999999822, 116.7812499999999858 ) ) ;
#361=CARTESIAN_POINT ( 'NONE',  ( 4.556349186104045934, 11.00000000000000000, 71.21875000409677625 ) ) ;
#371=CARTESIAN_POINT ( 'NONE',  ( -4.556349186104045934, 11.00000000000000000, 108.7187499999999858 ) ) ;
#373=CARTESIAN_POINT ( 'NONE',  ( 1.871523826299183495E-15, -10.18810118749999916, 110.4062500020483668 ) ) ;
#377=CARTESIAN_POINT ( 'NONE',  ( -10.18810118749999738, -4.220049686691941915, 73.75000000204836681 ) ) ;
#395=EDGE_CURVE ( 'NONE', #73730, #54851, #613, .T. ) ;
#414=CARTESIAN_POINT ( 'NONE',  ( -10.18810118749999738, -4.220049686691941915, 84.25000000204838102 ) ) ;
#417=CARTESIAN_POINT ( 'NONE',  ( -10.99999999999999822, -4.556349186104052151, 100.0937500000000142 ) ) ;
#443=CARTESIAN_POINT ( 'NONE',  ( -4.556349186104045934, 11.00000000000000000, 99.71875000000000000 ) ) ;
#448=CARTESIAN_POINT ( 'NONE',  ( 7.778174593052021635, 7.778174593052023411, 92.12500000409677625 ) ) ;
#464=CARTESIAN_POINT ( 'NONE',  ( 11.00000000000000000, 1.347111479062088405E-15, 100.7499999999999858 ) ) ;
#470=CARTESIAN_POINT ( 'NONE',  ( -7.204075437095965206, -7.204075437095968759, 99.71875000204838102 ) ) ;
#473=EDGE_CURVE ( 'NONE', #34245, #9171, #2555, .T. ) ;
#474=DIRECTION ( 'NONE',  ( -1.000000000000000000, 0.000000000000000000, 0.000000000000000000 ) ) ;
#478=CARTESIAN_POINT ( 'NONE',  ( -10.18810118749999916, 4.220049686691934809, 109.5625000020483810 ) ) ;
#485=CARTESIAN_POINT ( 'NONE',  ( 11.00000000000010836, -4.556349186103939353, 76.84375000409676204 ) ) ;
#488=CARTESIAN_POINT ( 'NONE',  ( -10.18810118749999916, 0.000000000000000000, 102.5312500020483810 ) ) ;
#500=ORIENTED_EDGE ( 'NONE', *, *, #41762, .F. ) ;
#503=CARTESIAN_POINT ( 'NONE',  ( -10.18810118749999738, -4.220049686691941915, 111.2500000020483952 ) ) ;
#513=FACE_OUTER_BOUND ( 'NONE', #13877, .T. ) ;
#520=CARTESIAN_POINT ( 'NONE',  ( 4.556349186104045934, 11.00000000000000000, 117.5312500000000142 ) ) ;
#531=CARTESIAN_POINT ( 'NONE',  ( -4.556349186104047710, -10.99999999999999822, 107.9687500040967905 ) ) ;
#535=CARTESIAN_POINT ( 'NONE',  ( -7.778174593052020747, -7.778174593052023411, 107.8750000040967763 ) ) ;
#545=VERTEX_POINT ( 'NONE', #46971 ) ;
#548=CARTESIAN_POINT ( 'NONE',  ( -15.99999999999999645, 15.99999999999999645, 20.00000000000000000 ) ) ;
#552=CARTESIAN_POINT ( 'NONE',  ( 7.204075437095968759, -7.204075437095966983, 83.21875000204836681 ) ) ;
#556=CARTESIAN_POINT ( 'NONE',  ( 4.220049686691941027, -10.18810118749999738, 113.5000000020483810 ) ) ;
#563=CARTESIAN_POINT ( 'NONE',  ( 1.871523826299183495E-15, -10.18810118749999916, 78.90625000204836681 ) ) ;
#577=CARTESIAN_POINT ( 'NONE',  ( 1.871523826299183495E-15, -10.18810118749999916, 71.03125000204838102 ) ) ;
#613=LINE ( 'NONE', #28883, #48986 ) ;
#644=CARTESIAN_POINT ( 'NONE',  ( 10.18810118749999916, 1.247682550866122264E-15, 101.4062500020483810 ) ) ;
#656=CARTESIAN_POINT ( 'NONE',  ( 10.99999999999989342, 4.556349186104152515, 99.53125000409680467 ) ) ;
#661=CARTESIAN_POINT ( 'NONE',  ( -4.220049686691935698, 10.18810118749999916, 93.25000000204838102 ) ) ;
#667=CARTESIAN_POINT ( 'NONE',  ( -4.220049686691937474, -10.18810118749999738, 77.31250000204836681 ) ) ;
#675=CARTESIAN_POINT ( 'NONE',  ( 7.204075437095966983, 7.204075437095967871, 89.59375000204838102 ) ) ;
#685=CARTESIAN_POINT ( 'NONE',  ( -7.204075437095965206, -7.204075437095968759, 75.71875000204836681 ) ) ;
#689=CARTESIAN_POINT ( 'NONE',  ( -4.556349186104048599, -10.99999999999999822, 112.2812500000000000 ) ) ;
#701=CARTESIAN_POINT ( 'NONE',  ( 7.204075437095968759, -7.204075437095966983, 68.21875000204836681 ) ) ;
#703=DIRECTION ( 'NONE',  ( 1.000000000000000000, 0.000000000000000000, 0.000000000000000000 ) ) ;
#704=CARTESIAN_POINT ( 'NONE',  ( -6.735557395310442023E-16, 11.00000000000000000, 84.62499999999997158 ) ) ;
#730=CARTESIAN_POINT ( 'NONE',  ( 7.778174593052023411, -7.778174593052021635, 117.0625000000000000 ) ) ;
#732=CARTESIAN_POINT ( 'NONE',  ( 4.556349186104045934, 11.00000000000000000, 68.21875000409676204 ) ) ;
#744=CARTESIAN_POINT ( 'NONE',  ( -4.220049686691937474, -10.18810118749999738, 111.8125000020483952 ) ) ;
#748=CARTESIAN_POINT ( 'NONE',  ( 1.871523826299183495E-15, -10.18810118749999916, 68.03125000204838102 ) ) ;
#760=DIRECTION ( 'NONE',  ( 1.000000000000000000, 0.000000000000000000, 0.000000000000000000 ) ) ;
#784=CARTESIAN_POINT ( 'NONE',  ( 4.220049686691934809, 10.18810118749999916, 86.68750000204838102 ) ) ;
#787=CARTESIAN_POINT ( 'NONE',  ( -7.778174593052023411, 7.778174593052023411, 102.8124999999999858 ) ) ;
#794=CARTESIAN_POINT ( 'NONE',  ( -4.556349186104045934, 11.00000000000000000, 78.71874999999998579 ) ) ;
#811=FACE_OUTER_BOUND ( 'NONE', #21335, .T. ) ;
#815=CARTESIAN_POINT ( 'NONE',  ( 11.00000000000000355, -4.556349186104045046, 84.34375000409677625 ) ) ;
#831=EDGE_CURVE ( 'NONE', #72883, #74244, #48089, .T. ) ;
#840=CARTESIAN_POINT ( 'NONE',  ( 7.204075437095968759, -7.204075437095966983, 94.09375000204838102 ) ) ;
#849=CARTESIAN_POINT ( 'NONE',  ( -10.18810118749999738, -4.220049686691941915, 108.2500000020483810 ) ) ;
#857=CARTESIAN_POINT ( 'NONE',  ( 7.204075437095968759, -7.204075437095966983, 104.5937500020483810 ) ) ;
#872=CARTESIAN_POINT ( 'NONE',  ( 4.220049686691941027, -10.18810118749999738, 105.6250000020483668 ) ) ;
#873=CARTESIAN_POINT ( 'NONE',  ( -7.778174593052020747, -7.778174593052023411, 103.1874999999999858 ) ) ;
#891=CARTESIAN_POINT ( 'NONE',  ( 4.220049686691934809, 10.18810118749999916, 70.56250000204836681 ) ) ;
#901=CARTESIAN_POINT ( 'NONE',  ( -11.00000000000000000, 4.556349186104045934, 106.0937500040968047 ) ) ;
#903=CARTESIAN_POINT ( 'NONE',  ( -11.00000000000000000, 0.000000000000000000, 71.49999999999998579 ) ) ;
#920=AXIS2_PLACEMENT_3D ( 'NONE', #37998, #55729, #39750 ) ;
#923=CARTESIAN_POINT ( 'NONE',  ( -7.204075437095965206, -7.204075437095968759, 84.34375000204836681 ) ) ;
#927=CARTESIAN_POINT ( 'NONE',  ( -7.204075437095967871, 7.204075437095967871, 109.8437500020483810 ) ) ;
#936=CARTESIAN_POINT ( 'NONE',  ( 7.204075437095966983, 7.204075437095967871, 79.46875000204836681 ) ) ;
#947=VECTOR ( 'NONE', #19692, 1000.000000000000000 ) ;
#948=CARTESIAN_POINT ( 'NONE',  ( -10.18810118749999916, 4.220049686691934809, 73.56250000204835260 ) ) ;
#1009=VERTEX_POINT ( 'NONE', #29882 ) ;
#1010=CARTESIAN_POINT ( 'NONE',  ( -9.761837184982935511, 4.601249817483572535, 117.7500899827576859 ) ) ;
#1011=CARTESIAN_POINT ( 'NONE',  ( -4.220049686691935698, 10.18810118749999916, 98.87500000204836681 ) ) ;
#1028=CARTESIAN_POINT ( 'NONE',  ( -7.204075437095965206, -7.204075437095968759, 95.21875000204838102 ) ) ;
#1034=CARTESIAN_POINT ( 'NONE',  ( -6.238412754330611322E-16, 10.18810118749999916, 78.15625000204836681 ) ) ;
#1041=CARTESIAN_POINT ( 'NONE',  ( -7.204075437095965206, -7.204075437095968759, 88.84375000204838102 ) ) ;
#1052=CARTESIAN_POINT ( 'NONE',  ( 1.871523826299183495E-15, -10.18810118749999916, 74.40625000204836681 ) ) ;
#1055=CARTESIAN_POINT ( 'NONE',  ( 11.00000000000000000, 1.347111479062088405E-15, 118.0000000000000000 ) ) ;
#1072=CARTESIAN_POINT ( 'NONE',  ( -4.556349186104045934, 11.00000000000000000, 81.71874999999998579 ) ) ;
#1088=CARTESIAN_POINT ( 'NONE',  ( -11.00000000000000000, 0.000000000000000000, 107.4999999999999858 ) ) ;
#1100=CARTESIAN_POINT ( 'NONE',  ( -7.778174593052023411, 7.778174593052023411, 70.00000000409677625 ) ) ;
#1104=EDGE_CURVE ( 'NONE', #72546, #34245, #53672, .T. ) ;
#1112=CARTESIAN_POINT ( 'NONE',  ( 1.871523826299183495E-15, -10.18810118749999916, 114.9062500020483810 ) ) ;
#1123=VERTEX_POINT ( 'NONE', #28393 ) ;
#1128=DIRECTION ( 'NONE',  ( 0.000000000000000000, 0.000000000000000000, 1.000000000000000000 ) ) ;
#1149=CARTESIAN_POINT ( 'NONE',  ( -10.18810118749999916, 4.220049686691934809, 87.06250000204838102 ) ) ;
#1150=UNCERTAINTY_MEASURE_WITH_UNIT (LENGTH_MEASURE( 1.000000000000000082E-05 ), #27939, 'distance_accuracy_value', 'NONE');
#1152=CARTESIAN_POINT ( 'NONE',  ( -7.778174593052020747, -7.778174593052023411, 100.1874999999999858 ) ) ;
#1159=CARTESIAN_POINT ( 'NONE',  ( 11.00000000000000000, 1.347111479062088405E-15, 78.24999999999998579 ) ) ;
#1170=CARTESIAN_POINT ( 'NONE',  ( -6.735557395310442023E-16, 11.00000000000000000, 86.12499999999998579 ) ) ;
#1175=DIRECTION ( 'NONE',  ( 1.000000000000000000, 0.000000000000000000, 0.000000000000000000 ) ) ;
#1177=CARTESIAN_POINT ( 'NONE',  ( -15.99999999999999645, -16.00000000000000355, 20.00000000000000000 ) ) ;
#1181=CARTESIAN_POINT ( 'NONE',  ( 7.778174593052021635, 7.778174593052023411, 87.62500000409677625 ) ) ;
#1184=CARTESIAN_POINT ( 'NONE',  ( 11.00000000000000000, 1.347111479062088405E-15, 103.9375000040967763 ) ) ;
#1203=CARTESIAN_POINT ( 'NONE',  ( -6.735557395310442023E-16, 11.00000000000000000, 90.81250000409676204 ) ) ;
#1204=AXIS2_PLACEMENT_3D ( 'NONE', #1366, #71469, #60161 ) ;
#1206=CARTESIAN_POINT ( 'NONE',  ( -7.204075437095967871, 7.204075437095967871, 91.84375000204838102 ) ) ;
#1214=CARTESIAN_POINT ( 'NONE',  ( -10.18810118749999916, 0.000000000000000000, 102.1562500020483810 ) ) ;
#1216=VERTEX_POINT ( 'NONE', #2315 ) ;
#1222=CARTESIAN_POINT ( 'NONE',  ( -7.204075437095965206, -7.204075437095968759, 101.2187500020483668 ) ) ;
#1226=LINE ( 'NONE', #29880, #67407 ) ;
#1240=CARTESIAN_POINT ( 'NONE',  ( -10.18810118749999738, -4.220049686691941915, 102.2500000020483810 ) ) ;
#1251=CARTESIAN_POINT ( 'NONE',  ( -11.00000000000010303, -4.556349186103947346, 109.0937499999999858 ) ) ;
#1257=CARTESIAN_POINT ( 'NONE',  ( -4.556349186104045934, 11.00000000000000000, 72.90625000409677625 ) ) ;
#1258=CARTESIAN_POINT ( 'NONE',  ( -7.204075437095967871, 7.204075437095967871, 69.34375000204836681 ) ) ;
#1269=CARTESIAN_POINT ( 'NONE',  ( -6.735557395310442023E-16, 11.00000000000000000, 107.3125000040967905 ) ) ;
#1291=CARTESIAN_POINT ( 'NONE',  ( 10.18810118749999916, 4.220049686691935698, 85.00000000204838102 ) ) ;
#1295=CARTESIAN_POINT ( 'NONE',  ( -6.238412754330611322E-16, 10.18810118749999916, 109.6562500020483668 ) ) ;
#1301=CARTESIAN_POINT ( 'NONE',  ( -7.204075437095967871, 7.204075437095967871, 76.84375000204838102 ) ) ;
#1304=CARTESIAN_POINT ( 'NONE',  ( 7.778174593052023411, -7.778174593052021635, 94.75000000409677625 ) ) ;
#1313=CARTESIAN_POINT ( 'NONE',  ( -10.18810118749999916, 4.220049686691934809, 70.56250000204836681 ) ) ;
#1338=CARTESIAN_POINT ( 'NONE',  ( 11.00000000000000000, 8.673617379884037444E-16, 41.99999999999999289 ) ) ;
#1366=CARTESIAN_POINT ( 'NONE',  ( 0.000000000000000000, 0.000000000000000000, 118.0000000000000000 ) ) ;
#1368=CARTESIAN_POINT ( 'NONE',  ( -11.00000000000010658, 4.556349186103942017, 101.5937500040967763 ) ) ;
#1379=CARTESIAN_POINT ( 'NONE',  ( -3.652275167153403945, 10.24818182827785229, 117.6308536796923363 ) ) ;
#1380=CARTESIAN_POINT ( 'NONE',  ( -6.238412754330611322E-16, 10.18810118749999916, 100.2812500020483810 ) ) ;
#1396=CARTESIAN_POINT ( 'NONE',  ( -10.18810118749999738, -4.220049686691941915, 98.12500000204838102 ) ) ;
#1402=CARTESIAN_POINT ( 'NONE',  ( -6.735557395310442023E-16, 11.00000000000000000, 102.6250000000000000 ) ) ;
#1403=CARTESIAN_POINT ( 'NONE',  ( -4.220049686691935698, 10.18810118749999916, 73.75000000204836681 ) ) ;
#1406=DIRECTION ( 'NONE',  ( 0.000000000000000000, 0.000000000000000000, 1.000000000000000000 ) ) ;
#1411=EDGE_CURVE ( 'NONE', #11029, #15561, #48507, .T. ) ;
#1412=CARTESIAN_POINT ( 'NONE',  ( -4.220049686691935698, 10.18810118749999916, 86.87500000204836681 ) ) ;
#1422=CARTESIAN_POINT ( 'NONE',  ( 7.204075437095966983, 7.204075437095967871, 76.46875000204836681 ) ) ;
#1423=VERTEX_POINT ( 'NONE', #20726 ) ;
#1427=CARTESIAN_POINT ( 'NONE',  ( 4.556349186104052151, -10.99999999999999822, 93.15625000409677625 ) ) ;
#1436=ORIENTED_EDGE ( 'NONE', *, *, #60922, .F. ) ;
#1444=CARTESIAN_POINT ( 'NONE',  ( -4.556349186104047710, -10.99999999999999822, 77.78125000000001421 ) ) ;
#1470=CARTESIAN_POINT ( 'NONE',  ( -4.556349186104045934, 11.00000000000000000, 66.90625000409677625 ) ) ;
#1483=CARTESIAN_POINT ( 'NONE',  ( 4.220049686691934809, 10.18810118749999916, 114.0625000020483668 ) ) ;
#1501=AXIS2_PLACEMENT_3D ( 'NONE', #19533, #13859, #42913 ) ;
#1503=EDGE_CURVE ( 'NONE', #10820, #23833, #40674, .T. ) ;
#1519=ORIENTED_EDGE ( 'NONE', *, *, #22892, .T. ) ;
#1525=CARTESIAN_POINT ( 'NONE',  ( 4.220049686691934809, 10.18810118749999916, 88.18750000204838102 ) ) ;
#1526=CARTESIAN_POINT ( 'NONE',  ( -7.778174593052020747, -7.778174593052023411, 97.18749999999998579 ) ) ;
#1532=CARTESIAN_POINT ( 'NONE',  ( 4.556349186104045934, 11.00000000000000000, 78.53125000000000000 ) ) ;
#1550=CARTESIAN_POINT ( 'NONE',  ( -11.00000000000013145, 4.556349186103913596, 104.5937500040967905 ) ) ;
#1554=CARTESIAN_POINT ( 'NONE',  ( -11.00000000000000000, 0.000000000000000000, 83.68750000409677625 ) ) ;
#1575=DIRECTION ( 'NONE',  ( -0.000000000000000000, -0.000000000000000000, -1.000000000000000000 ) ) ;
#1577=CARTESIAN_POINT ( 'NONE',  ( -4.220049686691937474, -10.18810118749999738, 93.81250000204839523 ) ) ;
#1580=CARTESIAN_POINT ( 'NONE',  ( -10.18810118749999916, 0.000000000000000000, 100.6562500020483810 ) ) ;
#1588=CARTESIAN_POINT ( 'NONE',  ( 10.18810118750000093, -4.220049686691933921, 95.68750000204838102 ) ) ;
#1605=CARTESIAN_POINT ( 'NONE',  ( 10.18810118750000093, -4.220049686691933033, 102.8125000020483952 ) ) ;
#1611=EDGE_CURVE ( 'NONE', #29602, #10820, #37813, .T. ) ;
#1624=CARTESIAN_POINT ( 'NONE',  ( 10.18810118749999916, 4.220049686691935698, 70.37500000204838102 ) ) ;
#1635=CARTESIAN_POINT ( 'NONE',  ( 7.778174593052023411, -7.778174593052021635, 106.7500000040967763 ) ) ;
#1638=CARTESIAN_POINT ( 'NONE',  ( -7.778174593052023411, 7.778174593052023411, 71.31249999999998579 ) ) ;
#1658=CARTESIAN_POINT ( 'NONE',  ( -10.18810118749999916, 0.000000000000000000, 107.0312500020483810 ) ) ;
#1665=CARTESIAN_POINT ( 'NONE',  ( 4.220049686691934809, 10.18810118749999916, 69.06250000204838102 ) ) ;
#1668=EDGE_LOOP ( 'NONE', ( #11795, #58115, #44784, #2229, #47593 ) ) ;
#1677=CARTESIAN_POINT ( 'NONE',  ( 4.220049686691941027, -10.18810118749999738, 69.62500000204838102 ) ) ;
#1680=CARTESIAN_POINT ( 'NONE',  ( -11.00000000000000533, -11.00000000000000355, 41.99999999999999289 ) ) ;
#1705=( BOUNDED_CURVE ( )  B_SPLINE_CURVE ( 2, ( #43005, #1922, #36259, #37365, #47557, #2661, #25281, #48299, #70944 ),
 .UNSPECIFIED., .F., .F. ) 
 B_SPLINE_CURVE_WITH_KNOTS ( ( 3, 2, 2, 2, 3 ),
 ( 0.4705882352941176960, 0.4742647058823529771, 0.4779411764705883137, 0.4816176470588235947, 0.4852941176470588758 ),
 .UNSPECIFIED. ) 
 CURVE ( )  GEOMETRIC_REPRESENTATION_ITEM ( )  RATIONAL_B_SPLINE_CURVE ( ( 0.9999999999999988898, 0.9238795325112878487, 1.000000000000000000, 0.9238795325112867385, 1.000000000000000000, 0.9238795325112867385, 1.000000000000000000, 0.9238795325112856283, 1.000000000000001110 ) ) 
 REPRESENTATION_ITEM ( '' )  );
#1734=CARTESIAN_POINT ( 'NONE',  ( -10.99999999999986677, -4.556349186104185378, 104.7812500040967905 ) ) ;
#1742=CARTESIAN_POINT ( 'NONE',  ( -4.220049686691937474, -10.18810118749999738, 99.43750000204836681 ) ) ;
#1749=EDGE_CURVE ( 'NONE', #58573, #2613, #66226, .T. ) ;
#1758=CARTESIAN_POINT ( 'NONE',  ( -7.204075437095965206, -7.204075437095968759, 86.21875000204836681 ) ) ;
#1759=EDGE_CURVE ( 'NONE', #33217, #31137, #14639, .T. ) ;
#1764=CARTESIAN_POINT ( 'NONE',  ( 4.220049686691934809, 10.18810118749999916, 72.06250000204836681 ) ) ;
#1770=CARTESIAN_POINT ( 'NONE',  ( 10.18810118750000093, -4.220049686691933921, 87.81250000204838102 ) ) ;
#1779=CARTESIAN_POINT ( 'NONE',  ( -6.238412754330611322E-16, 10.18810118749999916, 76.65625000204836681 ) ) ;
#1797=CARTESIAN_POINT ( 'NONE',  ( 11.00000000000000355, -4.556349186104045046, 79.65625000000000000 ) ) ;
#1800=CARTESIAN_POINT ( 'NONE',  ( -11.00000000000000000, 0.000000000000000000, 83.49999999999998579 ) ) ;
#1823=CARTESIAN_POINT ( 'NONE',  ( -7.204075437095967871, 7.204075437095967871, 84.34375000204836681 ) ) ;
#1824=CARTESIAN_POINT ( 'NONE',  ( -4.556349186104045934, 11.00000000000000000, 69.90625000409677625 ) ) ;
#1825=LINE ( 'NONE', #18059, #20216 ) ;
#1838=CARTESIAN_POINT ( 'NONE',  ( -7.204075437095967871, 7.204075437095967871, 115.8437500020483810 ) ) ;
#1861=CARTESIAN_POINT ( 'NONE',  ( -11.00000000000000000, 0.000000000000000000, 72.99999999999998579 ) ) ;
#1866=ORIENTED_EDGE ( 'NONE', *, *, #48044, .T. ) ;
#1873=CARTESIAN_POINT ( 'NONE',  ( 4.220049686691941027, -10.18810118749999738, 86.12500000204836681 ) ) ;
#1875=CARTESIAN_POINT ( 'NONE',  ( -7.778174593052023411, 7.778174593052023411, 96.81250000000000000 ) ) ;
#1904=CARTESIAN_POINT ( 'NONE',  ( -10.99999999999999822, -4.556349186104052151, 85.28125000409677625 ) ) ;
#1922=CARTESIAN_POINT ( 'NONE',  ( -10.99999999999994849, 4.556349186104097448, 92.59375000409679046 ) ) ;
#1929=CARTESIAN_POINT ( 'NONE',  ( -4.220049686691935698, 10.18810118749999916, 91.75000000204836681 ) ) ;
#1934=CARTESIAN_POINT ( 'NONE',  ( -6.238412754330611322E-16, 10.18810118749999916, 103.2812500020483810 ) ) ;
#1942=CARTESIAN_POINT ( 'NONE',  ( -7.204075437095965206, -7.204075437095968759, 98.21875000204838102 ) ) ;
#1959=CARTESIAN_POINT ( 'NONE',  ( -10.18810118749999738, -4.220049686691941915, 106.7500000020483668 ) ) ;
#1960=CARTESIAN_POINT ( 'NONE',  ( -6.735557395310442023E-16, 11.00000000000000000, 114.8125000040967763 ) ) ;
#1976=CARTESIAN_POINT ( 'NONE',  ( 11.00000000000000355, -4.556349186104045046, 112.6562499999999858 ) ) ;
#1980=CARTESIAN_POINT ( 'NONE',  ( 7.778174593052023411, -7.778174593052021635, 102.0624999999999858 ) ) ;
#1989=CARTESIAN_POINT ( 'NONE',  ( 2.020667218593132706E-15, -11.00000000000000000, 106.5625000040967763 ) ) ;
#1992=CARTESIAN_POINT ( 'NONE',  ( 11.00000000000000000, 4.556349186104045934, 70.84374999999998579 ) ) ;
#2012=CARTESIAN_POINT ( 'NONE',  ( 7.204075437095966983, 7.204075437095967871, 109.4687500020483810 ) ) ;
#2019=CARTESIAN_POINT ( 'NONE',  ( 7.204075437095968759, -7.204075437095966983, 68.59375000204836681 ) ) ;
#2023=DIRECTION ( 'NONE',  ( -1.000000000000000000, 0.000000000000000000, 0.000000000000000000 ) ) ;
#2033=CARTESIAN_POINT ( 'NONE',  ( -4.220049686691935698, 10.18810118749999916, 115.7500000020483668 ) ) ;
#2041=VECTOR ( 'NONE', #54132, 1000.000000000000000 ) ;
#2078=CARTESIAN_POINT ( 'NONE',  ( 11.00000000000000000, 1.347111479062088405E-15, 67.93750000409676204 ) ) ;
#2084=CARTESIAN_POINT ( 'NONE',  ( -10.99999999999989164, -4.556349186104158733, 85.09375000000001421 ) ) ;
#2087=CARTESIAN_POINT ( 'NONE',  ( 11.00000000000000000, 1.347111479062088405E-15, 108.2499999999999858 ) ) ;
#2094=DIRECTION ( 'NONE',  ( -0.000000000000000000, -0.000000000000000000, -1.000000000000000000 ) ) ;
#2095=CARTESIAN_POINT ( 'NONE',  ( -7.204075437095965206, -7.204075437095968759, 97.84375000204836681 ) ) ;
#2111=CARTESIAN_POINT ( 'NONE',  ( 10.18810118749999916, 4.220049686691935698, 89.87500000204836681 ) ) ;
#2112=EDGE_CURVE ( 'NONE', #26793, #2485, #22970, .T. ) ;
#2117=CARTESIAN_POINT ( 'NONE',  ( -11.00000000000005151, 4.556349186103993532, 102.9062499999999858 ) ) ;
#2118=CARTESIAN_POINT ( 'NONE',  ( 10.18810118749999916, 1.247682550866122264E-15, 74.78125000204836681 ) ) ;
#2123=CARTESIAN_POINT ( 'NONE',  ( -4.220049686691935698, 10.18810118749999916, 83.87500000204835260 ) ) ;
#2135=( BOUNDED_CURVE ( )  B_SPLINE_CURVE ( 2, ( #65724, #13291, #7287, #24253, #64983, #12926, #36699, #58980, #24984 ),
 .UNSPECIFIED., .F., .F. ) 
 B_SPLINE_CURVE_WITH_KNOTS ( ( 3, 2, 2, 2, 3 ),
 ( 0.8823529411764705621, 0.8860294117647058432, 0.8897058823529411242, 0.8933823529411765163, 0.8970588235294117974 ),
 .UNSPECIFIED. ) 
 CURVE ( )  GEOMETRIC_REPRESENTATION_ITEM ( )  RATIONAL_B_SPLINE_CURVE ( ( 1.000000000000000000, 0.9238795325112867385, 1.000000000000000000, 0.9238795325112867385, 1.000000000000000000, 0.9238795325112867385, 1.000000000000000000, 0.9238795325112867385, 1.000000000000000000 ) ) 
 REPRESENTATION_ITEM ( '' )  );
#2137=CARTESIAN_POINT ( 'NONE',  ( 10.18810118749999916, 1.247682550866122264E-15, 68.78125000204838102 ) ) ;
#2138=EDGE_LOOP ( 'NONE', ( #9116, #36634, #7967 ) ) ;
#2159=CARTESIAN_POINT ( 'NONE',  ( -4.556349186104045934, 11.00000000000000000, 75.71874999999998579 ) ) ;
#2162=CARTESIAN_POINT ( 'NONE',  ( -7.778174593052020747, -7.778174593052023411, 113.6875000000000000 ) ) ;
#2177=ORIENTED_EDGE ( 'NONE', *, *, #6585, .F. ) ;
#2185=CARTESIAN_POINT ( 'NONE',  ( -7.204075437095967871, 7.204075437095967871, 88.84375000204838102 ) ) ;
#2186=CARTESIAN_POINT ( 'NONE',  ( -10.18810118749999738, -4.220049686691941915, 115.7500000020483668 ) ) ;
#2195=AXIS2_PLACEMENT_3D ( 'NONE', #45969, #54137, #64714 ) ;
#2198=CARTESIAN_POINT ( 'NONE',  ( -4.220049686691935698, 10.18810118749999916, 106.7500000020483668 ) ) ;
#2207=VECTOR ( 'NONE', #51731, 1000.000000000000000 ) ;
#2212=VECTOR ( 'NONE', #37712, 1000.000000000000000 ) ;
#2218=( BOUNDED_CURVE ( )  B_SPLINE_CURVE ( 2, ( #58326, #45865, #39470, #5516, #68507, #28516, #29637, #69630, #23598 ),
 .UNSPECIFIED., .F., .F. ) 
 B_SPLINE_CURVE_WITH_KNOTS ( ( 3, 2, 2, 2, 3 ),
 ( 0.2058823529411766273, 0.2095588235294118529, 0.2132352941176470784, 0.2169117647058823040, 0.2205882352941175295 ),
 .UNSPECIFIED. ) 
 CURVE ( )  GEOMETRIC_REPRESENTATION_ITEM ( )  RATIONAL_B_SPLINE_CURVE ( ( 0.9999999999999965583, 0.9238795325112901802, 1.000000000000000000, 0.9238795325112867385, 1.000000000000000000, 0.9238795325112867385, 1.000000000000000000, 0.9238795325112890700, 0.9999999999999976685 ) ) 
 REPRESENTATION_ITEM ( '' )  );
#2222=CARTESIAN_POINT ( 'NONE',  ( 2.020667218593132706E-15, -11.00000000000000000, 78.06250000409677625 ) ) ;
#2229=ORIENTED_EDGE ( 'NONE', *, *, #33019, .F. ) ;
#2236=ORIENTED_EDGE ( 'NONE', *, *, #7464, .T. ) ;
#2237=CARTESIAN_POINT ( 'NONE',  ( -7.204075437095967871, 7.204075437095967871, 82.46875000204836681 ) ) ;
#2239=CARTESIAN_POINT ( 'NONE',  ( 11.00000000000000000, 1.347111479062088405E-15, 97.74999999999998579 ) ) ;
#2245=CARTESIAN_POINT ( 'NONE',  ( -10.99999999999986855, 4.556349186104178273, 106.0937500040967763 ) ) ;
#2256=DIRECTION ( 'NONE',  ( -0.000000000000000000, -0.000000000000000000, -1.000000000000000000 ) ) ;
#2269=CARTESIAN_POINT ( 'NONE',  ( 7.778174593052021635, 7.778174593052023411, 89.12500000409677625 ) ) ;
#2280=VERTEX_POINT ( 'NONE', #28820 ) ;
#2291=CARTESIAN_POINT ( 'NONE',  ( -10.18810118749999916, 0.000000000000000000, 89.03125000204836681 ) ) ;
#2296=CARTESIAN_POINT ( 'NONE',  ( -10.18810118749999916, 4.220049686691934809, 102.0625000020483810 ) ) ;
#2299=ORIENTED_EDGE ( 'NONE', *, *, #23828, .T. ) ;
#2305=CARTESIAN_POINT ( 'NONE',  ( 7.204075437095966983, 7.204075437095967871, 100.4687500020483810 ) ) ;
#2315=CARTESIAN_POINT ( 'NONE',  ( -11.00000000000000000, 0.000000000000000000, 86.68750000409677625 ) ) ;
#2324=CARTESIAN_POINT ( 'NONE',  ( -10.18810118749999916, 0.000000000000000000, 97.65625000204838102 ) ) ;
#2335=( BOUNDED_CURVE ( )  B_SPLINE_CURVE ( 2, ( #19307, #7632, #58956, #71353, #65335, #52917, #30638, #71725, #53291 ),
 .UNSPECIFIED., .F., .F. ) 
 B_SPLINE_CURVE_WITH_KNOTS ( ( 3, 2, 2, 2, 3 ),
 ( 0.8529411764705883137, 0.8566176470588235947, 0.8602941176470589868, 0.8639705882352942679, 0.8676470588235295489 ),
 .UNSPECIFIED. ) 
 CURVE ( )  GEOMETRIC_REPRESENTATION_ITEM ( )  RATIONAL_B_SPLINE_CURVE ( ( 0.9999999999999976685, 0.9238795325112890700, 1.000000000000000000, 0.9238795325112867385, 1.000000000000000000, 0.9238795325112867385, 1.000000000000000000, 0.9238795325112844070, 1.000000000000002220 ) ) 
 REPRESENTATION_ITEM ( '' )  );
#2344=CARTESIAN_POINT ( 'NONE',  ( -11.00000000000000000, 0.000000000000000000, 114.9999999999999858 ) ) ;
#2346=VECTOR ( 'NONE', #19963, 1000.000000000000000 ) ;
#2357=CARTESIAN_POINT ( 'NONE',  ( 2.020667218593132706E-15, -11.00000000000000000, 103.5625000040967763 ) ) ;
#2377=CARTESIAN_POINT ( 'NONE',  ( -7.778174593052023411, 7.778174593052023411, 69.81249999999998579 ) ) ;
#2378=CARTESIAN_POINT ( 'NONE',  ( -10.18810118749999916, 4.220049686691934809, 108.4375000020483668 ) ) ;
#2385=CARTESIAN_POINT ( 'NONE',  ( 4.220049686691934809, 10.18810118749999916, 73.56250000204836681 ) ) ;
#2399=CARTESIAN_POINT ( 'NONE',  ( -10.18810118749999916, 0.000000000000000000, 116.0312500020483810 ) ) ;
#2428=ORIENTED_EDGE ( 'NONE', *, *, #72520, .T. ) ;
#2437=LINE ( 'NONE', #42414, #17489 ) ;
#2438=CARTESIAN_POINT ( 'NONE',  ( -11.00000000000010303, -4.556349186103947346, 68.78125000409676204 ) ) ;
#2440=CARTESIAN_POINT ( 'NONE',  ( 4.556349186104045934, 11.00000000000000000, 75.71875000409677625 ) ) ;
#2443=DIRECTION ( 'NONE',  ( 1.000000000000000000, 3.154042683594195121E-16, 0.000000000000000000 ) ) ;
#2462=( BOUNDED_CURVE ( )  B_SPLINE_CURVE ( 2, ( #34014, #45671, #40392, #39278, #11714, #6064, #68685, #27955, #40757 ),
 .UNSPECIFIED., .F., .F. ) 
 B_SPLINE_CURVE_WITH_KNOTS ( ( 3, 2, 2, 2, 3 ),
 ( 0.5735294117647057321, 0.5772058823529410132, 0.5808823529411764053, 0.5845588235294115753, 0.5882352941176468564 ),
 .UNSPECIFIED. ) 
 CURVE ( )  GEOMETRIC_REPRESENTATION_ITEM ( )  RATIONAL_B_SPLINE_CURVE ( ( 1.000000000000002220, 0.9238795325112844070, 1.000000000000000000, 0.9238795325112867385, 1.000000000000000000, 0.9238795325112867385, 1.000000000000000000, 0.9238795325112912904, 0.9999999999999954481 ) ) 
 REPRESENTATION_ITEM ( '' )  );
#2464=VECTOR ( 'NONE', #27311, 1000.000000000000000 ) ;
#2465=CARTESIAN_POINT ( 'NONE',  ( -11.00000000000000000, 0.000000000000000000, 82.18750000409677625 ) ) ;
#2471=CARTESIAN_POINT ( 'NONE',  ( -10.18810118749999738, -4.220049686691941915, 97.75000000204838102 ) ) ;
#2472=CARTESIAN_POINT ( 'NONE',  ( 11.00000000000000000, 1.347111479062088405E-15, 85.93750000409677625 ) ) ;
#2483=CARTESIAN_POINT ( 'NONE',  ( -6.238412754330611322E-16, 10.18810118749999916, 88.65625000204838102 ) ) ;
#2485=VERTEX_POINT ( 'NONE', #26014 ) ;
#2489=CARTESIAN_POINT ( 'NONE',  ( 7.204075437095968759, -7.204075437095966983, 74.59375000204838102 ) ) ;
#2497=CARTESIAN_POINT ( 'NONE',  ( -10.18810118749999916, 0.000000000000000000, 84.15625000204838102 ) ) ;
#2508=CARTESIAN_POINT ( 'NONE',  ( -7.204075437095967871, 7.204075437095967871, 67.84375000204836681 ) ) ;
#2525=LINE ( 'NONE', #25517, #63460 ) ;
#2532=CARTESIAN_POINT ( 'NONE',  ( -10.99999999999999822, -4.556349186104052151, 76.09375000000000000 ) ) ;
#2555=( BOUNDED_CURVE ( )  B_SPLINE_CURVE ( 2, ( #63208, #34569, #34942, #69625, #35309, #5885, #6628, #68134, #29632 ),
 .UNSPECIFIED., .F., .F. ) 
 B_SPLINE_CURVE_WITH_KNOTS ( ( 3, 2, 2, 2, 3 ),
 ( 0.7352941176470587648, 0.7389705882352940458, 0.7426470588235294379, 0.7463235294117647189, 0.7500000000000000000 ),
 .UNSPECIFIED. ) 
 CURVE ( )  GEOMETRIC_REPRESENTATION_ITEM ( )  RATIONAL_B_SPLINE_CURVE ( ( 1.000000000000002220, 0.9238795325112844070, 1.000000000000000000, 0.9238795325112867385, 1.000000000000000000, 0.9238795325112867385, 1.000000000000000000, 0.9238795325112867385, 1.000000000000000000 ) ) 
 REPRESENTATION_ITEM ( '' )  );
#2560=CARTESIAN_POINT ( 'NONE',  ( -10.18810118749999738, -4.220049686691941915, 87.62500000204836681 ) ) ;
#2561=CARTESIAN_POINT ( 'NONE',  ( -7.204075437095967871, 7.204075437095967871, 113.9687500020483810 ) ) ;
#2574=CARTESIAN_POINT ( 'NONE',  ( -7.204075437095967871, 7.204075437095967871, 108.3437500020483810 ) ) ;
#2596=EDGE_CURVE ( 'NONE', #13320, #25175, #35974, .T. ) ;
#2610=CARTESIAN_POINT ( 'NONE',  ( -4.556349186104045934, 11.00000000000000000, 83.21874999999998579 ) ) ;
#2612=VERTEX_POINT ( 'NONE', #72914 ) ;
#2613=VERTEX_POINT ( 'NONE', #38595 ) ;
#2614=CARTESIAN_POINT ( 'NONE',  ( 10.18810118750000093, -4.220049686691933033, 83.31250000204836681 ) ) ;
#2617=CARTESIAN_POINT ( 'NONE',  ( -4.556349186104047710, -10.99999999999999822, 92.78124999999998579 ) ) ;
#2633=CARTESIAN_POINT ( 'NONE',  ( 0.000000000000000000, 0.000000000000000000, 118.0000000000000000 ) ) ;
#2634=CARTESIAN_POINT ( 'NONE',  ( -7.778174593052020747, -7.778174593052023411, 112.3750000040967763 ) ) ;
#2641=EDGE_LOOP ( 'NONE', ( #4450, #8629, #2872, #51592 ) ) ;
#2645=CARTESIAN_POINT ( 'NONE',  ( -6.735557395310442023E-16, 11.00000000000000000, 81.81250000409677625 ) ) ;
#2659=CARTESIAN_POINT ( 'NONE',  ( -7.204075437095967871, 7.204075437095967871, 76.46875000204836681 ) ) ;
#2661=CARTESIAN_POINT ( 'NONE',  ( 4.556349186104045934, 11.00000000000000000, 92.21875000409677625 ) ) ;
#2668=CARTESIAN_POINT ( 'NONE',  ( -6.238412754330611322E-16, 10.18810118749999916, 88.65625000204838102 ) ) ;
#2672=CARTESIAN_POINT ( 'NONE',  ( 2.020667218593132706E-15, -11.00000000000000000, 90.06250000409676204 ) ) ;
#2676=CARTESIAN_POINT ( 'NONE',  ( -10.18810118749999916, 0.000000000000000000, 99.15625000204838102 ) ) ;
#2684=CARTESIAN_POINT ( 'NONE',  ( -10.18810118749999738, -4.220049686691941915, 96.62500000204838102 ) ) ;
#2700=CARTESIAN_POINT ( 'NONE',  ( -10.18810118749999738, -4.220049686691941915, 96.25000000204838102 ) ) ;
#2701=CARTESIAN_POINT ( 'NONE',  ( 11.00000000000000000, 1.347111479062088405E-15, 114.4375000040967763 ) ) ;
#2711=CARTESIAN_POINT ( 'NONE',  ( -4.556349186104048599, -10.99999999999999822, 109.2812500000000000 ) ) ;
#2718=CARTESIAN_POINT ( 'NONE',  ( 4.556349186104051263, -10.99999999999999822, 112.4687499999999858 ) ) ;
#2730=CARTESIAN_POINT ( 'NONE',  ( 2.020667218593132706E-15, -11.00000000000000000, 100.5625000040967763 ) ) ;
#2734=CARTESIAN_POINT ( 'NONE',  ( 7.778174593052023411, -7.778174593052021635, 108.0624999999999858 ) ) ;
#2744=CARTESIAN_POINT ( 'NONE',  ( 11.00000000000000000, 1.347111479062088405E-15, 70.74999999999998579 ) ) ;
#2755=CARTESIAN_POINT ( 'NONE',  ( 7.204075437095968759, -7.204075437095966983, 103.0937500020483668 ) ) ;
#2759=LINE ( 'NONE', #25004, #13513 ) ;
#2763=CARTESIAN_POINT ( 'NONE',  ( -7.204075437095965206, -7.204075437095968759, 72.71875000204838102 ) ) ;
#2776=CARTESIAN_POINT ( 'NONE',  ( 1.871523826299183495E-15, -10.18810118749999916, 114.9062500020483810 ) ) ;
#2780=ORIENTED_EDGE ( 'NONE', *, *, #5070, .F. ) ;
#2805=CARTESIAN_POINT ( 'NONE',  ( 11.00000000000000000, 1.347111479062088405E-15, 118.0000000000000000 ) ) ;
#2818=VECTOR ( 'NONE', #31930, 1000.000000000000000 ) ;
#2832=CARTESIAN_POINT ( 'NONE',  ( 4.556349186104052151, -10.99999999999999822, 82.46874999999998579 ) ) ;
#2838=CARTESIAN_POINT ( 'NONE',  ( -6.238412754330611322E-16, 10.18810118749999916, 97.28125000204838102 ) ) ;
#2848=CARTESIAN_POINT ( 'NONE',  ( -11.00000000000000000, 0.000000000000000000, 77.49999999999998579 ) ) ;
#2854=CARTESIAN_POINT ( 'NONE',  ( -4.220049686691935698, 10.18810118749999916, 88.75000000204836681 ) ) ;
#2860=CARTESIAN_POINT ( 'NONE',  ( 4.220049686691934809, 10.18810118749999916, 75.06250000204836681 ) ) ;
#2868=CARTESIAN_POINT ( 'NONE',  ( 7.204075437095966983, 7.204075437095967871, 82.09375000204838102 ) ) ;
#2872=ORIENTED_EDGE ( 'NONE', *, *, #56977, .F. ) ;
#2903=CARTESIAN_POINT ( 'NONE',  ( 11.00000000000000355, -4.556349186104045046, 78.15624999999998579 ) ) ;
#2909=DIRECTION ( 'NONE',  ( -0.000000000000000000, -0.000000000000000000, -1.000000000000000000 ) ) ;
#2913=CARTESIAN_POINT ( 'NONE',  ( 7.778174593052021635, 7.778174593052023411, 116.1250000040967905 ) ) ;
#2929=VERTEX_POINT ( 'NONE', #49295 ) ;
#2930=CARTESIAN_POINT ( 'NONE',  ( 10.18810118750000093, -4.220049686691933921, 89.68750000204836681 ) ) ;
#2932=CARTESIAN_POINT ( 'NONE',  ( 4.220049686691941027, -10.18810118749999738, 111.6250000020483810 ) ) ;
#2944=CARTESIAN_POINT ( 'NONE',  ( 1.871523826299183495E-15, -10.18810118749999916, 104.4062500020483810 ) ) ;
#2965=ADVANCED_FACE ( 'NONE', ( #60994 ), #25798, .T. ) ;
#2982=CARTESIAN_POINT ( 'NONE',  ( -6.238412754330611322E-16, 10.18810118749999916, 80.78125000204838102 ) ) ;
#2985=CARTESIAN_POINT ( 'NONE',  ( -7.778174593052023411, 7.778174593052023411, 93.81250000000000000 ) ) ;
#2990=CARTESIAN_POINT ( 'NONE',  ( 4.556349186104045934, 11.00000000000000000, 89.03124999999998579 ) ) ;
#2993=( BOUNDED_CURVE ( )  B_SPLINE_CURVE ( 2, ( #37983, #48532, #8931, #9303, #60230, #65524, #54965, #20609, #3274 ),
 .UNSPECIFIED., .F., .F. ) 
 B_SPLINE_CURVE_WITH_KNOTS ( ( 3, 2, 2, 2, 3 ),
 ( 0.05882352941176474670, 0.06250000000000004163, 0.06617647058823533657, 0.06985294117647064538, 0.07352941176470594031 ),
 .UNSPECIFIED. ) 
 CURVE ( )  GEOMETRIC_REPRESENTATION_ITEM ( )  RATIONAL_B_SPLINE_CURVE ( ( 0.9999999999999991118, 0.9238795325112876267, 1.000000000000000000, 0.9238795325112867385, 1.000000000000000000, 0.9238795325112867385, 1.000000000000000000, 0.9238795325112856283, 1.000000000000001110 ) ) 
 REPRESENTATION_ITEM ( '' )  );
#3009=ADVANCED_FACE ( 'NONE', ( #64474 ), #41460, .T. ) ;
#3015=CARTESIAN_POINT ( 'NONE',  ( 2.020667218593132706E-15, -11.00000000000000000, 81.06250000409677625 ) ) ;
#3033=CARTESIAN_POINT ( 'NONE',  ( -7.204075437095965206, -7.204075437095968759, 76.84375000204838102 ) ) ;
#3042=CARTESIAN_POINT ( 'NONE',  ( 4.220049686691934809, 10.18810118749999916, 88.56250000204836681 ) ) ;
#3048=CARTESIAN_POINT ( 'NONE',  ( -10.18810118749999916, 4.220049686691934809, 93.06250000204839523 ) ) ;
#3057=CARTESIAN_POINT ( 'NONE',  ( 1.871523826299183495E-15, -10.18810118749999916, 95.40625000204836681 ) ) ;
#3073=CARTESIAN_POINT ( 'NONE',  ( 4.220049686691934809, 10.18810118749999916, 95.68750000204838102 ) ) ;
#3084=EDGE_CURVE ( 'NONE', #20382, #25230, #5137, .T. ) ;
#3093=CARTESIAN_POINT ( 'NONE',  ( -7.778174593052023411, 7.778174593052023411, 111.8125000000000000 ) ) ;
#3106=CARTESIAN_POINT ( 'NONE',  ( 7.778174593052021635, 7.778174593052023411, 98.12500000409676204 ) ) ;
#3132=CARTESIAN_POINT ( 'NONE',  ( 10.18810118750000093, -4.220049686691933921, 103.1875000020483810 ) ) ;
#3138=CARTESIAN_POINT ( 'NONE',  ( -7.204075437095965206, -7.204075437095968759, 71.21875000204836681 ) ) ;
#3150=CARTESIAN_POINT ( 'NONE',  ( 7.204075437095968759, -7.204075437095966983, 113.5937500020483810 ) ) ;
#3163=CARTESIAN_POINT ( 'NONE',  ( 4.556349186104045934, 11.00000000000000000, 90.53125000000000000 ) ) ;
#3164=ORIENTED_EDGE ( 'NONE', *, *, #25724, .F. ) ;
#3165=CARTESIAN_POINT ( 'NONE',  ( -4.220049686691935698, 10.18810118749999916, 113.8750000020483810 ) ) ;
#3173=CARTESIAN_POINT ( 'NONE',  ( -11.00000000000000533, 11.00000000000000000, 41.99999999999999289 ) ) ;
#3178=CARTESIAN_POINT ( 'NONE',  ( 0.000000000000000000, 0.000000000000000000, 118.0000000000000000 ) ) ;
#3183=CARTESIAN_POINT ( 'NONE',  ( 0.000000000000000000, 0.000000000000000000, 118.0000000000000000 ) ) ;
#3186=CARTESIAN_POINT ( 'NONE',  ( -10.99999999999989164, -4.556349186104158733, 89.59374999999998579 ) ) ;
#3191=CARTESIAN_POINT ( 'NONE',  ( 5.094045771088254959, 8.823157229062946527, 67.15552375567561683 ) ) ;
#3193=CARTESIAN_POINT ( 'NONE',  ( -11.00000000000000533, -11.00000000000000355, 41.99999999999999289 ) ) ;
#3198=DIRECTION ( 'NONE',  ( 1.000000000000000000, 0.000000000000000000, 0.000000000000000000 ) ) ;
#3213=ORIENTED_EDGE ( 'NONE', *, *, #69031, .F. ) ;
#3215=CARTESIAN_POINT ( 'NONE',  ( 4.220049686691934809, 10.18810118749999916, 97.18750000204836681 ) ) ;
#3216=CYLINDRICAL_SURFACE ( 'NONE', #51380, 11.00000000000000000 ) ;
#3229=CARTESIAN_POINT ( 'NONE',  ( 10.18810118749999916, 1.247682550866122264E-15, 89.78125000204836681 ) ) ;
#3244=CARTESIAN_POINT ( 'NONE',  ( -7.204075437095967871, 7.204075437095967871, 85.46875000204836681 ) ) ;
#3255=VERTEX_POINT ( 'NONE', #54639 ) ;
#3273=CARTESIAN_POINT ( 'NONE',  ( -15.99999999999999645, 15.99999999999999645, 20.00000000000000000 ) ) ;
#3274=CARTESIAN_POINT ( 'NONE',  ( 11.00000000000000000, 1.347111479062088405E-15, 114.2499999999999858 ) ) ;
#3278=CARTESIAN_POINT ( 'NONE',  ( 4.556349186104045934, 11.00000000000000000, 72.53124999999998579 ) ) ;
#3291=CARTESIAN_POINT ( 'NONE',  ( -11.00000000000000533, 11.00000000000000000, 41.99999999999999289 ) ) ;
#3305=CARTESIAN_POINT ( 'NONE',  ( -4.220049686691937474, -10.18810118749999738, 84.81250000204838102 ) ) ;
#3306=CARTESIAN_POINT ( 'NONE',  ( -4.220049686691935698, 10.18810118749999916, 115.3750000020483810 ) ) ;
#3309=LINE ( 'NONE', #31979, #34045 ) ;
#3318=CARTESIAN_POINT ( 'NONE',  ( -4.220049686691937474, -10.18810118749999738, 105.8125000020483952 ) ) ;
#3334=DIRECTION ( 'NONE',  ( -0.000000000000000000, -0.000000000000000000, -1.000000000000000000 ) ) ;
#3356=CARTESIAN_POINT ( 'NONE',  ( 7.204075437095966983, 7.204075437095967871, 79.09375000204838102 ) ) ;
#3359=CARTESIAN_POINT ( 'NONE',  ( -11.00000000000000000, 4.556349186104045934, 89.40625000000000000 ) ) ;
#3377=CARTESIAN_POINT ( 'NONE',  ( -11.00000000000000000, 0.000000000000000000, 118.0000000000000000 ) ) ;
#3390=CARTESIAN_POINT ( 'NONE',  ( 7.778174593052021635, 7.778174593052023411, 80.12500000409677625 ) ) ;
#3392=LINE ( 'NONE', #61099, #66102 ) ;
#3393=LINE ( 'NONE', #54337, #61214 ) ;
#3401=EDGE_LOOP ( 'NONE', ( #24639, #63539, #3626 ) ) ;
#3406=CARTESIAN_POINT ( 'NONE',  ( 10.99999999999999645, -10.99999999999999645, 41.99999999999999289 ) ) ;
#3407=CARTESIAN_POINT ( 'NONE',  ( -10.18810118749999916, 0.000000000000000000, 78.15625000204836681 ) ) ;
#3408=CARTESIAN_POINT ( 'NONE',  ( -11.00000000000000000, 0.000000000000000000, 118.0000000000000000 ) ) ;
#3415=CARTESIAN_POINT ( 'NONE',  ( 7.204075437095968759, -7.204075437095966983, 88.09375000204836681 ) ) ;
#3416=ORIENTED_EDGE ( 'NONE', *, *, #52675, .T. ) ;
#3419=CARTESIAN_POINT ( 'NONE',  ( 4.220049686691934809, 10.18810118749999916, 95.68750000204838102 ) ) ;
#3426=CARTESIAN_POINT ( 'NONE',  ( -10.18810118749999916, 4.220049686691934809, 91.93750000204836681 ) ) ;
#3428=DIRECTION ( 'NONE',  ( -0.000000000000000000, -0.000000000000000000, -1.000000000000000000 ) ) ;
#3445=CARTESIAN_POINT ( 'NONE',  ( 4.220049686691934809, 10.18810118749999916, 100.1875000020483952 ) ) ;
#3456=FACE_OUTER_BOUND ( 'NONE', #7297, .T. ) ;
#3468=EDGE_CURVE ( 'NONE', #8618, #74545, #56135, .T. ) ;
#3471=CARTESIAN_POINT ( 'NONE',  ( 11.00000000000000000, 1.347111479062088405E-15, 102.2500000000000000 ) ) ;
#3479=CARTESIAN_POINT ( 'NONE',  ( 7.778174593052023411, -7.778174593052021635, 100.7500000040967763 ) ) ;
#3494=ORIENTED_EDGE ( 'NONE', *, *, #22892, .F. ) ;
#3502=DIRECTION ( 'NONE',  ( -1.000000000000000000, 0.000000000000000000, 0.000000000000000000 ) ) ;
#3503=CARTESIAN_POINT ( 'NONE',  ( 7.204075437095968759, -7.204075437095966983, 101.5937500020483668 ) ) ;
#3509=CARTESIAN_POINT ( 'NONE',  ( -10.18810118749999738, -4.220049686691941915, 68.12500000204838102 ) ) ;
#3512=CARTESIAN_POINT ( 'NONE',  ( -4.220049686691935698, 10.18810118749999916, 110.8750000020483810 ) ) ;
#3522=CARTESIAN_POINT ( 'NONE',  ( -10.18810118749999738, -4.220049686691941915, 111.6250000020483810 ) ) ;
#3523=EDGE_CURVE ( 'NONE', #1216, #41579, #14846, .T. ) ;
#3536=ORIENTED_EDGE ( 'NONE', *, *, #16971, .F. ) ;
#3537=CARTESIAN_POINT ( 'NONE',  ( 10.18810118750000093, -4.220049686691933033, 116.3125000020483810 ) ) ;
#3538=CARTESIAN_POINT ( 'NONE',  ( 11.00000000000010836, -4.556349186103939353, 84.34375000409677625 ) ) ;
#3553=CARTESIAN_POINT ( 'NONE',  ( -4.556349186104048599, -10.99999999999999822, 94.28124999999998579 ) ) ;
#3558=CARTESIAN_POINT ( 'NONE',  ( -7.778174593052020747, -7.778174593052023411, 110.6875000000000000 ) ) ;
#3561=CARTESIAN_POINT ( 'NONE',  ( 0.000000000000000000, 0.000000000000000000, 118.0000000000000000 ) ) ;
#3566=DIRECTION ( 'NONE',  ( -1.000000000000000000, 0.000000000000000000, 0.000000000000000000 ) ) ;
#3581=EDGE_LOOP ( 'NONE', ( #293, #43508, #53671, #42316 ) ) ;
#3588=CARTESIAN_POINT ( 'NONE',  ( 10.18810118749999916, 1.247682550866122264E-15, 95.40625000204836681 ) ) ;
#3593=CARTESIAN_POINT ( 'NONE',  ( 11.00000000000000000, 1.347111479062088405E-15, 96.24999999999998579 ) ) ;
#3601=CARTESIAN_POINT ( 'NONE',  ( 4.220049686691941027, -10.18810118749999738, 82.00000000204838102 ) ) ;
#3608=CARTESIAN_POINT ( 'NONE',  ( 0.000000000000000000, 0.000000000000000000, 118.0000000000000000 ) ) ;
#3613=ADVANCED_FACE ( 'NONE', ( #54869 ), #60135, .T. ) ;
#3616=CARTESIAN_POINT ( 'NONE',  ( 4.220049686691941027, -10.18810118749999738, 81.62500000204836681 ) ) ;
#3618=EDGE_CURVE ( 'NONE', #54736, #47864, #58539, .T. ) ;
#3619=CARTESIAN_POINT ( 'NONE',  ( -7.778174593052023411, 7.778174593052023411, 110.3125000000000000 ) ) ;
#3626=ORIENTED_EDGE ( 'NONE', *, *, #24136, .F. ) ;
#3628=CARTESIAN_POINT ( 'NONE',  ( 11.00000000000000000, 1.347111479062088405E-15, 76.74999999999998579 ) ) ;
#3647=CARTESIAN_POINT ( 'NONE',  ( 11.00000000000000000, 4.556349186104045934, 70.84374999999997158 ) ) ;
#3655=CARTESIAN_POINT ( 'NONE',  ( 2.020667218593132706E-15, -11.00000000000000000, 114.0625000040967763 ) ) ;
#3677=CARTESIAN_POINT ( 'NONE',  ( -4.220049686691937474, -10.18810118749999738, 112.9375000020483810 ) ) ;
#3681=CARTESIAN_POINT ( 'NONE',  ( 2.020667218593132706E-15, -11.00000000000000000, 106.3750000000000000 ) ) ;
#3694=CARTESIAN_POINT ( 'NONE',  ( -10.18810118749999738, -4.220049686691941915, 108.6250000020483668 ) ) ;
#3721=DIRECTION ( 'NONE',  ( -0.000000000000000000, -0.000000000000000000, -1.000000000000000000 ) ) ;
#3732=CARTESIAN_POINT ( 'NONE',  ( -10.18810118749999738, -4.220049686691941915, 82.75000000204838102 ) ) ;
#3735=CARTESIAN_POINT ( 'NONE',  ( -7.778174593052020747, -7.778174593052023411, 91.18749999999998579 ) ) ;
#3764=CARTESIAN_POINT ( 'NONE',  ( 2.020667218593132706E-15, -11.00000000000000000, 78.06250000409677625 ) ) ;
#3767=AXIS2_PLACEMENT_3D ( 'NONE', #14042, #8401, #60452 ) ;
#3780=EDGE_LOOP ( 'NONE', ( #40358, #11191, #18710, #29366 ) ) ;
#3782=CARTESIAN_POINT ( 'NONE',  ( 7.204075437095968759, -7.204075437095966983, 78.71875000204836681 ) ) ;
#3786=CIRCLE ( 'NONE', #39907, 34.85072926314708752 ) ;
#3792=CARTESIAN_POINT ( 'NONE',  ( 10.18810118749999916, 4.220049686691935698, 86.87500000204836681 ) ) ;
#3795=CARTESIAN_POINT ( 'NONE',  ( 7.778174593052023411, -7.778174593052021635, 90.25000000409677625 ) ) ;
#3798=CARTESIAN_POINT ( 'NONE',  ( -10.18810118749999916, 4.220049686691934809, 97.56250000204836681 ) ) ;
#3808=CARTESIAN_POINT ( 'NONE',  ( -10.18810118749999738, -4.220049686691941915, 92.12500000204836681 ) ) ;
#3825=ORIENTED_EDGE ( 'NONE', *, *, #27919, .F. ) ;
#3826=CARTESIAN_POINT ( 'NONE',  ( -10.18810118749999738, -4.220049686691941915, 100.7500000020483810 ) ) ;
#3829=CARTESIAN_POINT ( 'NONE',  ( 7.778174593052021635, 7.778174593052023411, 109.9375000000000000 ) ) ;
#3861=CARTESIAN_POINT ( 'NONE',  ( -11.00000000000000000, 4.556349186104045934, 100.0937500040967905 ) ) ;
#3882=CARTESIAN_POINT ( 'NONE',  ( -11.00000000000000000, 0.000000000000000000, 69.99999999999998579 ) ) ;
#3883=CARTESIAN_POINT ( 'NONE',  ( -10.18810118749999738, -4.220049686691941915, 102.6250000020483810 ) ) ;
#3893=CARTESIAN_POINT ( 'NONE',  ( 1.871523826299183495E-15, -10.18810118749999916, 114.5312500020483810 ) ) ;
#3903=CARTESIAN_POINT ( 'NONE',  ( -4.220049686691935698, 10.18810118749999916, 109.7500000020483810 ) ) ;
#3905=AXIS2_PLACEMENT_3D ( 'NONE', #29404, #46736, #18073 ) ;
#3915=CARTESIAN_POINT ( 'NONE',  ( -11.00000000000000000, 0.000000000000000000, 98.49999999999998579 ) ) ;
#3923=CARTESIAN_POINT ( 'NONE',  ( 10.18810118749999916, 4.220049686691935698, 116.5000000020483810 ) ) ;
#3924=CARTESIAN_POINT ( 'NONE',  ( -11.00000000000000000, 0.000000000000000000, 83.68750000409677625 ) ) ;
#3935=CARTESIAN_POINT ( 'NONE',  ( 11.00000000000000355, -4.556349186104044158, 78.15624999999998579 ) ) ;
#3947=FACE_OUTER_BOUND ( 'NONE', #14700, .T. ) ;
#3952=CARTESIAN_POINT ( 'NONE',  ( -11.00000000000000000, 0.000000000000000000, 116.6875000040967763 ) ) ;
#3968=CARTESIAN_POINT ( 'NONE',  ( -4.556349186104048599, -10.99999999999999822, 82.28124999999998579 ) ) ;
#3974=CARTESIAN_POINT ( 'NONE',  ( -10.18810118749999916, 0.000000000000000000, 91.65625000204836681 ) ) ;
#3982=CARTESIAN_POINT ( 'NONE',  ( -6.735557395310442023E-16, 11.00000000000000000, 77.12499999999998579 ) ) ;
#3987=CARTESIAN_POINT ( 'NONE',  ( -7.204075437095965206, -7.204075437095968759, 84.71875000204836681 ) ) ;
#3993=DIRECTION ( 'NONE',  ( -0.000000000000000000, -0.000000000000000000, -1.000000000000000000 ) ) ;
#4000=CARTESIAN_POINT ( 'NONE',  ( -7.204075437095967871, 7.204075437095967871, 77.96875000204836681 ) ) ;
#4011=( BOUNDED_CURVE ( )  B_SPLINE_CURVE ( 2, ( #7731, #47705, #30372, #13002, #12639, #35670, #58685, #2438, #59785 ),
 .UNSPECIFIED., .F., .F. ) 
 B_SPLINE_CURVE_WITH_KNOTS ( ( 3, 2, 2, 2, 3 ),
 ( 0.9264705882352940458, 0.9301470588235294379, 0.9338235294117647189, 0.9375000000000000000, 0.9411764705882353921 ),
 .UNSPECIFIED. ) 
 CURVE ( )  GEOMETRIC_REPRESENTATION_ITEM ( )  RATIONAL_B_SPLINE_CURVE ( ( 1.000000000000002220, 0.9238795325112844070, 1.000000000000000000, 0.9238795325112867385, 1.000000000000000000, 0.9238795325112867385, 1.000000000000000000, 0.9238795325112844070, 1.000000000000002220 ) ) 
 REPRESENTATION_ITEM ( '' )  );
#4034=CARTESIAN_POINT ( 'NONE',  ( 7.778174593052021635, 7.778174593052023411, 70.93749999999998579 ) ) ;
#4037=CARTESIAN_POINT ( 'NONE',  ( -4.556349186104045934, 11.00000000000000000, 110.4062500040967620 ) ) ;
#4062=CARTESIAN_POINT ( 'NONE',  ( -4.220049686691937474, -10.18810118749999738, 106.9375000020483810 ) ) ;
#4075=CARTESIAN_POINT ( 'NONE',  ( -7.204075437095965206, -7.204075437095968759, 101.2187500020483668 ) ) ;
#4083=AXIS2_PLACEMENT_3D ( 'NONE', #26186, #25811, #3198 ) ;
#4095=CARTESIAN_POINT ( 'NONE',  ( -7.204075437095965206, -7.204075437095968759, 81.71875000204836681 ) ) ;
#4113=ORIENTED_EDGE ( 'NONE', *, *, #63748, .F. ) ;
#4114=CARTESIAN_POINT ( 'NONE',  ( -6.238412754330611322E-16, 10.18810118749999916, 71.78125000204838102 ) ) ;
#4117=CARTESIAN_POINT ( 'NONE',  ( 11.00000000000000000, 4.556349186104045934, 88.84374999999997158 ) ) ;
#4123=PLANE ( 'NONE',  #35981 ) ;
#4126=( BOUNDED_CURVE ( )  B_SPLINE_CURVE ( 2, ( #35962, #47631, #18972, #25357, #25723, #71377, #71752, #20066, #6916 ),
 .UNSPECIFIED., .F., .F. ) 
 B_SPLINE_CURVE_WITH_KNOTS ( ( 3, 2, 2, 2, 3 ),
 ( 0.5882352941176469674, 0.5919117647058822484, 0.5955882352941175295, 0.5992647058823528106, 0.6029411764705880916 ),
 .UNSPECIFIED. ) 
 CURVE ( )  GEOMETRIC_REPRESENTATION_ITEM ( )  RATIONAL_B_SPLINE_CURVE ( ( 1.000000000000002220, 0.9238795325112844070, 1.000000000000000000, 0.9238795325112867385, 1.000000000000000000, 0.9238795325112867385, 1.000000000000000000, 0.9238795325112890700, 0.9999999999999976685 ) ) 
 REPRESENTATION_ITEM ( '' )  );
#4146=CARTESIAN_POINT ( 'NONE',  ( 11.00000000000010836, -4.556349186103939353, 81.34375000409679046 ) ) ;
#4148=CARTESIAN_POINT ( 'NONE',  ( -4.556349186104045934, 11.00000000000000000, 80.40625000409676204 ) ) ;
#4166=CARTESIAN_POINT ( 'NONE',  ( 1.871523826299183495E-15, -10.18810118749999916, 78.53125000204836681 ) ) ;
#4168=CARTESIAN_POINT ( 'NONE',  ( 0.000000000000000000, 0.000000000000000000, 118.0000000000000000 ) ) ;
#4174=CARTESIAN_POINT ( 'NONE',  ( -4.220049686691935698, 10.18810118749999916, 84.25000000204838102 ) ) ;
#4177=CARTESIAN_POINT ( 'NONE',  ( -11.00000000000000000, 0.000000000000000000, 106.0000000000000000 ) ) ;
#4186=CARTESIAN_POINT ( 'NONE',  ( 1.871523826299183495E-15, -10.18810118749999916, 90.90625000204838102 ) ) ;
#4195=CARTESIAN_POINT ( 'NONE',  ( 11.00000000000000000, 1.347111479062088405E-15, 96.43750000409677625 ) ) ;
#4201=CARTESIAN_POINT ( 'NONE',  ( 10.18810118750000093, -4.220049686691933033, 95.31250000204838102 ) ) ;
#4203=CARTESIAN_POINT ( 'NONE',  ( -4.556349186104045934, 11.00000000000000000, 105.7187499999999716 ) ) ;
#4230=DIRECTION ( 'NONE',  ( -1.000000000000000000, -9.955163135201253416E-17, 0.000000000000000000 ) ) ;
#4234=CARTESIAN_POINT ( 'NONE',  ( -10.99999999999999822, -4.556349186104052151, 95.78125000409680467 ) ) ;
#4250=( BOUNDED_CURVE ( )  B_SPLINE_CURVE ( 2, ( #72191, #20503, #16609, #28321, #20133, #66165, #74339, #22647, #45667 ),
 .UNSPECIFIED., .F., .F. ) 
 B_SPLINE_CURVE_WITH_KNOTS ( ( 3, 2, 2, 2, 3 ),
 ( 0.05882352941176473976, 0.06250000000000004163, 0.06617647058823533657, 0.06985294117647063150, 0.07352941176470592644 ),
 .UNSPECIFIED. ) 
 CURVE ( )  GEOMETRIC_REPRESENTATION_ITEM ( )  RATIONAL_B_SPLINE_CURVE ( ( 0.9999999999999993339, 0.9238795325112874046, 1.000000000000000000, 0.9238795325112867385, 1.000000000000000000, 0.9238795325112867385, 1.000000000000000000, 0.9238795325112858503, 1.000000000000000888 ) ) 
 REPRESENTATION_ITEM ( '' )  );
#4255=CARTESIAN_POINT ( 'NONE',  ( -4.220049686691935698, 10.18810118749999916, 100.7500000020483526 ) ) ;
#4257=AXIS2_PLACEMENT_3D ( 'NONE', #53997, #24933, #20017 ) ;
#4260=CARTESIAN_POINT ( 'NONE',  ( -4.556349186104045934, 11.00000000000000000, 98.21875000000000000 ) ) ;
#4265=CARTESIAN_POINT ( 'NONE',  ( 10.18810118749999916, 4.220049686691935698, 115.0000000020483668 ) ) ;
#4273=CARTESIAN_POINT ( 'NONE',  ( 7.204075437095968759, -7.204075437095966983, 109.0937500020483810 ) ) ;
#4274=CARTESIAN_POINT ( 'NONE',  ( 11.00000000000000000, 1.347111479062088405E-15, 118.0000000000000000 ) ) ;
#4286=CARTESIAN_POINT ( 'NONE',  ( -11.00000000000021139, 4.556349186103834548, 90.90625000000001421 ) ) ;
#4288=CARTESIAN_POINT ( 'NONE',  ( -7.204075437095965206, -7.204075437095968759, 115.8437500020483810 ) ) ;
#4302=CARTESIAN_POINT ( 'NONE',  ( -11.00000000000000000, 0.000000000000000000, 118.0000000000000000 ) ) ;
#4316=CARTESIAN_POINT ( 'NONE',  ( -3.469446951953614189E-15, 16.00000000000000000, 38.34805510287551300 ) ) ;
#4338=CARTESIAN_POINT ( 'NONE',  ( 7.204075437095968759, -7.204075437095966983, 92.21875000204838102 ) ) ;
#4351=CARTESIAN_POINT ( 'NONE',  ( -4.220049686691935698, 10.18810118749999916, 81.25000000204838102 ) ) ;
#4364=CARTESIAN_POINT ( 'NONE',  ( 7.204075437095966983, 7.204075437095967871, 77.59375000204838102 ) ) ;
#4377=CARTESIAN_POINT ( 'NONE',  ( 4.556349186104052151, -10.99999999999999822, 73.65625000409676204 ) ) ;
#4385=ORIENTED_EDGE ( 'NONE', *, *, #16196, .F. ) ;
#4386=EDGE_CURVE ( 'NONE', #13669, #54736, #68654, .T. ) ;
#4399=CARTESIAN_POINT ( 'NONE',  ( 2.020667218593132706E-15, -11.00000000000000000, 68.87499999999998579 ) ) ;
#4424=CARTESIAN_POINT ( 'NONE',  ( -4.220049686691937474, -10.18810118749999738, 108.4375000020483668 ) ) ;
#4428=CARTESIAN_POINT ( 'NONE',  ( 11.00000000000000000, 1.347111479062088405E-15, 97.74999999999998579 ) ) ;
#4441=CARTESIAN_POINT ( 'NONE',  ( -7.204075437095967871, 7.204075437095967871, 103.8437500020483810 ) ) ;
#4450=ORIENTED_EDGE ( 'NONE', *, *, #5122, .T. ) ;
#4464=CARTESIAN_POINT ( 'NONE',  ( 10.18810118749999916, 1.247682550866122264E-15, 80.78125000204838102 ) ) ;
#4483=CARTESIAN_POINT ( 'NONE',  ( 7.204075437095968759, -7.204075437095966983, 77.21875000204836681 ) ) ;
#4486=CARTESIAN_POINT ( 'NONE',  ( 7.778174593052023411, -7.778174593052021635, 91.56249999999998579 ) ) ;
#4498=CARTESIAN_POINT ( 'NONE',  ( 4.556349186104052151, -10.99999999999999822, 99.15625000409677625 ) ) ;
#4513=CARTESIAN_POINT ( 'NONE',  ( 4.556349186104051263, -10.99999999999999822, 76.65625000409676204 ) ) ;
#4530=CARTESIAN_POINT ( 'NONE',  ( -4.220049686691935698, 10.18810118749999916, 71.87500000204836681 ) ) ;
#4533=DIRECTION ( 'NONE',  ( -0.000000000000000000, -0.000000000000000000, -1.000000000000000000 ) ) ;
#4539=CARTESIAN_POINT ( 'NONE',  ( 10.18810118750000093, -4.220049686691933921, 82.18750000204836681 ) ) ;
#4540=ORIENTED_EDGE ( 'NONE', *, *, #37, .T. ) ;
#4552=CARTESIAN_POINT ( 'NONE',  ( -10.18810118749999738, -4.220049686691941915, 90.62500000204836681 ) ) ;
#4565=LINE ( 'NONE', #27561, #28208 ) ;
#4568=EDGE_LOOP ( 'NONE', ( #18836, #10683, #54483, #26196, #69493, #24018, #2236, #27772, #52286 ) ) ;
#4569=CARTESIAN_POINT ( 'NONE',  ( -7.204075437095965206, -7.204075437095968759, 94.84375000204838102 ) ) ;
#4572=CARTESIAN_POINT ( 'NONE',  ( 11.00000000000000355, -4.556349186104045046, 106.6562500000000000 ) ) ;
#4577=AXIS2_PLACEMENT_3D ( 'NONE', #56879, #5563, #50452 ) ;
#4581=AXIS2_PLACEMENT_3D ( 'NONE', #14875, #8482, #43179 ) ;
#4588=CARTESIAN_POINT ( 'NONE',  ( 11.00000000000010658, 4.556349186103942017, 111.3437499999999858 ) ) ;
#4602=CARTESIAN_POINT ( 'NONE',  ( -11.00000000000000000, 4.556349186104045934, 92.59375000409677625 ) ) ;
#4623=CARTESIAN_POINT ( 'NONE',  ( 7.204075437095966983, 7.204075437095967871, 97.46875000204838102 ) ) ;
#4635=CARTESIAN_POINT ( 'NONE',  ( 10.18810118750000093, -4.220049686691933921, 111.8125000020483952 ) ) ;
#4642=VECTOR ( 'NONE', #2909, 1000.000000000000000 ) ;
#4647=CARTESIAN_POINT ( 'NONE',  ( -10.18810118749999916, 4.220049686691934809, 108.4375000020483668 ) ) ;
#4659=( BOUNDED_CURVE ( )  B_SPLINE_CURVE ( 2, ( #3593, #43569, #37554, #9251, #60929, #44701, #32272, #4717, #27334 ),
 .UNSPECIFIED., .F., .F. ) 
 B_SPLINE_CURVE_WITH_KNOTS ( ( 3, 2, 2, 2, 3 ),
 ( 0.4264705882352941568, 0.4301470588235294934, 0.4338235294117647745, 0.4375000000000000555, 0.4411764705882353366 ),
 .UNSPECIFIED. ) 
 CURVE ( )  GEOMETRIC_REPRESENTATION_ITEM ( )  RATIONAL_B_SPLINE_CURVE ( ( 0.9999999999999988898, 0.9238795325112878487, 1.000000000000000000, 0.9238795325112867385, 1.000000000000000000, 0.9238795325112867385, 1.000000000000000000, 0.9238795325112856283, 1.000000000000001110 ) ) 
 REPRESENTATION_ITEM ( '' )  );
#4662=CARTESIAN_POINT ( 'NONE',  ( -4.220049686691935698, 10.18810118749999916, 107.8750000020483810 ) ) ;
#4678=CARTESIAN_POINT ( 'NONE',  ( 11.00000000000010658, 4.556349186103942017, 107.0312500040967763 ) ) ;
#4684=CARTESIAN_POINT ( 'NONE',  ( 0.000000000000000000, 0.000000000000000000, 118.0000000000000000 ) ) ;
#4706=CARTESIAN_POINT ( 'NONE',  ( -6.735557395310442023E-16, 11.00000000000000000, 104.1250000000000000 ) ) ;
#4712=CARTESIAN_POINT ( 'NONE',  ( -10.18810118749999916, 4.220049686691934809, 91.56250000204836681 ) ) ;
#4717=CARTESIAN_POINT ( 'NONE',  ( -11.00000000000004796, -4.556349186104000637, 95.59375000000000000 ) ) ;
#4724=CARTESIAN_POINT ( 'NONE',  ( 4.220049686691934809, 10.18810118749999916, 82.56250000204836681 ) ) ;
#4726=ORIENTED_EDGE ( 'NONE', *, *, #65207, .T. ) ;
#4739=CARTESIAN_POINT ( 'NONE',  ( -4.220049686691935698, 10.18810118749999916, 79.37500000204838102 ) ) ;
#4770=DIRECTION ( 'NONE',  ( -0.000000000000000000, -0.000000000000000000, -1.000000000000000000 ) ) ;
#4775=CARTESIAN_POINT ( 'NONE',  ( -4.556349186104047710, -10.99999999999999822, 73.28125000000000000 ) ) ;
#4802=VECTOR ( 'NONE', #33378, 1000.000000000000000 ) ;
#4803=CARTESIAN_POINT ( 'NONE',  ( -7.204075437095967871, 7.204075437095967871, 106.4687500020483810 ) ) ;
#4818=CARTESIAN_POINT ( 'NONE',  ( -4.220049686691935698, 10.18810118749999916, 99.25000000204838102 ) ) ;
#4823=CARTESIAN_POINT ( 'NONE',  ( -11.00000000000000000, 0.000000000000000000, 106.1875000040967620 ) ) ;
#4834=EDGE_LOOP ( 'NONE', ( #63727, #47482, #30784, #4385 ) ) ;
#4840=CARTESIAN_POINT ( 'NONE',  ( 10.18810118749999916, 1.247682550866122264E-15, 79.28125000204836681 ) ) ;
#4847=DIRECTION ( 'NONE',  ( -0.000000000000000000, -0.000000000000000000, -1.000000000000000000 ) ) ;
#4859=CARTESIAN_POINT ( 'NONE',  ( -10.18810118749999738, -4.220049686691941915, 76.75000000204838102 ) ) ;
#4862=CARTESIAN_POINT ( 'NONE',  ( -10.99999999999999822, -4.556349186104052151, 86.59375000000000000 ) ) ;
#4887=CARTESIAN_POINT ( 'NONE',  ( -7.778174593052020747, -7.778174593052023411, 76.37500000409677625 ) ) ;
#4909=CARTESIAN_POINT ( 'NONE',  ( 4.220049686691941027, -10.18810118749999738, 74.12500000204836681 ) ) ;
#4919=CARTESIAN_POINT ( 'NONE',  ( -7.204075437095967871, 7.204075437095967871, 78.34375000204838102 ) ) ;
#4946=CARTESIAN_POINT ( 'NONE',  ( -4.220049686691937474, -10.18810118749999738, 94.93750000204836681 ) ) ;
#4949=CARTESIAN_POINT ( 'NONE',  ( -11.00000000000000000, 4.556349186104045934, 104.4062500000000000 ) ) ;
#4979=CARTESIAN_POINT ( 'NONE',  ( 4.556349186104051263, -10.99999999999999822, 94.65625000409680467 ) ) ;
#5000=AXIS2_PLACEMENT_3D ( 'NONE', #9447, #56219, #21125 ) ;
#5003=CARTESIAN_POINT ( 'NONE',  ( -6.238412754330611322E-16, 10.18810118749999916, 96.15625000204838102 ) ) ;
#5011=CARTESIAN_POINT ( 'NONE',  ( 1.871523826299183495E-15, -10.18810118749999916, 113.0312500020483810 ) ) ;
#5021=CARTESIAN_POINT ( 'NONE',  ( 4.220049686691934809, 10.18810118749999916, 108.0625000020483810 ) ) ;
#5023=CARTESIAN_POINT ( 'NONE',  ( -6.735557395310442023E-16, 11.00000000000000000, 75.62499999999998579 ) ) ;
#5034=ORIENTED_EDGE ( 'NONE', *, *, #6641, .F. ) ;
#5037=CARTESIAN_POINT ( 'NONE',  ( -10.18810118749999916, 4.220049686691934809, 111.0625000020483810 ) ) ;
#5064=CARTESIAN_POINT ( 'NONE',  ( 11.00000000000000355, -4.556349186104045046, 111.3437500040967763 ) ) ;
#5066=DIRECTION ( 'NONE',  ( -1.000000000000000000, 0.000000000000000000, 0.000000000000000000 ) ) ;
#5070=EDGE_CURVE ( 'NONE', #45401, #15013, #17551, .T. ) ;
#5080=CARTESIAN_POINT ( 'NONE',  ( 7.778174593052021635, 7.778174593052023411, 115.9375000000000000 ) ) ;
#5087=CARTESIAN_POINT ( 'NONE',  ( -4.220049686691937474, -10.18810118749999738, 88.93750000204839523 ) ) ;
#5092=CARTESIAN_POINT ( 'NONE',  ( 7.204075437095966983, 7.204075437095967871, 116.9687500020483810 ) ) ;
#5093=ORIENTED_EDGE ( 'NONE', *, *, #33466, .F. ) ;
#5094=CARTESIAN_POINT ( 'NONE',  ( 7.778174593052021635, 7.778174593052023411, 108.6250000040967763 ) ) ;
#5100=CARTESIAN_POINT ( 'NONE',  ( -10.18810118749999916, 0.000000000000000000, 81.53125000204838102 ) ) ;
#5107=AXIS2_PLACEMENT_3D ( 'NONE', #36163, #31987, #37652 ) ;
#5113=CARTESIAN_POINT ( 'NONE',  ( -10.18810118749999916, 4.220049686691934809, 75.06250000204836681 ) ) ;
#5116=CARTESIAN_POINT ( 'NONE',  ( 4.556349186104045934, 11.00000000000000000, 110.0312500000000000 ) ) ;
#5122=EDGE_CURVE ( 'NONE', #22824, #12782, #65914, .T. ) ;
#5137=CIRCLE ( 'NONE', #3905, 34.85072926314708752 ) ;
#5152=CARTESIAN_POINT ( 'NONE',  ( 11.00000000000000000, 1.347111479062088405E-15, 84.43750000409677625 ) ) ;
#5174=CARTESIAN_POINT ( 'NONE',  ( 7.204075437095966983, 7.204075437095967871, 104.5937500020483810 ) ) ;
#5177=CARTESIAN_POINT ( 'NONE',  ( -10.99999999999989164, -4.556349186104158733, 106.0937500000000142 ) ) ;
#5190=CARTESIAN_POINT ( 'NONE',  ( 7.204075437095966983, 7.204075437095967871, 100.4687500020483810 ) ) ;
#5192=ORIENTED_EDGE ( 'NONE', *, *, #10905, .F. ) ;
#5202=CARTESIAN_POINT ( 'NONE',  ( -4.220049686691935698, 10.18810118749999916, 95.87500000204838102 ) ) ;
#5209=CARTESIAN_POINT ( 'NONE',  ( 4.220049686691934809, 10.18810118749999916, 78.06250000204838102 ) ) ;
#5227=VERTEX_POINT ( 'NONE', #14094 ) ;
#5229=CARTESIAN_POINT ( 'NONE',  ( -10.18810118749999916, 0.000000000000000000, 72.15625000204836681 ) ) ;
#5232=CARTESIAN_POINT ( 'NONE',  ( 4.556349186104051263, -10.99999999999999822, 80.96874999999997158 ) ) ;
#5260=CARTESIAN_POINT ( 'NONE',  ( -4.556349186104047710, -10.99999999999999822, 73.46875000409677625 ) ) ;
#5266=EDGE_CURVE ( 'NONE', #73730, #6581, #41681, .T. ) ;
#5278=CARTESIAN_POINT ( 'NONE',  ( -6.238412754330611322E-16, 10.18810118749999916, 70.28125000204838102 ) ) ;
#5288=ORIENTED_EDGE ( 'NONE', *, *, #67533, .T. ) ;
#5302=AXIS2_PLACEMENT_3D ( 'NONE', #29190, #12927, #7288 ) ;
#5306=CYLINDRICAL_SURFACE ( 'NONE', #19291, 11.00000000000000000 ) ;
#5311=ADVANCED_FACE ( 'NONE', ( #48807 ), #49562, .F. ) ;
#5313=CARTESIAN_POINT ( 'NONE',  ( -7.204075437095967871, 7.204075437095967871, 91.46875000204838102 ) ) ;
#5316=CARTESIAN_POINT ( 'NONE',  ( -11.00000000000000000, 0.000000000000000000, 107.4999999999999858 ) ) ;
#5325=EDGE_CURVE ( 'NONE', #6581, #34878, #72338, .T. ) ;
#5346=CARTESIAN_POINT ( 'NONE',  ( -7.778174593052020747, -7.778174593052023411, 89.87500000409677625 ) ) ;
#5357=CARTESIAN_POINT ( 'NONE',  ( -4.556349186104045934, 11.00000000000000000, 102.9062500040967763 ) ) ;
#5370=CARTESIAN_POINT ( 'NONE',  ( 4.220049686691934809, 10.18810118749999916, 99.06250000204836681 ) ) ;
#5377=CARTESIAN_POINT ( 'NONE',  ( 10.18810118749999916, 4.220049686691935698, 104.5000000020483668 ) ) ;
#5385=CARTESIAN_POINT ( 'NONE',  ( 10.18810118750000093, -4.220049686691933921, 104.6875000020483810 ) ) ;
#5388=CARTESIAN_POINT ( 'NONE',  ( -11.00000000000000000, 0.000000000000000000, 75.99999999999998579 ) ) ;
#5392=EDGE_CURVE ( 'NONE', #62397, #32492, #4250, .T. ) ;
#5403=CARTESIAN_POINT ( 'NONE',  ( -4.220049686691935698, 10.18810118749999916, 110.8750000020483810 ) ) ;
#5414=CARTESIAN_POINT ( 'NONE',  ( -10.99999999999978684, -4.556349186104264426, 91.09375000000001421 ) ) ;
#5428=CARTESIAN_POINT ( 'NONE',  ( -11.00000000000000000, 0.000000000000000000, 110.6875000040967763 ) ) ;
#5453=CARTESIAN_POINT ( 'NONE',  ( 7.204075437095968759, -7.204075437095966983, 89.21875000204838102 ) ) ;
#5458=CARTESIAN_POINT ( 'NONE',  ( 7.204075437095966983, 7.204075437095967871, 115.4687500020483810 ) ) ;
#5466=CARTESIAN_POINT ( 'NONE',  ( -4.220049686691937474, -10.18810118749999738, 78.81250000204838102 ) ) ;
#5477=ADVANCED_FACE ( 'NONE', ( #58047 ), #51618, .T. ) ;
#5479=CARTESIAN_POINT ( 'NONE',  ( -4.220049686691935698, 10.18810118749999916, 76.37500000204838102 ) ) ;
#5502=CARTESIAN_POINT ( 'NONE',  ( -11.00000000000000000, 0.000000000000000000, 74.68750000409676204 ) ) ;
#5516=CARTESIAN_POINT ( 'NONE',  ( -4.556349186104045934, 11.00000000000000000, 107.2187499999999858 ) ) ;
#5539=CARTESIAN_POINT ( 'NONE',  ( -1.840719112916308964, 10.74941063447380785, 117.6042820761836794 ) ) ;
#5540=CARTESIAN_POINT ( 'NONE',  ( -10.18810118749999738, -4.220049686691941915, 106.7500000020483668 ) ) ;
#5558=CARTESIAN_POINT ( 'NONE',  ( 4.220049686691934809, 10.18810118749999916, 103.5625000020483810 ) ) ;
#5563=DIRECTION ( 'NONE',  ( -0.000000000000000000, 0.000000000000000000, 1.000000000000000000 ) ) ;
#5568=EDGE_LOOP ( 'NONE', ( #3536, #5744, #14073 ) ) ;
#5571=ADVANCED_FACE ( 'NONE', ( #57295 ), #29365, .T. ) ;
#5574=CARTESIAN_POINT ( 'NONE',  ( 7.204075437095968759, -7.204075437095966983, 98.21875000204838102 ) ) ;
#5584=CARTESIAN_POINT ( 'NONE',  ( -10.18810118749999916, 0.000000000000000000, 83.03125000204838102 ) ) ;
#5591=EDGE_CURVE ( 'NONE', #68586, #56611, #60633, .T. ) ;
#5598=VERTEX_POINT ( 'NONE', #1800 ) ;
#5603=CARTESIAN_POINT ( 'NONE',  ( -7.204075437095967871, 7.204075437095967871, 71.96875000204836681 ) ) ;
#5606=CARTESIAN_POINT ( 'NONE',  ( 4.556349186104045934, 11.00000000000000000, 83.03124999999998579 ) ) ;
#5609=CARTESIAN_POINT ( 'NONE',  ( 10.99999999999995026, -4.556349186104096560, 114.1562499999999716 ) ) ;
#5628=DIRECTION ( 'NONE',  ( -1.000000000000000000, 0.000000000000000000, 0.000000000000000000 ) ) ;
#5629=CARTESIAN_POINT ( 'NONE',  ( 5.499989586027935751, 9.526285454130809072, 66.68677389048282578 ) ) ;
#5631=CARTESIAN_POINT ( 'NONE',  ( -7.778174593052023411, 7.778174593052023411, 74.50000000409676204 ) ) ;
#5647=CARTESIAN_POINT ( 'NONE',  ( 7.204075437095968759, -7.204075437095966983, 69.71875000204836681 ) ) ;
#5683=CARTESIAN_POINT ( 'NONE',  ( -4.220049686691937474, -10.18810118749999738, 93.43750000204836681 ) ) ;
#5684=CARTESIAN_POINT ( 'NONE',  ( 7.778174593052021635, 7.778174593052023411, 91.93749999999998579 ) ) ;
#5686=CARTESIAN_POINT ( 'NONE',  ( -7.778174593052023411, 7.778174593052023411, 99.81250000000000000 ) ) ;
#5710=CARTESIAN_POINT ( 'NONE',  ( -10.99999999999989164, -4.556349186104158733, 88.09375000000000000 ) ) ;
#5715=CARTESIAN_POINT ( 'NONE',  ( -4.556349186104047710, -10.99999999999999822, 94.46875000409677625 ) ) ;
#5739=CARTESIAN_POINT ( 'NONE',  ( -6.238412754330611322E-16, 10.18810118749999916, 97.65625000204838102 ) ) ;
#5744=ORIENTED_EDGE ( 'NONE', *, *, #40247, .T. ) ;
#5746=CARTESIAN_POINT ( 'NONE',  ( -4.220049686691935698, 10.18810118749999916, 107.8750000020483668 ) ) ;
#5756=CARTESIAN_POINT ( 'NONE',  ( -4.220049686691935698, 10.18810118749999916, 102.2500000020483952 ) ) ;
#5761=DIRECTION ( 'NONE',  ( -0.000000000000000000, -0.000000000000000000, -1.000000000000000000 ) ) ;
#5766=VECTOR ( 'NONE', #47168, 1000.000000000000000 ) ;
#5776=CARTESIAN_POINT ( 'NONE',  ( -10.18810118749999738, -4.220049686691941915, 112.7500000020483810 ) ) ;
#5794=CARTESIAN_POINT ( 'NONE',  ( 2.729886528703372228, 10.18810118749999916, 67.59560454024895648 ) ) ;
#5804=CARTESIAN_POINT ( 'NONE',  ( 11.00000000000000355, -4.556349186104045046, 112.8437500040967620 ) ) ;
#5809=CARTESIAN_POINT ( 'NONE',  ( 10.99999999999992006, -4.556349186104122317, 108.3437500040967763 ) ) ;
#5827=CARTESIAN_POINT ( 'NONE',  ( 4.220049686691934809, 10.18810118749999916, 82.18750000204836681 ) ) ;
#5833=CARTESIAN_POINT ( 'NONE',  ( -7.204075437095965206, -7.204075437095968759, 116.2187500020483810 ) ) ;
#5835=VECTOR ( 'NONE', #54523, 1000.000000000000000 ) ;
#5836=CARTESIAN_POINT ( 'NONE',  ( -4.556349186104045934, 11.00000000000000000, 108.9062500040967763 ) ) ;
#5841=CARTESIAN_POINT ( 'NONE',  ( -7.204075437095965206, -7.204075437095968759, 74.21875000204838102 ) ) ;
#5845=CARTESIAN_POINT ( 'NONE',  ( -10.99999999999999822, -4.556349186104053040, 94.28125000409676204 ) ) ;
#5854=CARTESIAN_POINT ( 'NONE',  ( 7.204075437095968759, -7.204075437095966983, 72.71875000204838102 ) ) ;
#5862=EDGE_CURVE ( 'NONE', #10364, #2929, #63946, .T. ) ;
#5885=CARTESIAN_POINT ( 'NONE',  ( 4.556349186104045934, 11.00000000000000000, 80.03124999999998579 ) ) ;
#5889=CARTESIAN_POINT ( 'NONE',  ( 11.00000000000000000, 1.347111479062088405E-15, 118.0000000000000000 ) ) ;
#5916=CARTESIAN_POINT ( 'NONE',  ( 1.871523826299183495E-15, -10.18810118749999916, 102.5312500020483810 ) ) ;
#5919=CARTESIAN_POINT ( 'NONE',  ( 7.778174593052023411, -7.778174593052021635, 69.06249999999998579 ) ) ;
#5934=CARTESIAN_POINT ( 'NONE',  ( -10.18810118749999916, 0.000000000000000000, 98.03125000204838102 ) ) ;
#5948=CARTESIAN_POINT ( 'NONE',  ( -10.18810118749999738, -4.220049686691941915, 87.25000000204838102 ) ) ;
#5955=CARTESIAN_POINT ( 'NONE',  ( -4.220049686691937474, -10.18810118749999738, 75.81250000204838102 ) ) ;
#5974=CARTESIAN_POINT ( 'NONE',  ( 7.778174593052021635, 7.778174593052023411, 85.93749999999998579 ) ) ;
#5981=DIRECTION ( 'NONE',  ( -0.000000000000000000, -0.000000000000000000, -1.000000000000000000 ) ) ;
#6001=CARTESIAN_POINT ( 'NONE',  ( 4.556349186104052151, -10.99999999999999822, 74.96874999999998579 ) ) ;
#6002=CARTESIAN_POINT ( 'NONE',  ( -11.00000000000000000, 0.000000000000000000, 67.18750000409676204 ) ) ;
#6004=CARTESIAN_POINT ( 'NONE',  ( -4.556349186104047710, -10.99999999999999822, 76.46875000409677625 ) ) ;
#6014=CARTESIAN_POINT ( 'NONE',  ( 4.220049686691934809, 10.18810118749999916, 111.0625000020483810 ) ) ;
#6018=CARTESIAN_POINT ( 'NONE',  ( -10.18810118749999916, 4.220049686691934809, 72.06250000204836681 ) ) ;
#6026=EDGE_LOOP ( 'NONE', ( #49623, #8922, #53427, #66587 ) ) ;
#6032=ORIENTED_EDGE ( 'NONE', *, *, #1611, .F. ) ;
#6055=CARTESIAN_POINT ( 'NONE',  ( 4.220049686691941027, -10.18810118749999738, 89.12500000204836681 ) ) ;
#6058=CARTESIAN_POINT ( 'NONE',  ( -10.99999999999999822, -4.556349186104052151, 101.5937499999999858 ) ) ;
#6064=CARTESIAN_POINT ( 'NONE',  ( -4.556349186104048599, -10.99999999999999822, 86.96875000409677625 ) ) ;
#6091=CARTESIAN_POINT ( 'NONE',  ( -7.778174593052020747, -7.778174593052023411, 94.37500000409677625 ) ) ;
#6093=CARTESIAN_POINT ( 'NONE',  ( 11.00000000000000000, 1.347111479062088405E-15, 111.4375000040967763 ) ) ;
#6094=CARTESIAN_POINT ( 'NONE',  ( -7.778174593052023411, 7.778174593052023411, 101.3124999999999858 ) ) ;
#6115=CARTESIAN_POINT ( 'NONE',  ( -4.220049686691935698, 10.18810118749999916, 94.75000000204838102 ) ) ;
#6118=( BOUNDED_CURVE ( )  B_SPLINE_CURVE ( 2, ( #65005, #47653, #46923, #41997, #13314, #37089, #59731, #7678, #12589 ),
 .UNSPECIFIED., .F., .F. ) 
 B_SPLINE_CURVE_WITH_KNOTS ( ( 3, 2, 2, 2, 3 ),
 ( 0.1323529411764706731, 0.1360294117647059542, 0.1397058823529412630, 0.1433823529411765441, 0.1470588235294118529 ),
 .UNSPECIFIED. ) 
 CURVE ( )  GEOMETRIC_REPRESENTATION_ITEM ( )  RATIONAL_B_SPLINE_CURVE ( ( 0.9999999999999982236, 0.9238795325112885148, 1.000000000000000000, 0.9238795325112867385, 1.000000000000000000, 0.9238795325112867385, 1.000000000000000000, 0.9238795325112849621, 1.000000000000001776 ) ) 
 REPRESENTATION_ITEM ( '' )  );
#6123=CARTESIAN_POINT ( 'NONE',  ( 1.871523826299183495E-15, -10.18810118749999916, 107.0312500020483810 ) ) ;
#6125=ORIENTED_EDGE ( 'NONE', *, *, #20691, .F. ) ;
#6126=VERTEX_POINT ( 'NONE', #63588 ) ;
#6131=CARTESIAN_POINT ( 'NONE',  ( 4.220049686691934809, 10.18810118749999916, 106.5625000020483668 ) ) ;
#6145=ORIENTED_EDGE ( 'NONE', *, *, #31714, .T. ) ;
#6146=CARTESIAN_POINT ( 'NONE',  ( 4.220049686691934809, 10.18810118749999916, 112.1875000020483810 ) ) ;
#6165=CARTESIAN_POINT ( 'NONE',  ( 7.204075437095966983, 7.204075437095967871, 68.96875000204836681 ) ) ;
#6172=DIRECTION ( 'NONE',  ( -1.000000000000000000, 0.000000000000000000, 0.000000000000000000 ) ) ;
#6178=CARTESIAN_POINT ( 'NONE',  ( 4.556349186104051263, -10.99999999999999822, 108.1562500040967620 ) ) ;
#6192=CARTESIAN_POINT ( 'NONE',  ( -11.00000000000000000, 0.000000000000000000, 116.4999999999999858 ) ) ;
#6198=CARTESIAN_POINT ( 'NONE',  ( -10.18810118749999738, -4.220049686691941915, 84.25000000204838102 ) ) ;
#6204=CARTESIAN_POINT ( 'NONE',  ( 7.204075437095968759, -7.204075437095966983, 115.0937500020483810 ) ) ;
#6212=CARTESIAN_POINT ( 'NONE',  ( 7.204075437095966983, 7.204075437095967871, 76.46875000204836681 ) ) ;
#6221=EDGE_CURVE ( 'NONE', #9770, #36810, #37495, .T. ) ;
#6227=CARTESIAN_POINT ( 'NONE',  ( 4.220049686691941027, -10.18810118749999738, 71.12500000204836681 ) ) ;
#6230=( BOUNDED_CURVE ( )  B_SPLINE_CURVE ( 2, ( #18467, #17719, #35825, #37682, #2222, #32016, #42576, #26332, #37302 ),
 .UNSPECIFIED., .F., .F. ) 
 B_SPLINE_CURVE_WITH_KNOTS ( ( 3, 2, 2, 2, 3 ),
 ( 0.7499999999999998890, 0.7536764705882351700, 0.7573529411764705621, 0.7610294117647058432, 0.7647058823529411242 ),
 .UNSPECIFIED. ) 
 CURVE ( )  GEOMETRIC_REPRESENTATION_ITEM ( )  RATIONAL_B_SPLINE_CURVE ( ( 1.000000000000002220, 0.9238795325112844070, 1.000000000000000000, 0.9238795325112867385, 1.000000000000000000, 0.9238795325112867385, 1.000000000000000000, 0.9238795325112867385, 1.000000000000000000 ) ) 
 REPRESENTATION_ITEM ( '' )  );
#6259=CARTESIAN_POINT ( 'NONE',  ( -4.556349186104045934, 11.00000000000000000, 116.4062500040967905 ) ) ;
#6269=CARTESIAN_POINT ( 'NONE',  ( 7.778174593052021635, 7.778174593052023411, 84.62500000409677625 ) ) ;
#6292=CARTESIAN_POINT ( 'NONE',  ( 4.220049686691941027, -10.18810118749999738, 99.62500000204838102 ) ) ;
#6295=CARTESIAN_POINT ( 'NONE',  ( -7.778174593052020747, -7.778174593052023411, 68.68749999999998579 ) ) ;
#6301=EDGE_LOOP ( 'NONE', ( #34744, #61674, #53412, #67936 ) ) ;
#6306=DIRECTION ( 'NONE',  ( -0.000000000000000000, -0.000000000000000000, -1.000000000000000000 ) ) ;
#6310=CARTESIAN_POINT ( 'NONE',  ( -7.204075437095967871, 7.204075437095967871, 93.34375000204838102 ) ) ;
#6317=CARTESIAN_POINT ( 'NONE',  ( -10.18810118749999916, 4.220049686691934809, 81.43750000204836681 ) ) ;
#6318=CARTESIAN_POINT ( 'NONE',  ( 11.00000000000000000, 1.347111479062088405E-15, 73.74999999999998579 ) ) ;
#6324=CARTESIAN_POINT ( 'NONE',  ( -4.220049686691937474, -10.18810118749999738, 90.43750000204836681 ) ) ;
#6325=AXIS2_PLACEMENT_3D ( 'NONE', #24070, #22969, #35782 ) ;
#6329=ORIENTED_EDGE ( 'NONE', *, *, #11517, .T. ) ;
#6335=CARTESIAN_POINT ( 'NONE',  ( 10.18810118749999916, 1.247682550866122264E-15, 74.78125000204836681 ) ) ;
#6340=CARTESIAN_POINT ( 'NONE',  ( -11.00000000000000000, 0.000000000000000000, 92.68750000409677625 ) ) ;
#6355=CARTESIAN_POINT ( 'NONE',  ( 4.220049686691941027, -10.18810118749999738, 71.12500000204836681 ) ) ;
#6358=CARTESIAN_POINT ( 'NONE',  ( 11.00000000000000000, 4.556349186104045934, 84.34375000000000000 ) ) ;
#6383=CARTESIAN_POINT ( 'NONE',  ( -4.556349186104047710, -10.99999999999999822, 68.96875000409676204 ) ) ;
#6392=CARTESIAN_POINT ( 'NONE',  ( -11.00000000000000000, 0.000000000000000000, 108.9999999999999858 ) ) ;
#6394=CARTESIAN_POINT ( 'NONE',  ( 4.220049686691934809, 10.18810118749999916, 115.5625000020483810 ) ) ;
#6402=VECTOR ( 'NONE', #74127, 1000.000000000000000 ) ;
#6410=DIRECTION ( 'NONE',  ( 0.000000000000000000, 0.000000000000000000, 1.000000000000000000 ) ) ;
#6433=CARTESIAN_POINT ( 'NONE',  ( 7.204075437095966983, 7.204075437095967871, 85.09375000204836681 ) ) ;
#6434=CARTESIAN_POINT ( 'NONE',  ( 4.556349186104045934, 11.00000000000000000, 92.03124999999998579 ) ) ;
#6436=CARTESIAN_POINT ( 'NONE',  ( 11.00000000000000355, -4.556349186104045046, 100.6562500000000000 ) ) ;
#6449=FACE_OUTER_BOUND ( 'NONE', #46552, .T. ) ;
#6466=CARTESIAN_POINT ( 'NONE',  ( -6.735557395310442023E-16, 11.00000000000000000, 84.81250000409676204 ) ) ;
#6488=CARTESIAN_POINT ( 'NONE',  ( -7.204075437095967871, 7.204075437095967871, 93.34375000204838102 ) ) ;
#6491=CARTESIAN_POINT ( 'NONE',  ( -11.00000000000000000, 0.000000000000000000, 100.1875000040967763 ) ) ;
#6494=CARTESIAN_POINT ( 'NONE',  ( -10.18810118749999916, 0.000000000000000000, 108.1562500020483668 ) ) ;
#6502=CARTESIAN_POINT ( 'NONE',  ( 7.778174593052021635, 7.778174593052023411, 96.43749999999998579 ) ) ;
#6503=CARTESIAN_POINT ( 'NONE',  ( 4.220049686691934809, 10.18810118749999916, 102.0625000020483810 ) ) ;
#6507=ORIENTED_EDGE ( 'NONE', *, *, #30210, .T. ) ;
#6517=CARTESIAN_POINT ( 'NONE',  ( -10.18810118749999916, 4.220049686691934809, 103.5625000020483810 ) ) ;
#6535=CARTESIAN_POINT ( 'NONE',  ( -7.204075437095965206, -7.204075437095968759, 69.71875000204836681 ) ) ;
#6547=CARTESIAN_POINT ( 'NONE',  ( 4.556349186104051263, -10.99999999999999822, 102.1562500040967763 ) ) ;
#6549=CARTESIAN_POINT ( 'NONE',  ( 7.778174593052021635, 7.778174593052023411, 95.12500000409676204 ) ) ;
#6560=ORIENTED_EDGE ( 'NONE', *, *, #63748, .T. ) ;
#6567=CARTESIAN_POINT ( 'NONE',  ( 10.18810118749999916, 1.247682550866122264E-15, 81.90625000204838102 ) ) ;
#6571=CARTESIAN_POINT ( 'NONE',  ( 4.220049686691934809, 10.18810118749999916, 115.5625000020483810 ) ) ;
#6573=CARTESIAN_POINT ( 'NONE',  ( 10.49999999999998224, 1.285879139104718661E-15, 118.0000000000000000 ) ) ;
#6579=CARTESIAN_POINT ( 'NONE',  ( -7.204075437095967871, 7.204075437095967871, 78.34375000204838102 ) ) ;
#6581=VERTEX_POINT ( 'NONE', #15984 ) ;
#6585=EDGE_CURVE ( 'NONE', #46843, #72690, #3786, .T. ) ;
#6591=CARTESIAN_POINT ( 'NONE',  ( -7.204075437095967871, 7.204075437095967871, 70.46875000204836681 ) ) ;
#6598=ADVANCED_FACE ( 'NONE', ( #3947 ), #49955, .T. ) ;
#6615=AXIS2_PLACEMENT_3D ( 'NONE', #55167, #61562, #50233 ) ;
#6628=CARTESIAN_POINT ( 'NONE',  ( 7.778174593052021635, 7.778174593052023411, 79.93750000000000000 ) ) ;
#6637=DIRECTION ( 'NONE',  ( -1.000000000000000000, 0.000000000000000000, 0.000000000000000000 ) ) ;
#6641=EDGE_CURVE ( 'NONE', #54851, #72225, #49579, .T. ) ;
#6658=CARTESIAN_POINT ( 'NONE',  ( 7.204075437095968759, -7.204075437095966983, 99.71875000204838102 ) ) ;
#6674=CARTESIAN_POINT ( 'NONE',  ( 4.220049686691934809, 10.18810118749999916, 97.56250000204836681 ) ) ;
#6679=CARTESIAN_POINT ( 'NONE',  ( 0.000000000000000000, 0.000000000000000000, 118.0000000000000000 ) ) ;
#6681=CARTESIAN_POINT ( 'NONE',  ( 10.18810118750000093, -4.220049686691933921, 80.68750000204836681 ) ) ;
#6689=CARTESIAN_POINT ( 'NONE',  ( -7.204075437095967871, 7.204075437095967871, 91.46875000204838102 ) ) ;
#6698=CARTESIAN_POINT ( 'NONE',  ( 4.220049686691934809, 10.18810118749999916, 76.56250000204836681 ) ) ;
#6714=CARTESIAN_POINT ( 'NONE',  ( -7.204075437095967871, 7.204075437095967871, 68.96875000204836681 ) ) ;
#6717=CARTESIAN_POINT ( 'NONE',  ( -7.778174593052020747, -7.778174593052023411, 83.68750000000000000 ) ) ;
#6745=CARTESIAN_POINT ( 'NONE',  ( 7.778174593052023411, -7.778174593052021635, 69.25000000409677625 ) ) ;
#6754=CARTESIAN_POINT ( 'NONE',  ( 11.00000000000000000, 1.347111479062088405E-15, 108.2499999999999858 ) ) ;
#6756=CARTESIAN_POINT ( 'NONE',  ( 1.871523826299183495E-15, -10.18810118749999916, 113.4062500020483810 ) ) ;
#6774=ADVANCED_FACE ( 'NONE', ( #57866 ), #205, .T. ) ;
#6794=CARTESIAN_POINT ( 'NONE',  ( -4.220049686691935698, 10.18810118749999916, 88.37500000204838102 ) ) ;
#6796=CARTESIAN_POINT ( 'NONE',  ( 11.00000000000000000, 1.347111479062088405E-15, 103.7500000000000000 ) ) ;
#6824=CARTESIAN_POINT ( 'NONE',  ( 2.020667218593132706E-15, -11.00000000000000000, 84.06250000409676204 ) ) ;
#6847=CARTESIAN_POINT ( 'NONE',  ( 7.204075437095968759, -7.204075437095966983, 92.59375000204838102 ) ) ;
#6852=CARTESIAN_POINT ( 'NONE',  ( 2.020667218593132706E-15, -11.00000000000000000, 100.5625000040967763 ) ) ;
#6855=CARTESIAN_POINT ( 'NONE',  ( 7.204075437095968759, -7.204075437095966983, 108.7187500020483810 ) ) ;
#6864=CARTESIAN_POINT ( 'NONE',  ( -4.220049686691935698, 10.18810118749999916, 105.2500000020483952 ) ) ;
#6880=ORIENTED_EDGE ( 'NONE', *, *, #66984, .T. ) ;
#6882=CARTESIAN_POINT ( 'NONE',  ( 1.871523826299183495E-15, -10.18810118749999916, 104.0312500020483810 ) ) ;
#6883=CARTESIAN_POINT ( 'NONE',  ( 4.556349186104052151, -10.99999999999999822, 103.4687500000000000 ) ) ;
#6892=CARTESIAN_POINT ( 'NONE',  ( -11.00000000000000000, 0.000000000000000000, 108.9999999999999858 ) ) ;
#6899=CARTESIAN_POINT ( 'NONE',  ( -10.99999999999999822, -4.556349186104052151, 116.5937500000000000 ) ) ;
#6907=ORIENTED_EDGE ( 'NONE', *, *, #43607, .F. ) ;
#6910=CARTESIAN_POINT ( 'NONE',  ( 11.00000000000000000, 1.347111479062088405E-15, 102.4375000040967763 ) ) ;
#6916=CARTESIAN_POINT ( 'NONE',  ( 11.00000000000000000, 1.347111479062088405E-15, 87.25000000000000000 ) ) ;
#6932=CARTESIAN_POINT ( 'NONE',  ( 10.18810118749999916, 4.220049686691935698, 83.50000000204840944 ) ) ;
#6936=CARTESIAN_POINT ( 'NONE',  ( -4.220049686691935698, 10.18810118749999916, 111.2500000020483952 ) ) ;
#6943=CARTESIAN_POINT ( 'NONE',  ( 10.18810118749999916, 4.220049686691935698, 74.87500000204836681 ) ) ;
#6951=EDGE_CURVE ( 'NONE', #72883, #1423, #28428, .T. ) ;
#6956=CARTESIAN_POINT ( 'NONE',  ( -7.204075437095965206, -7.204075437095968759, 69.34375000204836681 ) ) ;
#6958=DIRECTION ( 'NONE',  ( -3.154042683594195121E-16, 1.000000000000000000, 0.000000000000000000 ) ) ;
#6980=ORIENTED_EDGE ( 'NONE', *, *, #59303, .T. ) ;
#6996=CARTESIAN_POINT ( 'NONE',  ( 11.00000000000000000, 1.347111479062088405E-15, 75.43750000409676204 ) ) ;
#7012=CARTESIAN_POINT ( 'NONE',  ( 4.556349186104052151, -10.99999999999999822, 85.46874999999998579 ) ) ;
#7022=CARTESIAN_POINT ( 'NONE',  ( -5.771752292166722142, 9.182361355190234775, 117.6647434345326104 ) ) ;
#7025=CARTESIAN_POINT ( 'NONE',  ( -7.204075437095965206, -7.204075437095968759, 99.34375000204836681 ) ) ;
#7026=FACE_OUTER_BOUND ( 'NONE', #12794, .T. ) ;
#7028=CARTESIAN_POINT ( 'NONE',  ( 10.99999999999989697, -4.556349186104149851, 69.15624999999998579 ) ) ;
#7042=CARTESIAN_POINT ( 'NONE',  ( 7.204075437095968759, -7.204075437095966983, 97.09375000204836681 ) ) ;
#7046=CARTESIAN_POINT ( 'NONE',  ( -11.00000000000000000, 0.000000000000000000, 80.49999999999998579 ) ) ;
#7048=CARTESIAN_POINT ( 'NONE',  ( -7.204075437095967871, 7.204075437095967871, 79.84375000204838102 ) ) ;
#7052=ADVANCED_FACE ( 'NONE', ( #25347 ), #60056, .F. ) ;
#7055=CARTESIAN_POINT ( 'NONE',  ( 4.220049686691934809, 10.18810118749999916, 88.18750000204838102 ) ) ;
#7061=AXIS2_PLACEMENT_3D ( 'NONE', #47021, #64751, #70416 ) ;
#7066=CARTESIAN_POINT ( 'NONE',  ( 4.220049686691934809, 10.18810118749999916, 72.06250000204836681 ) ) ;
#7085=CARTESIAN_POINT ( 'NONE',  ( -7.778174593052020747, -7.778174593052023411, 76.18749999999998579 ) ) ;
#7088=DIRECTION ( 'NONE',  ( -1.000000000000000000, 0.000000000000000000, 0.000000000000000000 ) ) ;
#7114=CARTESIAN_POINT ( 'NONE',  ( 2.020667218593132706E-15, -11.00000000000000000, 70.56250000409677625 ) ) ;
#7125=CARTESIAN_POINT ( 'NONE',  ( 7.204075437095968759, -7.204075437095966983, 112.0937500020483810 ) ) ;
#7159=AXIS2_PLACEMENT_3D ( 'NONE', #3608, #36319, #13279 ) ;
#7165=CARTESIAN_POINT ( 'NONE',  ( 4.220049686691934809, 10.18810118749999916, 83.68750000204836681 ) ) ;
#7168=CARTESIAN_POINT ( 'NONE',  ( 4.556349186104051263, -10.99999999999999822, 103.4687500000000000 ) ) ;
#7169=CARTESIAN_POINT ( 'NONE',  ( -10.99999999999989164, -4.556349186104158733, 86.59375000000002842 ) ) ;
#7193=CARTESIAN_POINT ( 'NONE',  ( -11.00000000000000000, 0.000000000000000000, 118.0000000000000000 ) ) ;
#7198=CARTESIAN_POINT ( 'NONE',  ( -11.00000000000000000, 4.556349186104045934, 85.09375000409676204 ) ) ;
#7224=CARTESIAN_POINT ( 'NONE',  ( 7.204075437095966983, 7.204075437095967871, 94.46875000204838102 ) ) ;
#7230=CARTESIAN_POINT ( 'NONE',  ( 7.204075437095966983, 7.204075437095967871, 103.0937500020483668 ) ) ;
#7238=CARTESIAN_POINT ( 'NONE',  ( 10.18810118750000093, -4.220049686691933921, 97.18750000204836681 ) ) ;
#7250=VERTEX_POINT ( 'NONE', #60431 ) ;
#7252=CARTESIAN_POINT ( 'NONE',  ( -10.18810118749999738, -4.220049686691941915, 105.2500000020483810 ) ) ;
#7271=CARTESIAN_POINT ( 'NONE',  ( 4.220049686691934809, 10.18810118749999916, 69.06250000204839523 ) ) ;
#7283=CARTESIAN_POINT ( 'NONE',  ( 11.00000000000000000, 4.556349186104045934, 107.0312500040967763 ) ) ;
#7287=CARTESIAN_POINT ( 'NONE',  ( -7.778174593052023411, 7.778174593052023411, 71.50000000409677625 ) ) ;
#7288=DIRECTION ( 'NONE',  ( -1.000000000000000000, 0.000000000000000000, 0.000000000000000000 ) ) ;
#7297=EDGE_LOOP ( 'NONE', ( #68432, #62746 ) ) ;
#7306=CARTESIAN_POINT ( 'NONE',  ( -7.204075437095965206, -7.204075437095968759, 107.2187500020483810 ) ) ;
#7314=CARTESIAN_POINT ( 'NONE',  ( -10.18810118749999916, 4.220049686691934809, 69.43750000204838102 ) ) ;
#7329=CARTESIAN_POINT ( 'NONE',  ( 4.220049686691934809, 10.18810118749999916, 71.68750000204836681 ) ) ;
#7330=PLANE ( 'NONE',  #66709 ) ;
#7336=EDGE_CURVE ( 'NONE', #29969, #28981, #26851, .T. ) ;
#7352=EDGE_CURVE ( 'NONE', #34878, #20382, #42308, .T. ) ;
#7373=VECTOR ( 'NONE', #63151, 1000.000000000000000 ) ;
#7394=CARTESIAN_POINT ( 'NONE',  ( -10.18810118749999916, 0.000000000000000000, 99.15625000204838102 ) ) ;
#7397=DIRECTION ( 'NONE',  ( -0.000000000000000000, -0.000000000000000000, -1.000000000000000000 ) ) ;
#7409=CARTESIAN_POINT ( 'NONE',  ( -4.220049686691935698, 10.18810118749999916, 96.25000000204838102 ) ) ;
#7414=CARTESIAN_POINT ( 'NONE',  ( -4.556349186104045934, 11.00000000000000000, 102.7187500000000000 ) ) ;
#7415=CARTESIAN_POINT ( 'NONE',  ( -7.204075437095965206, -7.204075437095968759, 74.21875000204838102 ) ) ;
#7418=LINE ( 'NONE', #65501, #68010 ) ;
#7422=( BOUNDED_CURVE ( )  B_SPLINE_CURVE ( 2, ( #59308, #7616, #53645, #64591, #58942, #12889, #47589 ),
 .UNSPECIFIED., .F., .F. ) 
 B_SPLINE_CURVE_WITH_KNOTS ( ( 3, 2, 2, 3 ),
 ( 0.9705882352941178626, 0.9742647058823530326, 0.9779411764705883137, 0.9803851213646477269 ),
 .UNSPECIFIED. ) 
 CURVE ( )  GEOMETRIC_REPRESENTATION_ITEM ( )  RATIONAL_B_SPLINE_CURVE ( ( 0.9999999999999954481, 0.9238795325112912904, 1.000000000000000000, 0.9238795325112867385, 1.000000000000000000, 0.9493986900241293547, 0.9660721264009082265 ) ) 
 REPRESENTATION_ITEM ( '' )  );
#7423=CARTESIAN_POINT ( 'NONE',  ( 4.220049686691941027, -10.18810118749999738, 92.12500000204836681 ) ) ;
#7424=EDGE_CURVE ( 'NONE', #54851, #72690, #43073, .T. ) ;
#7436=CARTESIAN_POINT ( 'NONE',  ( -7.204075437095965206, -7.204075437095968759, 74.21875000204838102 ) ) ;
#7453=CARTESIAN_POINT ( 'NONE',  ( -4.220049686691937474, -10.18810118749999738, 69.43750000204838102 ) ) ;
#7456=CARTESIAN_POINT ( 'NONE',  ( -11.00000000000000000, 0.000000000000000000, 77.49999999999998579 ) ) ;
#7464=EDGE_CURVE ( 'NONE', #2613, #70285, #55170, .T. ) ;
#7483=CARTESIAN_POINT ( 'NONE',  ( -10.18810118749999738, -4.220049686691941915, 86.12500000204836681 ) ) ;
#7484=CARTESIAN_POINT ( 'NONE',  ( 11.00000000000000000, 1.347111479062088405E-15, 70.93750000409676204 ) ) ;
#7495=CARTESIAN_POINT ( 'NONE',  ( -4.220049686691935698, 10.18810118749999916, 111.2500000020483952 ) ) ;
#7535=CARTESIAN_POINT ( 'NONE',  ( 10.18810118749999916, 1.247682550866122264E-15, 86.40625000204838102 ) ) ;
#7537=CARTESIAN_POINT ( 'NONE',  ( 11.00000000000000000, 4.556349186104045934, 97.84375000000000000 ) ) ;
#7552=DIRECTION ( 'NONE',  ( -0.000000000000000000, -0.000000000000000000, -1.000000000000000000 ) ) ;
#7563=CARTESIAN_POINT ( 'NONE',  ( -4.556349186104045934, 11.00000000000000000, 104.4062500040967620 ) ) ;
#7567=CARTESIAN_POINT ( 'NONE',  ( 11.00000000000000000, 1.347111479062088405E-15, 85.93750000409677625 ) ) ;
#7570=CARTESIAN_POINT ( 'NONE',  ( 4.556349186104045934, 11.00000000000000000, 101.0312499999999858 ) ) ;
#7587=CARTESIAN_POINT ( 'NONE',  ( 4.556349186104045934, 11.00000000000000000, 90.71875000409676204 ) ) ;
#7589=CARTESIAN_POINT ( 'NONE',  ( 10.18810118750000093, -4.220049686691933921, 92.68750000204838102 ) ) ;
#7594=CARTESIAN_POINT ( 'NONE',  ( -4.220049686691935698, 10.18810118749999916, 100.3750000020484094 ) ) ;
#7602=CARTESIAN_POINT ( 'NONE',  ( -10.18810118749999738, -4.220049686691941915, 99.62500000204838102 ) ) ;
#7608=ORIENTED_EDGE ( 'NONE', *, *, #1503, .T. ) ;
#7616=CARTESIAN_POINT ( 'NONE',  ( -10.99999999999978861, 4.556349186104256432, 68.40624999999997158 ) ) ;
#7620=CARTESIAN_POINT ( 'NONE',  ( 1.871523826299183495E-15, -10.18810118749999916, 102.5312500020483810 ) ) ;
#7632=CARTESIAN_POINT ( 'NONE',  ( -10.99999999999989342, 4.556349186104152515, 74.40625000000000000 ) ) ;
#7640=CARTESIAN_POINT ( 'NONE',  ( -11.00000000000000000, 4.556349186104045934, 114.9062499999999716 ) ) ;
#7653=CARTESIAN_POINT ( 'NONE',  ( 7.778174593052021635, 7.778174593052023411, 102.6250000040967763 ) ) ;
#7656=CARTESIAN_POINT ( 'NONE',  ( -11.00000000000000000, 0.000000000000000000, 95.68750000409677625 ) ) ;
#7658=CARTESIAN_POINT ( 'NONE',  ( -11.00000000000000000, 0.000000000000000000, 110.6875000040967763 ) ) ;
#7675=CARTESIAN_POINT ( 'NONE',  ( 7.204075437095968759, -7.204075437095966983, 112.0937500020483810 ) ) ;
#7678=CARTESIAN_POINT ( 'NONE',  ( -11.00000000000007816, -4.556349186103974880, 109.2812500040967620 ) ) ;
#7682=CARTESIAN_POINT ( 'NONE',  ( 4.220049686691934809, 10.18810118749999916, 70.56250000204836681 ) ) ;
#7696=CARTESIAN_POINT ( 'NONE',  ( 10.18810118749999916, 1.247682550866122264E-15, 116.7812500020483810 ) ) ;
#7698=CARTESIAN_POINT ( 'NONE',  ( 0.000000000000000000, 0.000000000000000000, 118.0000000000000000 ) ) ;
#7710=ADVANCED_FACE ( 'NONE', ( #20632 ), #49302, .T. ) ;
#7717=VECTOR ( 'NONE', #8891, 1000.000000000000000 ) ;
#7725=CARTESIAN_POINT ( 'NONE',  ( -11.00000000000000000, 0.000000000000000000, 83.68750000409677625 ) ) ;
#7731=CARTESIAN_POINT ( 'NONE',  ( 11.00000000000000000, 1.347111479062088405E-15, 69.43750000409676204 ) ) ;
#7733=CARTESIAN_POINT ( 'NONE',  ( 0.000000000000000000, 0.000000000000000000, 38.34805510287551300 ) ) ;
#7757=CARTESIAN_POINT ( 'NONE',  ( -4.556349186104048599, -10.99999999999999822, 115.2812500000000000 ) ) ;
#7762=CARTESIAN_POINT ( 'NONE',  ( -10.18810118749999916, 4.220049686691934809, 94.56250000204838102 ) ) ;
#7763=CARTESIAN_POINT ( 'NONE',  ( -11.00000000000021139, 4.556349186103834548, 86.59375000409681888 ) ) ;
#7772=CARTESIAN_POINT ( 'NONE',  ( 4.556349186104052151, -10.99999999999999822, 73.46874999999998579 ) ) ;
#7777=CARTESIAN_POINT ( 'NONE',  ( -10.18810118749999738, -4.220049686691941915, 92.12500000204836681 ) ) ;
#7783=CARTESIAN_POINT ( 'NONE',  ( 10.18810118750000093, -4.220049686691933921, 76.18750000204839523 ) ) ;
#7791=CARTESIAN_POINT ( 'NONE',  ( 10.18810118750000093, -4.220049686691933921, 84.81250000204838102 ) ) ;
#7821=CARTESIAN_POINT ( 'NONE',  ( -4.556349186104047710, -10.99999999999999822, 76.28125000000000000 ) ) ;
#7830=CARTESIAN_POINT ( 'NONE',  ( 11.00000000000000355, -4.556349186104045046, 115.8437500040967620 ) ) ;
#7846=CARTESIAN_POINT ( 'NONE',  ( -10.18810118749999738, -4.220049686691941915, 89.12500000204836681 ) ) ;
#7847=CARTESIAN_POINT ( 'NONE',  ( 10.18810118749999916, 4.220049686691935698, 113.5000000020483810 ) ) ;
#7863=CARTESIAN_POINT ( 'NONE',  ( 10.18810118749999916, 4.220049686691935698, 107.8750000020483810 ) ) ;
#7892=CARTESIAN_POINT ( 'NONE',  ( 4.556349186104052151, -10.99999999999999822, 98.96875000000000000 ) ) ;
#7899=CARTESIAN_POINT ( 'NONE',  ( 1.871523826299183495E-15, -10.18810118749999916, 78.53125000204836681 ) ) ;
#7901=CARTESIAN_POINT ( 'NONE',  ( -11.00000000000000000, 0.000000000000000000, 93.99999999999998579 ) ) ;
#7915=CARTESIAN_POINT ( 'NONE',  ( 10.99999999999999467, 11.00000000000000355, 41.99999999999999289 ) ) ;
#7931=CARTESIAN_POINT ( 'NONE',  ( 7.778174593052023411, -7.778174593052021635, 87.25000000409677625 ) ) ;
#7943=ORIENTED_EDGE ( 'NONE', *, *, #2112, .F. ) ;
#7955=ADVANCED_FACE ( 'NONE', ( #811 ), #64163, .F. ) ;
#7957=CARTESIAN_POINT ( 'NONE',  ( -10.18810118749999738, -4.220049686691941915, 89.12500000204836681 ) ) ;
#7964=CARTESIAN_POINT ( 'NONE',  ( -4.220049686691937474, -10.18810118749999738, 103.9375000020483810 ) ) ;
#7967=ORIENTED_EDGE ( 'NONE', *, *, #831, .T. ) ;
#7973=CARTESIAN_POINT ( 'NONE',  ( 1.871523826299183495E-15, -10.18810118749999916, 98.40625000204838102 ) ) ;
#7986=CARTESIAN_POINT ( 'NONE',  ( -10.18810118749999916, 4.220049686691934809, 102.0625000020483810 ) ) ;
#8002=CARTESIAN_POINT ( 'NONE',  ( -10.99999999999999822, -4.556349186104052151, 113.5937499999999858 ) ) ;
#8009=LINE ( 'NONE', #25346, #947 ) ;
#8015=CARTESIAN_POINT ( 'NONE',  ( 4.556349186104051263, -10.99999999999999822, 105.1562500040967763 ) ) ;
#8028=VERTEX_POINT ( 'NONE', #32347 ) ;
#8031=CYLINDRICAL_SURFACE ( 'NONE', #41135, 11.00000000000000000 ) ;
#8037=CARTESIAN_POINT ( 'NONE',  ( 10.18810118749999916, 1.247682550866122264E-15, 109.2812500020483668 ) ) ;
#8045=CARTESIAN_POINT ( 'NONE',  ( 4.220049686691934809, 10.18810118749999916, 72.06250000204836681 ) ) ;
#8060=CARTESIAN_POINT ( 'NONE',  ( 10.18810118750000093, -4.220049686691933921, 116.6875000020483952 ) ) ;
#8108=CARTESIAN_POINT ( 'NONE',  ( -10.99999999999999822, -4.556349186104053040, 79.09375000000000000 ) ) ;
#8116=CARTESIAN_POINT ( 'NONE',  ( 4.556349186104045934, 11.00000000000000000, 101.2187500040967905 ) ) ;
#8121=CARTESIAN_POINT ( 'NONE',  ( -11.00000000000000000, 0.000000000000000000, 114.9999999999999858 ) ) ;
#8125=CYLINDRICAL_SURFACE ( 'NONE', #66872, 11.00000000000000000 ) ;
#8126=CARTESIAN_POINT ( 'NONE',  ( 10.18810118749999916, 4.220049686691935698, 92.50000000204838102 ) ) ;
#8142=CARTESIAN_POINT ( 'NONE',  ( -6.238412754330611322E-16, 10.18810118749999916, 90.15625000204838102 ) ) ;
#8147=CARTESIAN_POINT ( 'NONE',  ( -7.204075437095967871, 7.204075437095967871, 73.84375000204838102 ) ) ;
#8154=CARTESIAN_POINT ( 'NONE',  ( -10.18810118749999738, -4.220049686691941915, 82.75000000204838102 ) ) ;
#8165=CARTESIAN_POINT ( 'NONE',  ( 1.871523826299183495E-15, -10.18810118749999916, 68.40625000204836681 ) ) ;
#8186=CARTESIAN_POINT ( 'NONE',  ( 7.778174593052021635, 7.778174593052023411, 76.93749999999998579 ) ) ;
#8205=ORIENTED_EDGE ( 'NONE', *, *, #49985, .T. ) ;
#8213=CARTESIAN_POINT ( 'NONE',  ( 4.220049686691934809, 10.18810118749999916, 87.06250000204838102 ) ) ;
#8214=CARTESIAN_POINT ( 'NONE',  ( -10.18810118749999738, -4.220049686691941915, 114.2500000020483952 ) ) ;
#8225=DIRECTION ( 'NONE',  ( -0.000000000000000000, -0.000000000000000000, -1.000000000000000000 ) ) ;
#8228=CARTESIAN_POINT ( 'NONE',  ( 10.18810118750000093, -4.220049686691933033, 104.6875000020483810 ) ) ;
#8261=CARTESIAN_POINT ( 'NONE',  ( 4.220049686691934809, 10.18810118749999916, 79.18750000204836681 ) ) ;
#8264=CARTESIAN_POINT ( 'NONE',  ( -10.99999999999999822, -4.556349186104052151, 97.09375000000001421 ) ) ;
#8270=CARTESIAN_POINT ( 'NONE',  ( -7.778174593052023411, 7.778174593052023411, 106.0000000040967763 ) ) ;
#8274=VECTOR ( 'NONE', #30838, 1000.000000000000000 ) ;
#8279=CARTESIAN_POINT ( 'NONE',  ( 0.000000000000000000, 0.000000000000000000, 38.34805510287551300 ) ) ;
#8295=CARTESIAN_POINT ( 'NONE',  ( 11.00000000000000000, 4.556349186104045934, 81.53125000409677625 ) ) ;
#8297=DIRECTION ( 'NONE',  ( -0.000000000000000000, -0.000000000000000000, -1.000000000000000000 ) ) ;
#8312=CARTESIAN_POINT ( 'NONE',  ( 10.18810118750000093, -4.220049686691933921, 83.31250000204836681 ) ) ;
#8320=CARTESIAN_POINT ( 'NONE',  ( -10.18810118749999738, -4.220049686691941915, 83.12500000204835260 ) ) ;
#8326=CARTESIAN_POINT ( 'NONE',  ( -10.18810118749999916, 4.220049686691934809, 100.5625000020483668 ) ) ;
#8333=CARTESIAN_POINT ( 'NONE',  ( 7.204075437095968759, -7.204075437095966983, 98.59375000204836681 ) ) ;
#8336=CYLINDRICAL_SURFACE ( 'NONE', #25929, 11.00000000000000000 ) ;
#8349=CARTESIAN_POINT ( 'NONE',  ( 10.18810118749999916, 1.247682550866122264E-15, 101.4062500020483810 ) ) ;
#8350=CARTESIAN_POINT ( 'NONE',  ( -10.99999999999998579, 4.556349186104061921, 115.0937500040967620 ) ) ;
#8369=CARTESIAN_POINT ( 'NONE',  ( 11.00000000000000000, 1.347111479062088405E-15, 115.7499999999999858 ) ) ;
#8382=CARTESIAN_POINT ( 'NONE',  ( -11.00000000000000000, 4.556349186104045934, 101.5937500040967620 ) ) ;
#8384=EDGE_CURVE ( 'NONE', #67283, #46864, #55796, .T. ) ;
#8401=DIRECTION ( 'NONE',  ( -0.000000000000000000, -0.000000000000000000, -1.000000000000000000 ) ) ;
#8406=CARTESIAN_POINT ( 'NONE',  ( 11.00000000000000000, 1.347111479062088405E-15, 70.93750000409676204 ) ) ;
#8407=CARTESIAN_POINT ( 'NONE',  ( -4.220049686691937474, -10.18810118749999738, 105.8125000020483952 ) ) ;
#8408=VERTEX_POINT ( 'NONE', #2087 ) ;
#8414=CARTESIAN_POINT ( 'NONE',  ( 10.18810118749999916, 4.220049686691935698, 70.37500000204838102 ) ) ;
#8426=CARTESIAN_POINT ( 'NONE',  ( -4.220049686691935698, 10.18810118749999916, 117.2500000020484094 ) ) ;
#8428=DIRECTION ( 'NONE',  ( -0.000000000000000000, -0.000000000000000000, -1.000000000000000000 ) ) ;
#8441=CARTESIAN_POINT ( 'NONE',  ( -7.204075437095967871, 7.204075437095967871, 116.9687500020483810 ) ) ;
#8454=CARTESIAN_POINT ( 'NONE',  ( -11.00000000000021139, 4.556349186103834548, 88.09375000409677625 ) ) ;
#8482=DIRECTION ( 'NONE',  ( -0.000000000000000000, -0.000000000000000000, -1.000000000000000000 ) ) ;
#8492=CARTESIAN_POINT ( 'NONE',  ( 5.055468900453003123, 9.773537533938954525, 117.5066621467264838 ) ) ;
#8494=CARTESIAN_POINT ( 'NONE',  ( -4.220049686691935698, 10.18810118749999916, 92.87500000204838102 ) ) ;
#8509=CARTESIAN_POINT ( 'NONE',  ( 4.220049686691934809, 10.18810118749999916, 87.06250000204838102 ) ) ;
#8514=CARTESIAN_POINT ( 'NONE',  ( 4.556349186104052151, -10.99999999999999822, 102.1562500040967763 ) ) ;
#8515=CARTESIAN_POINT ( 'NONE',  ( -7.204075437095967871, 7.204075437095967871, 72.34375000204836681 ) ) ;
#8519=FACE_OUTER_BOUND ( 'NONE', #6026, .T. ) ;
#8524=CARTESIAN_POINT ( 'NONE',  ( -10.18810118749999916, 4.220049686691934809, 82.56250000204836681 ) ) ;
#8559=CARTESIAN_POINT ( 'NONE',  ( -7.778174593052023411, 7.778174593052023411, 74.31249999999998579 ) ) ;
#8569=CARTESIAN_POINT ( 'NONE',  ( 11.00000000000000000, 1.347111479062088405E-15, 114.4375000040967763 ) ) ;
#8576=CARTESIAN_POINT ( 'NONE',  ( 0.000000000000000000, 0.000000000000000000, 118.0000000000000000 ) ) ;
#8586=CARTESIAN_POINT ( 'NONE',  ( -4.220049686691937474, -10.18810118749999738, 86.31250000204838102 ) ) ;
#8587=CARTESIAN_POINT ( 'NONE',  ( 10.18810118749999916, 4.220049686691935698, 112.0000000020483668 ) ) ;
#8590=DIRECTION ( 'NONE',  ( -0.000000000000000000, -0.000000000000000000, -1.000000000000000000 ) ) ;
#8600=CARTESIAN_POINT ( 'NONE',  ( 4.220049686691934809, 10.18810118749999916, 105.0625000020483810 ) ) ;
#8618=VERTEX_POINT ( 'NONE', #64266 ) ;
#8629=ORIENTED_EDGE ( 'NONE', *, *, #74582, .T. ) ;
#8641=CARTESIAN_POINT ( 'NONE',  ( -7.204075437095967871, 7.204075437095967871, 80.96875000204836681 ) ) ;
#8644=CARTESIAN_POINT ( 'NONE',  ( 11.00000000000000000, 4.556349186104045934, 96.34374999999998579 ) ) ;
#8669=CARTESIAN_POINT ( 'NONE',  ( -11.00000000000000000, 0.000000000000000000, 104.6875000040967763 ) ) ;
#8670=CARTESIAN_POINT ( 'NONE',  ( -6.735557395310442023E-16, 11.00000000000000000, 69.81250000409677625 ) ) ;
#8672=CARTESIAN_POINT ( 'NONE',  ( 11.00000000000000355, -4.556349186104045046, 79.84375000409677625 ) ) ;
#8689=CARTESIAN_POINT ( 'NONE',  ( -6.238412754330611322E-16, 10.18810118749999916, 74.78125000204836681 ) ) ;
#8698=CARTESIAN_POINT ( 'NONE',  ( -7.204075437095967871, 7.204075437095967871, 82.84375000204838102 ) ) ;
#8704=CARTESIAN_POINT ( 'NONE',  ( 4.220049686691941027, -10.18810118749999738, 101.1250000020483810 ) ) ;
#8706=VERTEX_POINT ( 'NONE', #29198 ) ;
#8712=CARTESIAN_POINT ( 'NONE',  ( 10.18810118749999916, 1.247682550866122264E-15, 95.78125000204836681 ) ) ;
#8721=CARTESIAN_POINT ( 'NONE',  ( 0.000000000000000000, 0.000000000000000000, 38.34805510287551300 ) ) ;
#8724=CARTESIAN_POINT ( 'NONE',  ( 11.00000000000005329, -4.556349186103991755, 96.34375000409677625 ) ) ;
#8727=LINE ( 'NONE', #15860, #47679 ) ;
#8731=CARTESIAN_POINT ( 'NONE',  ( -6.238412754330611322E-16, 10.18810118749999916, 98.78125000204838102 ) ) ;
#8744=CARTESIAN_POINT ( 'NONE',  ( 0.000000000000000000, 0.000000000000000000, 118.0000000000000000 ) ) ;
#8752=CARTESIAN_POINT ( 'NONE',  ( -4.556349186104045934, 11.00000000000000000, 111.7187499999999858 ) ) ;
#8765=CARTESIAN_POINT ( 'NONE',  ( 2.020667218593132706E-15, -11.00000000000000000, 99.06250000409677625 ) ) ;
#8787=CARTESIAN_POINT ( 'NONE',  ( 7.778174593052021635, 7.778174593052023411, 69.43749999999998579 ) ) ;
#8788=CARTESIAN_POINT ( 'NONE',  ( 4.220049686691934809, 10.18810118749999916, 105.0625000020483810 ) ) ;
#8795=CARTESIAN_POINT ( 'NONE',  ( 10.18810118749999916, 1.247682550866122264E-15, 70.28125000204838102 ) ) ;
#8798=CARTESIAN_POINT ( 'NONE',  ( 7.204075437095966983, 7.204075437095967871, 116.5937500020483810 ) ) ;
#8809=CARTESIAN_POINT ( 'NONE',  ( 10.18810118750000093, -4.220049686691933921, 113.6875000020483952 ) ) ;
#8846=DIRECTION ( 'NONE',  ( -1.000000000000000000, 0.000000000000000000, 0.000000000000000000 ) ) ;
#8872=CARTESIAN_POINT ( 'NONE',  ( -7.204075437095967871, 7.204075437095967871, 94.46875000204838102 ) ) ;
#8886=CARTESIAN_POINT ( 'NONE',  ( 1.871523826299183495E-15, -10.18810118749999916, 86.40625000204838102 ) ) ;
#8891=DIRECTION ( 'NONE',  ( -1.000000000000000000, -1.577021341797097560E-16, -0.000000000000000000 ) ) ;
#8899=EDGE_CURVE ( 'NONE', #26634, #58573, #42765, .T. ) ;
#8901=CARTESIAN_POINT ( 'NONE',  ( -7.204075437095965206, -7.204075437095968759, 85.84375000204836681 ) ) ;
#8912=VERTEX_POINT ( 'NONE', #2744 ) ;
#8922=ORIENTED_EDGE ( 'NONE', *, *, #60821, .T. ) ;
#8931=CARTESIAN_POINT ( 'NONE',  ( -7.778174593052023411, 7.778174593052023411, 114.8125000000000000 ) ) ;
#8935=CARTESIAN_POINT ( 'NONE',  ( -6.735557395310442023E-16, 11.00000000000000000, 74.12500000000000000 ) ) ;
#8944=CARTESIAN_POINT ( 'NONE',  ( -11.00000000000000000, 0.000000000000000000, 115.1875000040967763 ) ) ;
#8961=CARTESIAN_POINT ( 'NONE',  ( -10.18810118749999916, 4.220049686691934809, 87.43750000204838102 ) ) ;
#8962=CARTESIAN_POINT ( 'NONE',  ( 10.18810118749999916, 1.247682550866122264E-15, 114.9062500020483810 ) ) ;
#8966=CARTESIAN_POINT ( 'NONE',  ( -11.00000000000000000, 0.000000000000000000, 68.49999999999997158 ) ) ;
#8976=CARTESIAN_POINT ( 'NONE',  ( 10.18810118749999916, 1.247682550866122264E-15, 107.7812500020483810 ) ) ;
#8978=ORIENTED_EDGE ( 'NONE', *, *, #37103, .F. ) ;
#9006=CARTESIAN_POINT ( 'NONE',  ( -10.18810118749999916, 0.000000000000000000, 117.5312500020483810 ) ) ;
#9009=ORIENTED_EDGE ( 'NONE', *, *, #68991, .F. ) ;
#9015=CARTESIAN_POINT ( 'NONE',  ( -7.204075437095967871, 7.204075437095967871, 79.46875000204836681 ) ) ;
#9018=CARTESIAN_POINT ( 'NONE',  ( -11.00000000000000000, 0.000000000000000000, 95.49999999999998579 ) ) ;
#9045=CARTESIAN_POINT ( 'NONE',  ( -7.778174593052023411, 7.778174593052023411, 70.00000000409677625 ) ) ;
#9047=CARTESIAN_POINT ( 'NONE',  ( 2.020667218593132706E-15, -11.00000000000000000, 82.56250000409677625 ) ) ;
#9067=CARTESIAN_POINT ( 'NONE',  ( -4.220049686691937474, -10.18810118749999738, 78.43750000204838102 ) ) ;
#9075=CARTESIAN_POINT ( 'NONE',  ( -10.18810118749999738, -4.220049686691941915, 84.62500000204838102 ) ) ;
#9080=CARTESIAN_POINT ( 'NONE',  ( 10.18810118750000093, -4.220049686691933921, 96.81250000204839523 ) ) ;
#9089=CARTESIAN_POINT ( 'NONE',  ( 4.220049686691941027, -10.18810118749999738, 91.00000000204836681 ) ) ;
#9106=CARTESIAN_POINT ( 'NONE',  ( -7.204075437095965206, -7.204075437095968759, 97.84375000204836681 ) ) ;
#9116=ORIENTED_EDGE ( 'NONE', *, *, #65198, .F. ) ;
#9124=CARTESIAN_POINT ( 'NONE',  ( 7.778174593052021635, 7.778174593052023411, 114.4375000000000000 ) ) ;
#9131=CYLINDRICAL_SURFACE ( 'NONE', #19007, 11.00000000000000000 ) ;
#9132=DIRECTION ( 'NONE',  ( -1.084202172485504434E-16, 1.000000000000000000, 0.000000000000000000 ) ) ;
#9136=CARTESIAN_POINT ( 'NONE',  ( 11.00000000000000355, -4.556349186104045046, 100.8437500040967620 ) ) ;
#9137=CARTESIAN_POINT ( 'NONE',  ( -11.00000000000000000, 0.000000000000000000, 106.1875000040967620 ) ) ;
#9159=CARTESIAN_POINT ( 'NONE',  ( -4.556349186104045934, 11.00000000000000000, 69.71875000000000000 ) ) ;
#9160=CARTESIAN_POINT ( 'NONE',  ( 4.220049686691934809, 10.18810118749999916, 102.0625000020483810 ) ) ;
#9169=CARTESIAN_POINT ( 'NONE',  ( 4.220049686691934809, 10.18810118749999916, 110.6875000020483952 ) ) ;
#9171=VERTEX_POINT ( 'NONE', #45337 ) ;
#9178=CARTESIAN_POINT ( 'NONE',  ( -10.18810118749999916, 0.000000000000000000, 113.0312500020483810 ) ) ;
#9191=ADVANCED_FACE ( 'NONE', ( #34419 ), #46453, .T. ) ;
#9193=CARTESIAN_POINT ( 'NONE',  ( -7.204075437095967871, 7.204075437095967871, 115.4687500020483810 ) ) ;
#9213=CARTESIAN_POINT ( 'NONE',  ( 11.00000000000000000, 1.347111479062088405E-15, 111.2499999999999858 ) ) ;
#9224=CARTESIAN_POINT ( 'NONE',  ( -4.556349186104045934, 11.00000000000000000, 77.40625000409679046 ) ) ;
#9239=CARTESIAN_POINT ( 'NONE',  ( 11.00000000000000000, 1.347111479062088405E-15, 81.43750000409677625 ) ) ;
#9244=CARTESIAN_POINT ( 'NONE',  ( 10.18810118749999916, 4.220049686691935698, 97.00000000204836681 ) ) ;
#9251=CARTESIAN_POINT ( 'NONE',  ( 4.556349186104052151, -10.99999999999999822, 95.96875000000000000 ) ) ;
#9258=CARTESIAN_POINT ( 'NONE',  ( -6.238412754330611322E-16, 10.18810118749999916, 84.15625000204838102 ) ) ;
#9271=AXIS2_PLACEMENT_3D ( 'NONE', #12054, #1128, #760 ) ;
#9272=CARTESIAN_POINT ( 'NONE',  ( -4.220049686691935698, 10.18810118749999916, 82.37500000204838102 ) ) ;
#9296=CLOSED_SHELL ( 'NONE', ( #71303, #6774, #16683, #41926, #45494, #34171, #7710, #66035, #16539, #58955, #35570, #37087, #30103, #30681, #12538, #34829, #50483, #35251, #6598, #32496, #9477, #21874, #10098, #5477, #57979, #60302, #56834, #47504, #72071, #70426, #51217, #49872, #70751, #65614, #5571, #20040, #45508, #17358, #45435, #3009, #51727, #16849, #49534, #20201, #70829, #32863, #43613, #9191, #57078, #72105, #35964, #74362, #54975, #36076, #35042, #67532, #72652, #54655, #31784, #16597, #3613, #50951, #22860, #12537, #64229, #31626, #40759, #15282, #52363, #16582, #7955, #47719, #41715, #53618, #56974, #34054, #34827, #7052, #31162, #5311, #64065, #9820, #34202, #57164, #40356, #57448, #29160, #74514, #2965, #23639, #59827 ) ) ;
#9303=CARTESIAN_POINT ( 'NONE',  ( -4.556349186104045934, 11.00000000000000000, 114.7187500000000000 ) ) ;
#9307=CARTESIAN_POINT ( 'NONE',  ( 11.00000000000000000, 4.556349186104045934, 69.34374999999998579 ) ) ;
#9315=CARTESIAN_POINT ( 'NONE',  ( 4.556349186104052151, -10.99999999999999822, 114.1562500040967763 ) ) ;
#9322=CARTESIAN_POINT ( 'NONE',  ( -11.00000000000020783, -4.556349186103842541, 70.09375000000000000 ) ) ;
#9337=CARTESIAN_POINT ( 'NONE',  ( 1.871523826299183495E-15, -10.18810118749999916, 113.0312500020483810 ) ) ;
#9351=CARTESIAN_POINT ( 'NONE',  ( 10.18810118750000093, -4.220049686691933033, 106.1875000020483810 ) ) ;
#9377=EDGE_CURVE ( 'NONE', #21890, #56060, #36958, .T. ) ;
#9385=VERTEX_POINT ( 'NONE', #7915 ) ;
#9388=ORIENTED_EDGE ( 'NONE', *, *, #25724, .T. ) ;
#9390=CARTESIAN_POINT ( 'NONE',  ( 7.204075437095968759, -7.204075437095966983, 80.21875000204836681 ) ) ;
#9393=CARTESIAN_POINT ( 'NONE',  ( -6.735557395310442023E-16, 11.00000000000000000, 92.12499999999998579 ) ) ;
#9420=CARTESIAN_POINT ( 'NONE',  ( 4.556349186104052151, -10.99999999999999822, 71.96874999999998579 ) ) ;
#9426=CARTESIAN_POINT ( 'NONE',  ( 4.556349186104051263, -10.99999999999999822, 78.15625000409677625 ) ) ;
#9444=DIRECTION ( 'NONE',  ( -1.000000000000000000, 0.000000000000000000, 0.000000000000000000 ) ) ;
#9445=CARTESIAN_POINT ( 'NONE',  ( 10.18810118749999916, 4.220049686691935698, 76.00000000204838102 ) ) ;
#9447=CARTESIAN_POINT ( 'NONE',  ( 0.000000000000000000, 0.000000000000000000, 118.0000000000000000 ) ) ;
#9454=CARTESIAN_POINT ( 'NONE',  ( -4.220049686691937474, -10.18810118749999738, 86.31250000204838102 ) ) ;
#9460=CARTESIAN_POINT ( 'NONE',  ( -10.18810118749999738, -4.220049686691941915, 97.75000000204838102 ) ) ;
#9467=CARTESIAN_POINT ( 'NONE',  ( 10.18810118749999916, 4.220049686691935698, 92.87500000204838102 ) ) ;
#9477=ADVANCED_FACE ( 'NONE', ( #36591 ), #64885, .T. ) ;
#9488=CARTESIAN_POINT ( 'NONE',  ( 4.220049686691934809, 10.18810118749999916, 98.68750000204838102 ) ) ;
#9491=CARTESIAN_POINT ( 'NONE',  ( 4.556349186104045934, 11.00000000000000000, 105.5312500000000142 ) ) ;
#9519=ORIENTED_EDGE ( 'NONE', *, *, #70375, .F. ) ;
#9522=CARTESIAN_POINT ( 'NONE',  ( 4.556349186104051263, -10.99999999999999822, 97.65625000409680467 ) ) ;
#9546=CARTESIAN_POINT ( 'NONE',  ( 4.220049686691934809, 10.18810118749999916, 103.5625000020483668 ) ) ;
#9555=CARTESIAN_POINT ( 'NONE',  ( 10.18810118749999916, 1.247682550866122264E-15, 113.4062500020483810 ) ) ;
#9563=CARTESIAN_POINT ( 'NONE',  ( -10.18810118749999916, 0.000000000000000000, 107.0312500020483810 ) ) ;
#9571=CARTESIAN_POINT ( 'NONE',  ( 4.220049686691934809, 10.18810118749999916, 70.56250000204836681 ) ) ;
#9597=CARTESIAN_POINT ( 'NONE',  ( 11.00000000000000000, 1.347111479062088405E-15, 76.93750000409677625 ) ) ;
#9602=CARTESIAN_POINT ( 'NONE',  ( 5.499987861550171608, 9.526286449755788865, 67.99927393035380874 ) ) ;
#9604=DIRECTION ( 'NONE',  ( 2.168404344971008868E-16, -1.000000000000000000, 0.000000000000000000 ) ) ;
#9628=CARTESIAN_POINT ( 'NONE',  ( -4.220049686691935698, 10.18810118749999916, 91.37500000204838102 ) ) ;
#9641=CARTESIAN_POINT ( 'NONE',  ( 1.871523826299183495E-15, -10.18810118749999916, 84.90625000204838102 ) ) ;
#9656=CARTESIAN_POINT ( 'NONE',  ( 7.204075437095968759, -7.204075437095966983, 78.71875000204836681 ) ) ;
#9670=CARTESIAN_POINT ( 'NONE',  ( 11.00000000000000355, -4.556349186104044158, 73.84375000409676204 ) ) ;
#9678=AXIS2_PLACEMENT_3D ( 'NONE', #36583, #71264, #12815 ) ;
#9683=CARTESIAN_POINT ( 'NONE',  ( -1.925929944387235853E-31, 16.00000000000000000, 3.497325839728428143 ) ) ;
#9690=CARTESIAN_POINT ( 'NONE',  ( 11.00000000000000000, 1.347111479062088405E-15, 73.74999999999998579 ) ) ;
#9696=CARTESIAN_POINT ( 'NONE',  ( -4.556349186104048599, -10.99999999999999822, 113.9687500040968047 ) ) ;
#9700=CARTESIAN_POINT ( 'NONE',  ( -11.00000000000000000, 0.000000000000000000, 69.99999999999998579 ) ) ;
#9715=CARTESIAN_POINT ( 'NONE',  ( 10.18810118749999916, 1.247682550866122264E-15, 108.9062500020483668 ) ) ;
#9729=CARTESIAN_POINT ( 'NONE',  ( -10.18810118749999916, 4.220049686691934809, 100.9375000020483810 ) ) ;
#9752=CARTESIAN_POINT ( 'NONE',  ( -7.204075437095967871, 7.204075437095967871, 81.34375000204838102 ) ) ;
#9770=VERTEX_POINT ( 'NONE', #19787 ) ;
#9771=CARTESIAN_POINT ( 'NONE',  ( 4.220049686691934809, 10.18810118749999916, 71.68750000204838102 ) ) ;
#9774=CARTESIAN_POINT ( 'NONE',  ( -6.735557395310442023E-16, 11.00000000000000000, 90.62499999999998579 ) ) ;
#9795=CARTESIAN_POINT ( 'NONE',  ( -6.735557395310442023E-16, 11.00000000000000000, 111.8125000040967763 ) ) ;
#9799=CARTESIAN_POINT ( 'NONE',  ( -11.00000000000000000, 0.000000000000000000, 77.68750000409677625 ) ) ;
#9815=CARTESIAN_POINT ( 'NONE',  ( -7.204075437095967871, 7.204075437095967871, 79.46875000204836681 ) ) ;
#9818=AXIS2_PLACEMENT_3D ( 'NONE', #38184, #9132, #4230 ) ;
#9820=ADVANCED_FACE ( 'NONE', ( #31110 ), #42426, .T. ) ;
#9824=CARTESIAN_POINT ( 'NONE',  ( 7.204075437095968759, -7.204075437095966983, 85.09375000204836681 ) ) ;
#9825=ORIENTED_EDGE ( 'NONE', *, *, #47443, .T. ) ;
#9829=CARTESIAN_POINT ( 'NONE',  ( 4.220049686691941027, -10.18810118749999738, 96.62500000204838102 ) ) ;
#9838=CARTESIAN_POINT ( 'NONE',  ( 1.871523826299183495E-15, -10.18810118749999916, 93.90625000204836681 ) ) ;
#9856=CARTESIAN_POINT ( 'NONE',  ( 10.18810118749999916, 4.220049686691935698, 98.50000000204838102 ) ) ;
#9859=CARTESIAN_POINT ( 'NONE',  ( -11.00000000000000000, 4.556349186104045934, 107.4062500000000000 ) ) ;
#9883=CARTESIAN_POINT ( 'NONE',  ( 11.00000000000000000, 1.347111479062088405E-15, 70.93750000409676204 ) ) ;
#9884=CARTESIAN_POINT ( 'NONE',  ( 11.00000000000000000, 1.347111479062088405E-15, 118.0000000000000000 ) ) ;
#9885=ORIENTED_EDGE ( 'NONE', *, *, #3523, .F. ) ;
#9889=CARTESIAN_POINT ( 'NONE',  ( -7.778174593052020747, -7.778174593052023411, 98.87500000409676204 ) ) ;
#9905=CARTESIAN_POINT ( 'NONE',  ( 11.00000000000000000, 1.347111479062088405E-15, 84.43750000409677625 ) ) ;
#9907=CARTESIAN_POINT ( 'NONE',  ( -10.18810118749999916, 0.000000000000000000, 101.0312500020483810 ) ) ;
#9908=ORIENTED_EDGE ( 'NONE', *, *, #52687, .T. ) ;
#9913=CARTESIAN_POINT ( 'NONE',  ( 5.094044972490348933, 8.823157690132404696, 67.53052377765949643 ) ) ;
#9915=ORIENTED_EDGE ( 'NONE', *, *, #41924, .F. ) ;
#9916=CARTESIAN_POINT ( 'NONE',  ( -10.18810118749999916, 0.000000000000000000, 115.6562500020483810 ) ) ;
#9925=CARTESIAN_POINT ( 'NONE',  ( -7.204075437095967871, 7.204075437095967871, 111.3437500020483810 ) ) ;
#9933=VECTOR ( 'NONE', #8590, 1000.000000000000000 ) ;
#9935=CARTESIAN_POINT ( 'NONE',  ( -7.204075437095965206, -7.204075437095968759, 68.21875000204836681 ) ) ;
#9946=CARTESIAN_POINT ( 'NONE',  ( 7.778174593052021635, 7.778174593052023411, 96.62500000409676204 ) ) ;
#9964=CARTESIAN_POINT ( 'NONE',  ( -11.00000000000000000, 0.000000000000000000, 110.4999999999999858 ) ) ;
#9996=CARTESIAN_POINT ( 'NONE',  ( -15.99999999999999645, 15.99999999999999645, 20.00000000000000000 ) ) ;
#9997=CARTESIAN_POINT ( 'NONE',  ( -6.238412754330611322E-16, 10.18810118749999916, 91.28125000204836681 ) ) ;
#10010=CARTESIAN_POINT ( 'NONE',  ( 7.204075437095966983, 7.204075437095967871, 80.96875000204836681 ) ) ;
#10024=CARTESIAN_POINT ( 'NONE',  ( -7.204075437095965206, -7.204075437095968759, 78.34375000204838102 ) ) ;
#10051=ORIENTED_EDGE ( 'NONE', *, *, #66274, .F. ) ;
#10056=CARTESIAN_POINT ( 'NONE',  ( -7.778174593052020747, -7.778174593052023411, 68.68749999999998579 ) ) ;
#10081=ORIENTED_EDGE ( 'NONE', *, *, #29708, .T. ) ;
#10083=CARTESIAN_POINT ( 'NONE',  ( -7.204075437095965206, -7.204075437095968759, 105.3437500020483810 ) ) ;
#10097=CARTESIAN_POINT ( 'NONE',  ( -7.204075437095965206, -7.204075437095968759, 102.7187500020483668 ) ) ;
#10098=ADVANCED_FACE ( 'NONE', ( #34869 ), #23145, .T. ) ;
#10117=CARTESIAN_POINT ( 'NONE',  ( 7.204075437095966983, 7.204075437095967871, 82.46875000204836681 ) ) ;
#10129=ORIENTED_EDGE ( 'NONE', *, *, #50105, .T. ) ;
#10134=CARTESIAN_POINT ( 'NONE',  ( -10.18810118749999916, 4.220049686691934809, 73.56250000204836681 ) ) ;
#10137=CARTESIAN_POINT ( 'NONE',  ( 2.020667218593132706E-15, -11.00000000000000000, 91.37499999999998579 ) ) ;
#10148=ORIENTED_EDGE ( 'NONE', *, *, #44836, .T. ) ;
#10168=CARTESIAN_POINT ( 'NONE',  ( 11.00000000000000000, 1.347111479062088405E-15, 75.43750000409676204 ) ) ;
#10188=CARTESIAN_POINT ( 'NONE',  ( 10.18810118749999916, 1.247682550866122264E-15, 72.90625000204836681 ) ) ;
#10197=CARTESIAN_POINT ( 'NONE',  ( -10.18810118749999916, 0.000000000000000000, 78.53125000204836681 ) ) ;
#10209=CARTESIAN_POINT ( 'NONE',  ( 4.220049686691941027, -10.18810118749999738, 92.50000000204838102 ) ) ;
#10225=CARTESIAN_POINT ( 'NONE',  ( 1.871523826299183495E-15, -10.18810118749999916, 90.53125000204836681 ) ) ;
#10228=CARTESIAN_POINT ( 'NONE',  ( 11.00000000000000355, -4.556349186104045046, 108.1562500000000000 ) ) ;
#10232=EDGE_CURVE ( 'NONE', #11931, #13626, #54470, .T. ) ;
#10260=CARTESIAN_POINT ( 'NONE',  ( 7.778174593052021635, 7.778174593052023411, 93.62500000409677625 ) ) ;
#10282=CARTESIAN_POINT ( 'NONE',  ( -10.18810118749999916, 4.220049686691934809, 94.93750000204838102 ) ) ;
#10292=CARTESIAN_POINT ( 'NONE',  ( 10.18810118749999916, 4.220049686691935698, 112.0000000020483668 ) ) ;
#10301=CARTESIAN_POINT ( 'NONE',  ( -10.18810118749999738, -4.220049686691941915, 108.6250000020483668 ) ) ;
#10313=CARTESIAN_POINT ( 'NONE',  ( 10.99999999999989342, 4.556349186104152515, 90.34375000000000000 ) ) ;
#10315=CARTESIAN_POINT ( 'NONE',  ( -7.204075437095965206, -7.204075437095968759, 112.8437500020483810 ) ) ;
#10316=CARTESIAN_POINT ( 'NONE',  ( -4.556349186104045934, 11.00000000000000000, 96.90625000409677625 ) ) ;
#10330=CARTESIAN_POINT ( 'NONE',  ( -4.556349186104048599, -10.99999999999999822, 91.28125000000000000 ) ) ;
#10361=CARTESIAN_POINT ( 'NONE',  ( -7.778174593052023411, 7.778174593052023411, 104.3124999999999858 ) ) ;
#10364=VERTEX_POINT ( 'NONE', #7658 ) ;
#10365=CARTESIAN_POINT ( 'NONE',  ( -7.204075437095965206, -7.204075437095968759, 87.34375000204836681 ) ) ;
#10379=CARTESIAN_POINT ( 'NONE',  ( 10.18810118749999916, 1.247682550866122264E-15, 82.28125000204838102 ) ) ;
#10391=ORIENTED_EDGE ( 'NONE', *, *, #44076, .T. ) ;
#10393=CARTESIAN_POINT ( 'NONE',  ( -4.220049686691937474, -10.18810118749999738, 78.43750000204838102 ) ) ;
#10427=CARTESIAN_POINT ( 'NONE',  ( -10.99999999999999822, -4.556349186104052151, 73.09375000000000000 ) ) ;
#10436=EDGE_CURVE ( 'NONE', #32560, #39397, #62614, .T. ) ;
#10445=ORIENTED_EDGE ( 'NONE', *, *, #395, .T. ) ;
#10452=CARTESIAN_POINT ( 'NONE',  ( -4.220049686691935698, 10.18810118749999916, 107.8750000020483668 ) ) ;
#10468=CARTESIAN_POINT ( 'NONE',  ( 7.204075437095966983, 7.204075437095967871, 101.9687500020483668 ) ) ;
#10488=CARTESIAN_POINT ( 'NONE',  ( -10.18810118749999738, -4.220049686691941915, 81.62500000204836681 ) ) ;
#10494=FACE_OUTER_BOUND ( 'NONE', #51606, .T. ) ;
#10509=CARTESIAN_POINT ( 'NONE',  ( -6.238412754330611322E-16, 10.18810118749999916, 74.78125000204836681 ) ) ;
#10512=CARTESIAN_POINT ( 'NONE',  ( -4.556349186104047710, -10.99999999999999822, 89.78125000000000000 ) ) ;
#10537=CARTESIAN_POINT ( 'NONE',  ( -6.735557395310442023E-16, 11.00000000000000000, 80.31250000409677625 ) ) ;
#10539=CARTESIAN_POINT ( 'NONE',  ( -11.00000000000000000, 4.556349186104045934, 77.59375000409676204 ) ) ;
#10546=CARTESIAN_POINT ( 'NONE',  ( 10.99999999999994849, 4.556349186104097448, 98.03125000409677625 ) ) ;
#10557=CARTESIAN_POINT ( 'NONE',  ( -10.18810118749999738, -4.220049686691941915, 69.25000000204836681 ) ) ;
#10566=CARTESIAN_POINT ( 'NONE',  ( 10.18810118749999916, 1.247682550866122264E-15, 82.28125000204838102 ) ) ;
#10597=CARTESIAN_POINT ( 'NONE',  ( -7.204075437095965206, -7.204075437095968759, 93.34375000204838102 ) ) ;
#10600=CARTESIAN_POINT ( 'NONE',  ( -7.778174593052020747, -7.778174593052023411, 104.6874999999999858 ) ) ;
#10626=CARTESIAN_POINT ( 'NONE',  ( 2.020667218593132706E-15, -11.00000000000000000, 88.37499999999998579 ) ) ;
#10627=ORIENTED_EDGE ( 'NONE', *, *, #2596, .T. ) ;
#10630=CARTESIAN_POINT ( 'NONE',  ( -6.735557395310442023E-16, 11.00000000000000000, 90.81250000409676204 ) ) ;
#10646=CARTESIAN_POINT ( 'NONE',  ( 0.000000000000000000, 0.000000000000000000, 41.99999999999999289 ) ) ;
#10650=CARTESIAN_POINT ( 'NONE',  ( -7.204075437095965206, -7.204075437095968759, 96.71875000204838102 ) ) ;
#10652=EDGE_CURVE ( 'NONE', #21157, #72571, #31764, .T. ) ;
#10658=CARTESIAN_POINT ( 'NONE',  ( 7.204075437095966983, 7.204075437095967871, 110.5937500020483810 ) ) ;
#10664=CARTESIAN_POINT ( 'NONE',  ( -10.99999999999989164, -4.556349186104158733, 76.28125000409679046 ) ) ;
#10668=CARTESIAN_POINT ( 'NONE',  ( -6.238412754330611322E-16, 10.18810118749999916, 109.6562500020483668 ) ) ;
#10672=VERTEX_POINT ( 'NONE', #19456 ) ;
#10683=ORIENTED_EDGE ( 'NONE', *, *, #65730, .T. ) ;
#10684=CARTESIAN_POINT ( 'NONE',  ( -4.220049686691937474, -10.18810118749999738, 109.9375000020483810 ) ) ;
#10691=EDGE_CURVE ( 'NONE', #9385, #10672, #16387, .T. ) ;
#10705=CARTESIAN_POINT ( 'NONE',  ( -10.59405059374999958, 0.000000000000000000, 117.7656250010241905 ) ) ;
#10710=CARTESIAN_POINT ( 'NONE',  ( 2.020667218593132706E-15, -11.00000000000000000, 109.5625000040967763 ) ) ;
#10727=CARTESIAN_POINT ( 'NONE',  ( -11.00000000000000000, 0.000000000000000000, 104.5000000000000000 ) ) ;
#10732=CARTESIAN_POINT ( 'NONE',  ( 10.18810118750000093, -4.220049686691933921, 86.31250000204838102 ) ) ;
#10737=CARTESIAN_POINT ( 'NONE',  ( -4.220049686691935698, 10.18810118749999916, 114.2500000020483952 ) ) ;
#10745=CARTESIAN_POINT ( 'NONE',  ( -10.18810118749999738, -4.220049686691941915, 81.62500000204836681 ) ) ;
#10757=CARTESIAN_POINT ( 'NONE',  ( -7.204075437095965206, -7.204075437095968759, 75.34375000204838102 ) ) ;
#10760=CARTESIAN_POINT ( 'NONE',  ( 11.00000000000007994, 4.556349186103967774, 109.8437500000000000 ) ) ;
#10820=VERTEX_POINT ( 'NONE', #24491 ) ;
#10823=CARTESIAN_POINT ( 'NONE',  ( 7.204075437095968759, -7.204075437095966983, 108.7187500020483810 ) ) ;
#10840=CARTESIAN_POINT ( 'NONE',  ( 10.18810118749999916, 4.220049686691935698, 98.87500000204838102 ) ) ;
#10861=CARTESIAN_POINT ( 'NONE',  ( -10.18810118749999738, -4.220049686691941915, 78.62500000204838102 ) ) ;
#10882=CARTESIAN_POINT ( 'NONE',  ( 10.18810118749999916, 4.220049686691935698, 73.00000000204836681 ) ) ;
#10885=CARTESIAN_POINT ( 'NONE',  ( -4.556349186104045934, 11.00000000000000000, 90.71874999999998579 ) ) ;
#10891=VECTOR ( 'NONE', #12264, 1000.000000000000000 ) ;
#10905=EDGE_CURVE ( 'NONE', #68143, #1009, #6230, .T. ) ;
#10909=CARTESIAN_POINT ( 'NONE',  ( -11.00000000000000000, 0.000000000000000000, 74.49999999999998579 ) ) ;
#10910=CARTESIAN_POINT ( 'NONE',  ( -7.778174593052023411, 7.778174593052023411, 80.50000000409676204 ) ) ;
#10912=CARTESIAN_POINT ( 'NONE',  ( 11.00000000000000000, 1.347111479062088405E-15, 72.43750000409676204 ) ) ;
#10919=CARTESIAN_POINT ( 'NONE',  ( -7.778174593052023411, 7.778174593052023411, 98.50000000409677625 ) ) ;
#10927=ORIENTED_EDGE ( 'NONE', *, *, #7464, .F. ) ;
#10929=CARTESIAN_POINT ( 'NONE',  ( -6.238412754330611322E-16, 10.18810118749999916, 68.78125000204838102 ) ) ;
#10941=CARTESIAN_POINT ( 'NONE',  ( -6.238412754330611322E-16, 10.18810118749999916, 82.65625000204838102 ) ) ;
#10970=CARTESIAN_POINT ( 'NONE',  ( 10.18810118749999916, 4.220049686691935698, 92.50000000204838102 ) ) ;
#10973=CARTESIAN_POINT ( 'NONE',  ( -4.556349186104047710, -10.99999999999999822, 107.7812500000000000 ) ) ;
#10976=DIRECTION ( 'NONE',  ( -1.084202172485504434E-16, 1.000000000000000000, 0.000000000000000000 ) ) ;
#10991=CARTESIAN_POINT ( 'NONE',  ( -7.778174593052023411, 7.778174593052023411, 86.31249999999998579 ) ) ;
#11004=CARTESIAN_POINT ( 'NONE',  ( -4.556349186104045934, 11.00000000000000000, 95.40625000409677625 ) ) ;
#11028=CARTESIAN_POINT ( 'NONE',  ( 10.18810118750000093, -4.220049686691933921, 100.1875000020483668 ) ) ;
#11029=VERTEX_POINT ( 'NONE', #21058 ) ;
#11036=CARTESIAN_POINT ( 'NONE',  ( 10.18810118749999916, 4.220049686691935698, 106.0000000020483668 ) ) ;
#11046=CARTESIAN_POINT ( 'NONE',  ( -7.204075437095965206, -7.204075437095968759, 108.7187500020483810 ) ) ;
#11059=ORIENTED_EDGE ( 'NONE', *, *, #5122, .F. ) ;
#11062=VERTEX_POINT ( 'NONE', #42940 ) ;
#11063=CARTESIAN_POINT ( 'NONE',  ( -7.204075437095967871, 7.204075437095967871, 110.9687500020483810 ) ) ;
#11073=CARTESIAN_POINT ( 'NONE',  ( 11.00000000000000000, 1.347111479062088405E-15, 109.7499999999999858 ) ) ;
#11090=CARTESIAN_POINT ( 'NONE',  ( -4.556349186104047710, -10.99999999999999822, 109.4687500040967763 ) ) ;
#11093=CARTESIAN_POINT ( 'NONE',  ( -11.00000000000000533, 11.00000000000000000, 20.00000000000000000 ) ) ;
#11106=EDGE_LOOP ( 'NONE', ( #19011, #29358, #24276, #49518 ) ) ;
#11115=CARTESIAN_POINT ( 'NONE',  ( -6.238412754330611322E-16, 10.18810118749999916, 86.78125000204836681 ) ) ;
#11119=CARTESIAN_POINT ( 'NONE',  ( -4.220049686691935698, 10.18810118749999916, 117.2500000020484094 ) ) ;
#11127=CARTESIAN_POINT ( 'NONE',  ( -4.220049686691937474, -10.18810118749999738, 77.31250000204836681 ) ) ;
#11141=CARTESIAN_POINT ( 'NONE',  ( -7.204075437095967871, 7.204075437095967871, 74.96875000204836681 ) ) ;
#11144=ORIENTED_EDGE ( 'NONE', *, *, #32337, .T. ) ;
#11191=ORIENTED_EDGE ( 'NONE', *, *, #11782, .T. ) ;
#11199=CARTESIAN_POINT ( 'NONE',  ( 10.18810118749999916, 4.220049686691935698, 109.0000000020483810 ) ) ;
#11215=CARTESIAN_POINT ( 'NONE',  ( -7.204075437095965206, -7.204075437095968759, 98.21875000204838102 ) ) ;
#11229=CARTESIAN_POINT ( 'NONE',  ( 10.18810118749999916, 1.247682550866122264E-15, 96.90625000204838102 ) ) ;
#11238=CARTESIAN_POINT ( 'NONE',  ( 7.204075437095968759, -7.204075437095966983, 83.59375000204838102 ) ) ;
#11256=CARTESIAN_POINT ( 'NONE',  ( 1.871523826299183495E-15, -10.18810118749999916, 74.03125000204836681 ) ) ;
#11259=CARTESIAN_POINT ( 'NONE',  ( 2.020667218593132706E-15, -11.00000000000000000, 83.87499999999998579 ) ) ;
#11284=CARTESIAN_POINT ( 'NONE',  ( 10.99999999999989342, 4.556349186104152515, 80.03125000409677625 ) ) ;
#11286=CARTESIAN_POINT ( 'NONE',  ( 7.778174593052023411, -7.778174593052021635, 72.25000000409677625 ) ) ;
#11303=CARTESIAN_POINT ( 'NONE',  ( -6.238412754330611322E-16, 10.18810118749999916, 73.28125000204838102 ) ) ;
#11313=EDGE_CURVE ( 'NONE', #55577, #41775, #28910, .T. ) ;
#11339=CARTESIAN_POINT ( 'NONE',  ( -10.18810118749999738, -4.220049686691941915, 90.25000000204838102 ) ) ;
#11341=CARTESIAN_POINT ( 'NONE',  ( 4.556349186104051263, -10.99999999999999822, 101.9687500000000000 ) ) ;
#11343=CARTESIAN_POINT ( 'NONE',  ( 11.00000000000010836, -4.556349186103939353, 87.15625000000000000 ) ) ;
#11344=DIRECTION ( 'NONE',  ( -1.000000000000000000, -9.955163135201253416E-17, 0.000000000000000000 ) ) ;
#11356=CARTESIAN_POINT ( 'NONE',  ( 11.00000000000000000, 1.347111479062088405E-15, 111.2499999999999858 ) ) ;
#11369=ORIENTED_EDGE ( 'NONE', *, *, #45345, .T. ) ;
#11372=CARTESIAN_POINT ( 'NONE',  ( -11.00000000000000000, 0.000000000000000000, 94.18750000409677625 ) ) ;
#11395=CARTESIAN_POINT ( 'NONE',  ( 4.220049686691934809, 10.18810118749999916, 96.06250000204836681 ) ) ;
#11397=( BOUNDED_CURVE ( )  B_SPLINE_CURVE ( 2, ( #40638, #28945, #74596, #47400, #53074, #64396, #63266, #35727, #58381 ),
 .UNSPECIFIED., .F., .F. ) 
 B_SPLINE_CURVE_WITH_KNOTS ( ( 3, 2, 2, 2, 3 ),
 ( 0.5294117647058820264, 0.5330882352941173075, 0.5367647058823526995, 0.5404411764705880916, 0.5441176470588233727 ),
 .UNSPECIFIED. ) 
 CURVE ( )  GEOMETRIC_REPRESENTATION_ITEM ( )  RATIONAL_B_SPLINE_CURVE ( ( 1.000000000000006883, 0.9238795325112798551, 1.000000000000000000, 0.9238795325112867385, 1.000000000000000000, 0.9238795325112867385, 1.000000000000000000, 0.9238795325112890700, 0.9999999999999976685 ) ) 
 REPRESENTATION_ITEM ( '' )  );
#11400=CARTESIAN_POINT ( 'NONE',  ( -10.99999999999989164, -4.556349186104158733, 100.2812500040967478 ) ) ;
#11404=CARTESIAN_POINT ( 'NONE',  ( 10.18810118750000093, -4.220049686691933921, 107.3125000020483668 ) ) ;
#11406=ORIENTED_EDGE ( 'NONE', *, *, #32746, .F. ) ;
#11412=CARTESIAN_POINT ( 'NONE',  ( -10.18810118749999916, 4.220049686691934809, 103.9375000020483810 ) ) ;
#11422=DIRECTION ( 'NONE',  ( 0.000000000000000000, 0.000000000000000000, 1.000000000000000000 ) ) ;
#11429=CARTESIAN_POINT ( 'NONE',  ( 1.871523826299183495E-15, -10.18810118749999916, 113.0312500020483810 ) ) ;
#11446=CARTESIAN_POINT ( 'NONE',  ( -6.238412754330611322E-16, 10.18810118749999916, 67.65625000204836681 ) ) ;
#11453=DIRECTION ( 'NONE',  ( -0.000000000000000000, -0.000000000000000000, -1.000000000000000000 ) ) ;
#11459=CARTESIAN_POINT ( 'NONE',  ( 11.00000000000000000, 1.347111479062088405E-15, 108.4375000040967763 ) ) ;
#11482=CARTESIAN_POINT ( 'NONE',  ( 10.18810118750000093, -4.220049686691933921, 81.81250000204838102 ) ) ;
#11494=CARTESIAN_POINT ( 'NONE',  ( 7.204075437095968759, -7.204075437095966983, 74.59375000204838102 ) ) ;
#11496=EDGE_LOOP ( 'NONE', ( #58530, #24482, #31743, #15773 ) ) ;
#11497=CARTESIAN_POINT ( 'NONE',  ( -4.556349186104048599, -10.99999999999999822, 94.46875000409677625 ) ) ;
#11506=CARTESIAN_POINT ( 'NONE',  ( -6.238412754330611322E-16, 10.18810118749999916, 68.78125000204838102 ) ) ;
#11517=EDGE_CURVE ( 'NONE', #15561, #27901, #40653, .T. ) ;
#11565=CARTESIAN_POINT ( 'NONE',  ( -4.220049686691935698, 10.18810118749999916, 101.8750000020483810 ) ) ;
#11575=EDGE_LOOP ( 'NONE', ( #11369, #40807, #22516, #28916 ) ) ;
#11581=CARTESIAN_POINT ( 'NONE',  ( 10.18810118749999916, 1.247682550866122264E-15, 92.78125000204836681 ) ) ;
#11594=CARTESIAN_POINT ( 'NONE',  ( -6.238412754330611322E-16, 10.18810118749999916, 97.28125000204838102 ) ) ;
#11604=CARTESIAN_POINT ( 'NONE',  ( -6.238412754330611322E-16, 10.18810118749999916, 72.15625000204836681 ) ) ;
#11616=CARTESIAN_POINT ( 'NONE',  ( -4.556349186104048599, -10.99999999999999822, 88.46875000409677625 ) ) ;
#11623=CARTESIAN_POINT ( 'NONE',  ( 10.18810118749999916, 1.247682550866122264E-15, 71.40625000204836681 ) ) ;
#11626=CARTESIAN_POINT ( 'NONE',  ( 11.00000000000000355, -4.556349186104045046, 85.65625000000001421 ) ) ;
#11629=DIRECTION ( 'NONE',  ( -0.000000000000000000, -0.000000000000000000, -1.000000000000000000 ) ) ;
#11632=CARTESIAN_POINT ( 'NONE',  ( 0.000000000000000000, 0.000000000000000000, 118.0000000000000000 ) ) ;
#11648=CARTESIAN_POINT ( 'NONE',  ( 0.000000000000000000, 0.000000000000000000, 118.0000000000000000 ) ) ;
#11651=DIRECTION ( 'NONE',  ( -0.000000000000000000, -0.000000000000000000, -1.000000000000000000 ) ) ;
#11652=CARTESIAN_POINT ( 'NONE',  ( 11.00000000000000000, 1.347111479062088405E-15, 117.2500000000000000 ) ) ;
#11654=CARTESIAN_POINT ( 'NONE',  ( 7.778174593052021635, 7.778174593052023411, 75.62500000409677625 ) ) ;
#11663=CARTESIAN_POINT ( 'NONE',  ( 7.778174593052021635, 7.778174593052023411, 108.4374999999999858 ) ) ;
#11665=CARTESIAN_POINT ( 'NONE',  ( -10.18810118749999916, 0.000000000000000000, 113.0312500020483810 ) ) ;
#11669=CARTESIAN_POINT ( 'NONE',  ( 7.204075437095968759, -7.204075437095966983, 72.71875000204838102 ) ) ;
#11700=DIRECTION ( 'NONE',  ( 0.000000000000000000, -1.000000000000000000, 0.000000000000000000 ) ) ;
#11705=CARTESIAN_POINT ( 'NONE',  ( -4.220049686691935698, 10.18810118749999916, 92.87500000204838102 ) ) ;
#11706=CARTESIAN_POINT ( 'NONE',  ( -11.00000000000000000, 0.000000000000000000, 92.49999999999998579 ) ) ;
#11708=CARTESIAN_POINT ( 'NONE',  ( -4.556349186104045934, 11.00000000000000000, 101.2187500000000000 ) ) ;
#11709=CONICAL_SURFACE ( 'NONE', #920, 10.49999999999998224, 0.7853981633974378429 ) ;
#11714=CARTESIAN_POINT ( 'NONE',  ( 2.020667218593132706E-15, -11.00000000000000000, 87.06250000409676204 ) ) ;
#11742=CARTESIAN_POINT ( 'NONE',  ( -4.556349186104045934, 11.00000000000000000, 92.40625000409676204 ) ) ;
#11765=CARTESIAN_POINT ( 'NONE',  ( -6.238412754330611322E-16, 10.18810118749999916, 99.15625000204838102 ) ) ;
#11768=CARTESIAN_POINT ( 'NONE',  ( -4.556349186104048599, -10.99999999999999822, 100.4687500040967763 ) ) ;
#11771=CARTESIAN_POINT ( 'NONE',  ( -4.220049686691935698, 10.18810118749999916, 106.3750000020483668 ) ) ;
#11781=CARTESIAN_POINT ( 'NONE',  ( -7.204075437095967871, 7.204075437095967871, 103.8437500020483810 ) ) ;
#11782=EDGE_CURVE ( 'NONE', #12782, #36860, #34218, .T. ) ;
#11795=ORIENTED_EDGE ( 'NONE', *, *, #26071, .F. ) ;
#11797=CARTESIAN_POINT ( 'NONE',  ( 4.220049686691941027, -10.18810118749999738, 110.1250000020483810 ) ) ;
#11811=CARTESIAN_POINT ( 'NONE',  ( 7.778174593052023411, -7.778174593052021635, 91.56249999999998579 ) ) ;
#11815=CARTESIAN_POINT ( 'NONE',  ( -6.238412754330611322E-16, 10.18810118749999916, 70.65625000204836681 ) ) ;
#11827=CARTESIAN_POINT ( 'NONE',  ( -6.735557395310442023E-16, 11.00000000000000000, 111.8125000040967763 ) ) ;
#11834=( BOUNDED_CURVE ( )  B_SPLINE_CURVE ( 2, ( #73443, #60634, #56478, #67417, #73813, #66663, #73074, #44404, #14969 ),
 .UNSPECIFIED., .F., .F. ) 
 B_SPLINE_CURVE_WITH_KNOTS ( ( 3, 2, 2, 2, 3 ),
 ( 0.7058823529411764053, 0.7095588235294116863, 0.7132352941176469674, 0.7169117647058823595, 0.7205882352941176405 ),
 .UNSPECIFIED. ) 
 CURVE ( )  GEOMETRIC_REPRESENTATION_ITEM ( )  RATIONAL_B_SPLINE_CURVE ( ( 1.000000000000002220, 0.9238795325112844070, 1.000000000000000000, 0.9238795325112867385, 1.000000000000000000, 0.9238795325112867385, 1.000000000000000000, 0.9238795325112867385, 1.000000000000000000 ) ) 
 REPRESENTATION_ITEM ( '' )  );
#11849=CARTESIAN_POINT ( 'NONE',  ( -6.238412754330611322E-16, 10.18810118749999916, 80.78125000204838102 ) ) ;
#11854=CARTESIAN_POINT ( 'NONE',  ( -6.238412754330611322E-16, 10.18810118749999916, 117.1562500020483810 ) ) ;
#11855=ORIENTED_EDGE ( 'NONE', *, *, #5591, .T. ) ;
#11862=CARTESIAN_POINT ( 'NONE',  ( 7.204075437095968759, -7.204075437095966983, 79.09375000204838102 ) ) ;
#11875=CARTESIAN_POINT ( 'NONE',  ( -7.204075437095965206, -7.204075437095968759, 72.34375000204836681 ) ) ;
#11881=ORIENTED_EDGE ( 'NONE', *, *, #41331, .T. ) ;
#11887=CARTESIAN_POINT ( 'NONE',  ( -11.00000000000000000, 0.000000000000000000, 74.68750000409676204 ) ) ;
#11911=DIRECTION ( 'NONE',  ( 1.000000000000000000, 0.000000000000000000, 0.000000000000000000 ) ) ;
#11928=FACE_OUTER_BOUND ( 'NONE', #3581, .T. ) ;
#11931=VERTEX_POINT ( 'NONE', #68858 ) ;
#11940=CARTESIAN_POINT ( 'NONE',  ( -4.220049686691937474, -10.18810118749999738, 102.4375000020483810 ) ) ;
#11958=CARTESIAN_POINT ( 'NONE',  ( -7.204075437095965206, -7.204075437095968759, 92.21875000204838102 ) ) ;
#11972=CARTESIAN_POINT ( 'NONE',  ( 4.220049686691934809, 10.18810118749999916, 89.68750000204836681 ) ) ;
#11981=CARTESIAN_POINT ( 'NONE',  ( -10.18810118749999916, 0.000000000000000000, 75.53125000204836681 ) ) ;
#11984=CARTESIAN_POINT ( 'NONE',  ( -11.00000000000000000, 0.000000000000000000, 111.9999999999999858 ) ) ;
#11997=CARTESIAN_POINT ( 'NONE',  ( -10.18810118749999738, -4.220049686691941915, 70.75000000204836681 ) ) ;
#12000=CARTESIAN_POINT ( 'NONE',  ( -11.00000000000000000, 0.000000000000000000, 81.99999999999998579 ) ) ;
#12020=DIRECTION ( 'NONE',  ( -1.000000000000000000, 0.000000000000000000, 0.000000000000000000 ) ) ;
#12026=CARTESIAN_POINT ( 'NONE',  ( -4.556349186104047710, -10.99999999999999822, 67.46875000409676204 ) ) ;
#12037=CARTESIAN_POINT ( 'NONE',  ( -10.18810118749999738, -4.220049686691941915, 114.6250000020483810 ) ) ;
#12041=CARTESIAN_POINT ( 'NONE',  ( -7.204075437095965206, -7.204075437095968759, 67.84375000204836681 ) ) ;
#12054=CARTESIAN_POINT ( 'NONE',  ( 0.000000000000000000, 0.000000000000000000, 118.0000000000000000 ) ) ;
#12066=FACE_OUTER_BOUND ( 'NONE', #62925, .T. ) ;
#12074=CARTESIAN_POINT ( 'NONE',  ( -10.18810118749999916, 4.220049686691934809, 84.06250000204838102 ) ) ;
#12075=CARTESIAN_POINT ( 'NONE',  ( -6.735557395310442023E-16, 11.00000000000000000, 92.12499999999998579 ) ) ;
#12077=CARTESIAN_POINT ( 'NONE',  ( -4.556349186104047710, -10.99999999999999822, 100.2812499999999858 ) ) ;
#12084=CARTESIAN_POINT ( 'NONE',  ( 7.778174593052021635, 7.778174593052023411, 78.43750000000000000 ) ) ;
#12107=CARTESIAN_POINT ( 'NONE',  ( -7.778174593052023411, 7.778174593052023411, 86.50000000409677625 ) ) ;
#12127=CARTESIAN_POINT ( 'NONE',  ( -11.00000000000000000, 0.000000000000000000, 91.18750000409677625 ) ) ;
#12130=CARTESIAN_POINT ( 'NONE',  ( -7.204075437095965206, -7.204075437095968759, 93.71875000204838102 ) ) ;
#12133=CARTESIAN_POINT ( 'NONE',  ( 0.000000000000000000, 0.000000000000000000, 118.0000000000000000 ) ) ;
#12134=LINE ( 'NONE', #46836, #15861 ) ;
#12138=CARTESIAN_POINT ( 'NONE',  ( 10.18810118749999916, 1.247682550866122264E-15, 110.4062500020483668 ) ) ;
#12147=CARTESIAN_POINT ( 'NONE',  ( 10.18810118749999916, 1.247682550866122264E-15, 104.7812500020483810 ) ) ;
#12164=CARTESIAN_POINT ( 'NONE',  ( 10.18810118749999916, 4.220049686691935698, 104.5000000020483668 ) ) ;
#12166=VECTOR ( 'NONE', #49488, 1000.000000000000000 ) ;
#12180=CARTESIAN_POINT ( 'NONE',  ( 7.204075437095966983, 7.204075437095967871, 70.46875000204836681 ) ) ;
#12191=CARTESIAN_POINT ( 'NONE',  ( 11.00000000000000000, 4.556349186104045934, 111.5312500040968047 ) ) ;
#12210=CARTESIAN_POINT ( 'NONE',  ( 7.204075437095966983, 7.204075437095967871, 80.59375000204838102 ) ) ;
#12216=CARTESIAN_POINT ( 'NONE',  ( -10.18810118749999916, 4.220049686691934809, 112.9375000020483810 ) ) ;
#12220=AXIS2_PLACEMENT_3D ( 'NONE', #53338, #65752, #24645 ) ;
#12225=CARTESIAN_POINT ( 'NONE',  ( -7.204075437095965206, -7.204075437095968759, 75.71875000204836681 ) ) ;
#12232=AXIS2_PLACEMENT_3D ( 'NONE', #8576, #24156, #70201 ) ;
#12238=CARTESIAN_POINT ( 'NONE',  ( 1.871523826299183495E-15, -10.18810118749999916, 74.03125000204836681 ) ) ;
#12251=CARTESIAN_POINT ( 'NONE',  ( -6.735557395310442023E-16, 11.00000000000000000, 93.81250000409677625 ) ) ;
#12264=DIRECTION ( 'NONE',  ( -0.000000000000000000, -0.000000000000000000, -1.000000000000000000 ) ) ;
#12286=CARTESIAN_POINT ( 'NONE',  ( 0.000000000000000000, 0.000000000000000000, 118.0000000000000000 ) ) ;
#12296=CARTESIAN_POINT ( 'NONE',  ( -11.00000000000000000, 0.000000000000000000, 101.6875000040967763 ) ) ;
#12308=CARTESIAN_POINT ( 'NONE',  ( -10.55165312886146367, 1.890739080934536576, 117.7907753267484878 ) ) ;
#12309=CARTESIAN_POINT ( 'NONE',  ( -7.204075437095967871, 7.204075437095967871, 100.4687500020483668 ) ) ;
#12321=CARTESIAN_POINT ( 'NONE',  ( 10.99999999999989697, -4.556349186104149851, 73.65625000000000000 ) ) ;
#12326=CARTESIAN_POINT ( 'NONE',  ( 4.220049686691941027, -10.18810118749999738, 97.00000000204838102 ) ) ;
#12331=CARTESIAN_POINT ( 'NONE',  ( 7.204075437095966983, 7.204075437095967871, 82.46875000204836681 ) ) ;
#12338=CARTESIAN_POINT ( 'NONE',  ( -4.220049686691937474, -10.18810118749999738, 87.43750000204838102 ) ) ;
#12347=CARTESIAN_POINT ( 'NONE',  ( -7.204075437095967871, 7.204075437095967871, 73.84375000204838102 ) ) ;
#12361=( BOUNDED_SURFACE ( )  B_SPLINE_SURFACE ( 1, 2, ( 
 ( #22044, #51845, #34890, #11119, #11854, #57895, #5092, #28460, #46179, #45807, #57526, #22787, #190, #23166, #5833, #57142, #74111, #68086, #16374, #34521, #39413, #6571, #5458, #28827, #40155, #69196, #6204, #62411, #34143, #40524, #28084, #29211, #52224, #69570, #17508, #10737, #56772, #51098, #51467, #45433, #16749, #74480, #68818, #556, #23539, #68446, #46551, #63159, #40898, #12216, #35252, #58270, #65746, #41269, #36348, #42362, #13677, #35614, #7675, #71030, #58628, #30682, #19348, #23910, #59001, #53700, #48019, #6936, #41992, #69945, #65377, #13311, #41637, #29947, #30313, #71395, #24638, #36716, #64648, #52961, #29578, #59363, #927, #46920, #1295, #24275, #2012, #19721, #8037, #59728, #42732, #18627, #47286, #54069, #25001, #14048, #25374, #2378, #31044, #35984, #48391, #37085, #60089, #64279, #47650, #52590, #70311, #18253, #12585, #12946, #7306, #53332, #1658, #70671, #18988, #65002, #54447, #54822, #21586, #72147, #49517, #20458, #43860, #66118, #31420, #8407, #38588, #38211, #15550, #44611, #43478, #66490, #38952, #8788, #25743, #14800, #14427, #67626, #15921, #26115, #50259, #37460, #21214, #32559, #48763, #43101, #73282, #26491, #26878, #9546, #71771, #67255, #55198, #3132, #2755, #20087, #55569, #60458, #27243, #3883, #72536, #61215, #15180, #31801, #49135, #9160, #37839, #60837, #32177, #49893, #3503, #20842, #66873, #72907, #44242, #61588, #9907, #32939, #55946, #4255, #74019, #69482, #17416, #33308, #23080, #11028, #45718, #51010, #34060, #73649, #470, #57056, #23451, #51755, #39690, #44984, #11765, #5370, #68363, #67990, #46463, #68729, #57432, #28370, #51378, #28737, #69108, #16286, #34431, #45347, #63072, #27621, #5739, #21956, #4623, #34803, #56306, #17044, #74390, #62689, #39326, #62324, #10650, #61955, #40067, #50630, #33682, #56685, #5003, #11395, #29120, #40439, #46089, #52138, #22321, #28001, #57809, #101, #16658, #17793, #22700, #10282, #63438, #6115, #18169, #30961, #7224, #29493, #13228, #69857, #840, #53981, #70949, #1577, #12130, #35169, #70230, #58543, #6488, #19265, #65290, #30227, #58183, #35530, #64195, #7589, #6847, #12499, #24187, #47932, #47200, #52503, #41911, #24916, #1206, #1929, #42277, #41184, #18540, #36264, #35897, #47565, #12858, #64919, #59280, #70588, #41547, #29862, #23826, #46831, #24557, #52874, #71314, #64564, #18904, #53247, #30596, #13595, #40806, #58914, #53615, #36633, #59640, #7957, #2291, #25288, #63816, #48305, #2668, #3042, #42647, #60372, #43391, #66406, #3415, #20756, #19633, #32470, #60752, #72823, #72056, #61501, #38499, #55858, #31331, #26400, #55480, #3792, #25659, #72448, #61123, #48675, #43771, #9454, #13957, #49048, #66785, #38124, #71682, #32088, #60004, #26792, #49428, #31712, #20002, #20373, #9824, #14714, #49807, #54735, #43012, #9075, #21130, #37752, #32850, #4174, #27161, #54358, #15089, #44152, #67167, #66033, #15462, #50178, #14340, #65659, #36998, #8320, #55108, #37371, #8698, #26026, #10941, #38869, #12331, #58011, #10566, #4539, #73935, #41379, #68279, #58375, #33597, #50546, #73196, #6317, #44523, #15835, #73562, #21872, #23652, #64390, #52700, #6681, #12688, #62239, #16200, #24014, #52330, #39240, #30056, #33226, #7048, #56603, #69678, #44900, #35722, #39611, #61875, #46659, #27534, #56225, #58737, #29683, #33976, #67538, #10197, #27913, #4919, #67906, #1034, #47023, #62609, #50923, #22238, #45268, #41009, #16574, #29321, #667, #70055, #17991, #64018, #35364, #18365, #21504, #54184, #25481, #36089, #13419, #59833, #7783, #71134, #30788, #13779, #42470, #19457, #65108, #30423, #47396, #24388, #48128, #70418, #2860, #42096, #65487, #2118, #36823, #2489, #53069, #70780, #48498, #7415, #71502, #19826, #37193, #8147, #1403, #64753, #53443, #59471, #41743, #36457, #25111, #31152, #42831, #65850, #18735, #14160, #60193, #19092, #53808, #8515, #13051, #59108, #1764, #24745, #31531, #54553, #47756, #47250, #57489, #63868, #23876, #40488, #24236, #18589, #52552, #46886, #64615, #11815, #891, #12180, #1624, #17092, #17468, #58964, #34853, #35217, #57859, #6535, #28791, #68782, #45771, #1258, #69909, #52925, #7271, #6165, #29174, #40114, #46142, #63120, #52189, #51806, #30279, #53299, #63493, #12911, #154, #58593, #18220, #11446, #5794, #35944 ),
 ( #41234, #34482, #23130, #46514, #69159, #520, #23500, #64241, #69533, #17845, #40861, #35579, #58236, #29541, #12551, #6899, #29910, #41600, #70277, #32140, #54782, #70635, #60425, #48353, #8369, #13644, #71359, #36314, #37803, #19684, #60799, #14391, #2344, #7640, #49099, #42694, #31009, #30645, #9124, #31385, #20047, #65706, #14011, #66081, #31762, #53664, #71733, #8002, #25706, #64965, #43065, #59330, #41958, #72112, #18954, #54411, #37047, #1976, #24604, #2718, #13275, #24968, #47984, #70997, #48726, #66456, #3093, #8752, #14764, #36682, #42324, #20425, #37425, #65342, #55161, #19313, #47611, #54034, #26078, #59694, #25338, #60048, #43441, #38901, #55517, #33256, #3829, #61159, #16606, #38158, #27570, #61904, #44559, #21163, #44186, #72858, #57002, #39643, #62640, #50955, #50209, #16234, #34008, #45295, #26826, #10228, #21903, #38535, #22273, #10973, #50578, #44933, #5316, #9859, #73595, #56255, #74335, #15126, #15498, #28318, #32887, #4572, #55889, #67940, #49839, #66824, #43809, #73967, #39271, #68308, #51327, #4203, #27193, #9491, #67200, #32505, #73230, #61536, #21536, #67572, #15869, #62271, #10600, #56635, #33628, #4949, #27948, #12809, #40750, #41128, #23770, #40015, #6796, #69426, #17363, #7168, #63017, #46774, #51699, #41494, #69798, #63759, #787, #29438, #68679, #35841, #23397, #16988, #57753, #46038, #18114, #11341, #58856, #30173, #12443, #6058, #69058, #34377, #34749, #11708, #70175, #29064, #53190, #52817, #57377, #6436, #64135, #22644, #35475, #12077, #1152, #417, #64511, #45664, #5686, #28685, #52449, #58489, #29806, #45, #24130, #47144, #23030, #18484, #40386, #63385, #52085, #46412, #17734, #35113, #58127, #41858, #14281, #59949, #13535, #7537, #2239, #43333, #71257, #60316, #36574, #53559, #1526, #8264, #47510, #18851, #1875, #24861, #25607, #66353, #54679, #8644, #14657, #65231, #19214, #25969, #54306, #42219, #32032, #36208, #9018, #59587, #71627, #47880, #37698, #42591, #70899, #37319, #65606, #24506, #60698, #31658, #36944, #70536, #64869, #30906, #7901, #13172, #2985, #48992, #13905, #59225, #53926, #25233, #42958, #48250, #19576, #31278, #72002, #2617, #30543, #48620, #20317, #19949, #65977, #62185, #9393, #32793, #50491, #50125, #61819, #27110, #4486, #56173, #10137, #61447, #3735, #72387, #26349, #38819, #49370, #10885, #9774, #33175, #44470, #15782, #16142, #55052, #44101, #44844, #32413, #10512, #33544, #73883, #27477, #3359, #20700, #38072, #38444, #43718, #21077, #4117, #73141, #73504, #66731, #68223, #55801, #15036, #15404, #26734, #21811, #61071, #16520, #39560, #67851, #21447, #49754, #55426, #67109, #67483, #27858, #39181, #62554, #56545, #72771, #4862, #50867, #22187, #45212, #57667, #45581, #47059, #5974, #70096, #23687, #11626, #16902, #58411, #28977, #40297, #39928, #18402, #17651, #29362, #334, #23315, #704, #41047, #62934, #6358, #68971, #51997, #68595, #46327, #11259, #51241, #6717, #28233, #40670, #69341, #34664, #34288, #57292, #5606, #41417, #29724, #52738, #64055, #63298, #52368, #24050, #35401, #28604, #63673, #12000, #51615, #12366, #1072, #35032, #58044, #64429, #74631, #46693, #69717, #33919, #5232, #22947, #56919, #45954, #18031, #17280, #74252, #22560, #35760, #12728, #42874, #42511, #19868, #25888, #1797, #47796, #43253, #13091, #30091, #70819, #18774, #48907, #71921, #30463, #54597, #41779, #25524, #36865, #53110, #47432, #2903, #30824, #31197, #13821, #1444, #71544, #59508, #7456, #20234, #24425, #59873, #64790, #31573, #8186, #53846, #65528, #24781, #36495, #70456, #58777, #7821, #7085, #2532, #65148, #36126, #37236, #2159, #19131, #59147, #53480, #71177, #54222, #25153, #48169, #48536, #65893, #42135, #14199, #13457, #19495, #60234, #8559, #26265, #8935, #39101, #60611, #50039, #9690, #67022, #43631, #66641, #20613, #4775, #62104, #10427, #73425, #72686, #38740, #56458, #67773, #3278, #32710, #44385, #60985, #44760, #33457, #73053, #67396, #27767, #32331, #21361, #55719, #22102, #37612, #37987, #50779, #55344, #4034, #3647, #27028, #49285, #14576, #66269, #21729, #15698, #16067, #73793, #26647, #49669, #31946, #14948, #54969, #20988, #72301, #9307, #44012, #15319, #38355, #61363, #4399, #61739, #10056, #33093, #56090, #27391, #50411, #46238, #62467, #29270, #17190 ) ),
 .UNSPECIFIED., .F., .F., .F. ) 
 B_SPLINE_SURFACE_WITH_KNOTS ( ( 2, 2 ),
 ( 3, 2, 2, 2, 2, 2, 2, 2, 2, 2, 2, 2, 2, 2, 2, 2, 2, 2, 2, 2, 2, 2, 2, 2, 2, 2, 2, 2, 2, 2, 2, 2, 2, 2, 2, 2, 2, 2, 2, 2, 2, 2, 2, 2, 2, 2, 2, 2, 2, 2, 2, 2, 2, 2, 2, 2, 2, 2, 2, 2, 2, 2, 2, 2, 2, 2, 2, 2, 2, 2, 2, 2, 2, 2, 2, 2, 2, 2, 2, 2, 2, 2, 2, 2, 2, 2, 2, 2, 2, 2, 2, 2, 2, 2, 2, 2, 2, 2, 2, 2, 2, 2, 2, 2, 2, 2, 2, 2, 2, 2, 2, 2, 2, 2, 2, 2, 2, 2, 2, 2, 2, 2, 2, 2, 2, 2, 2, 2, 2, 2, 2, 2, 2, 2, 2, 2, 2, 2, 2, 2, 2, 2, 2, 2, 2, 2, 2, 2, 2, 2, 2, 2, 2, 2, 2, 2, 2, 2, 2, 2, 2, 2, 2, 2, 2, 2, 2, 2, 2, 2, 2, 2, 2, 2, 2, 2, 2, 2, 2, 2, 2, 2, 2, 2, 2, 2, 2, 2, 2, 2, 2, 2, 2, 2, 2, 2, 2, 2, 2, 2, 2, 2, 2, 2, 2, 2, 2, 2, 2, 2, 2, 2, 2, 2, 2, 2, 2, 2, 2, 2, 2, 2, 2, 2, 2, 2, 2, 2, 2, 2, 2, 2, 2, 2, 2, 2, 2, 2, 2, 2, 2, 2, 2, 2, 2, 2, 2, 2, 2, 2, 2, 2, 2, 2, 2, 2, 2, 2, 2, 2, 2, 2, 2, 2, 2, 2, 2, 3 ),
 ( 0.000000000000000000, 1.000000000000000000 ),
 ( 0.000000000000000000, 0.003676470588235294067, 0.007352941176470588133, 0.01102941176470588307, 0.01470588235294117627, 0.01838235294117647120, 0.02205882352941176613, 0.02573529411764705760, 0.02941176470588235253, 0.03308823529411764747, 0.03676470588235294240, 0.04044117647058823733, 0.04411764705882353227, 0.04779411764705882026, 0.05147058823529411520, 0.05514705882352941013, 0.05882352941176470507, 0.06250000000000000000, 0.06617647058823529493, 0.06985294117647058987, 0.07352941176470588480, 0.07720588235294117974, 0.08088235294117647467, 0.08455882352941176960, 0.08823529411764706454, 0.09191176470588235947, 0.09558823529411764053, 0.09926470588235293546, 0.1029411764705882304, 0.1066176470588235253, 0.1102941176470588203, 0.1139705882352941152, 0.1176470588235294101, 0.1213235294117647051, 0.1250000000000000000, 0.1286764705882352811, 0.1323529411764705899, 0.1360294117647058709, 0.1397058823529411797, 0.1433823529411764608, 0.1470588235294117696, 0.1507352941176470507, 0.1544117647058823595, 0.1580882352941176405, 0.1617647058823529493, 0.1654411764705882304, 0.1691176470588235392, 0.1727941176470588203, 0.1764705882352941291, 0.1801470588235294101, 0.1838235294117647189, 0.1875000000000000000, 0.1911764705882352811, 0.1948529411764705899, 0.1985294117647058709, 0.2022058823529411797, 0.2058823529411764608, 0.2095588235294117696, 0.2132352941176470507, 0.2169117647058823595, 0.2205882352941176405, 0.2242647058823529493, 0.2279411764705882304, 0.2316176470588235392, 0.2352941176470588203, 0.2389705882352941291, 0.2426470588235294101, 0.2463235294117647189, 0.2500000000000000000, 0.2536764705882352811, 0.2573529411764705621, 0.2610294117647058987, 0.2647058823529411797, 0.2683823529411764608, 0.2720588235294117418, 0.2757352941176470784, 0.2794117647058823595, 0.2830882352941176405, 0.2867647058823529216, 0.2904411764705882582, 0.2941176470588235392, 0.2977941176470588203, 0.3014705882352941013, 0.3051470588235294379, 0.3088235294117647189, 0.3125000000000000000, 0.3161764705882352811, 0.3198529411764705621, 0.3235294117647058987, 0.3272058823529411797, 0.3308823529411764608, 0.3345588235294117418, 0.3382352941176470784, 0.3419117647058823595, 0.3455882352941176405, 0.3492647058823529216, 0.3529411764705882582, 0.3566176470588235392, 0.3602941176470588203, 0.3639705882352941013, 0.3676470588235294379, 0.3713235294117647189, 0.3750000000000000000, 0.3786764705882352811, 0.3823529411764705621, 0.3860294117647058987, 0.3897058823529411797, 0.3933823529411764608, 0.3970588235294117418, 0.4007352941176470784, 0.4044117647058823595, 0.4080882352941176405, 0.4117647058823529216, 0.4154411764705882582, 0.4191176470588235392, 0.4227941176470588203, 0.4264705882352941013, 0.4301470588235294379, 0.4338235294117647189, 0.4375000000000000000, 0.4411764705882352811, 0.4448529411764705621, 0.4485294117647058987, 0.4522058823529411797, 0.4558823529411764608, 0.4595588235294117418, 0.4632352941176470784, 0.4669117647058823595, 0.4705882352941176405, 0.4742647058823529216, 0.4779411764705882582, 0.4816176470588235392, 0.4852941176470588203, 0.4889705882352941013, 0.4926470588235294379, 0.4963235294117647189, 0.5000000000000000000, 0.5036764705882352811, 0.5073529411764705621, 0.5110294117647058432, 0.5147058823529411242, 0.5183823529411765163, 0.5220588235294117974, 0.5257352941176470784, 0.5294117647058823595, 0.5330882352941176405, 0.5367647058823529216, 0.5404411764705882026, 0.5441176470588234837, 0.5477941176470588758, 0.5514705882352941568, 0.5551470588235294379, 0.5588235294117647189, 0.5625000000000000000, 0.5661764705882352811, 0.5698529411764705621, 0.5735294117647058432, 0.5772058823529411242, 0.5808823529411765163, 0.5845588235294117974, 0.5882352941176470784, 0.5919117647058823595, 0.5955882352941176405, 0.5992647058823529216, 0.6029411764705882026, 0.6066176470588234837, 0.6102941176470588758, 0.6139705882352941568, 0.6176470588235294379, 0.6213235294117647189, 0.6250000000000000000, 0.6286764705882352811, 0.6323529411764705621, 0.6360294117647058432, 0.6397058823529411242, 0.6433823529411765163, 0.6470588235294117974, 0.6507352941176470784, 0.6544117647058823595, 0.6580882352941176405, 0.6617647058823529216, 0.6654411764705882026, 0.6691176470588234837, 0.6727941176470588758, 0.6764705882352941568, 0.6801470588235294379, 0.6838235294117647189, 0.6875000000000000000, 0.6911764705882352811, 0.6948529411764705621, 0.6985294117647058432, 0.7022058823529411242, 0.7058823529411765163, 0.7095588235294117974, 0.7132352941176470784, 0.7169117647058823595, 0.7205882352941176405, 0.7242647058823529216, 0.7279411764705882026, 0.7316176470588234837, 0.7352941176470588758, 0.7389705882352941568, 0.7426470588235294379, 0.7463235294117647189, 0.7500000000000000000, 0.7536764705882352811, 0.7573529411764705621, 0.7610294117647058432, 0.7647058823529411242, 0.7683823529411765163, 0.7720588235294117974, 0.7757352941176470784, 0.7794117647058823595, 0.7830882352941176405, 0.7867647058823529216, 0.7904411764705882026, 0.7941176470588234837, 0.7977941176470588758, 0.8014705882352941568, 0.8051470588235294379, 0.8088235294117647189, 0.8125000000000000000, 0.8161764705882352811, 0.8198529411764705621, 0.8235294117647058432, 0.8272058823529411242, 0.8308823529411765163, 0.8345588235294117974, 0.8382352941176470784, 0.8419117647058823595, 0.8455882352941176405, 0.8492647058823529216, 0.8529411764705882026, 0.8566176470588234837, 0.8602941176470588758, 0.8639705882352941568, 0.8676470588235294379, 0.8713235294117647189, 0.8750000000000000000, 0.8786764705882352811, 0.8823529411764705621, 0.8860294117647058432, 0.8897058823529411242, 0.8933823529411765163, 0.8970588235294117974, 0.9007352941176470784, 0.9044117647058823595, 0.9080882352941176405, 0.9117647058823529216, 0.9154411764705882026, 0.9191176470588234837, 0.9227941176470588758, 0.9264705882352941568, 0.9301470588235294379, 0.9338235294117647189, 0.9375000000000000000, 0.9411764705882352811, 0.9448529411764705621, 0.9485294117647058432, 0.9522058823529411242, 0.9558823529411765163, 0.9595588235294117974, 0.9632352941176470784, 0.9669117647058823595, 0.9705882352941176405, 0.9742647058823529216, 0.9779411764705882026, 0.9803851213646477269 ),
 .UNSPECIFIED. ) 
 GEOMETRIC_REPRESENTATION_ITEM ( )  RATIONAL_B_SPLINE_SURFACE ( (
 ( 1.000000000000000000, 0.9238795325112867385, 1.000000000000000000, 0.9238795325112867385, 1.000000000000000000, 0.9238795325112867385, 1.000000000000000000, 0.9238795325112867385, 1.000000000000000000, 0.9238795325112867385, 1.000000000000000000, 0.9238795325112867385, 1.000000000000000000, 0.9238795325112867385, 1.000000000000000000, 0.9238795325112867385, 1.000000000000000000, 0.9238795325112867385, 1.000000000000000000, 0.9238795325112867385, 1.000000000000000000, 0.9238795325112867385, 1.000000000000000000, 0.9238795325112867385, 1.000000000000000000, 0.9238795325112867385, 1.000000000000000000, 0.9238795325112867385, 1.000000000000000000, 0.9238795325112867385, 1.000000000000000000, 0.9238795325112867385, 1.000000000000000000, 0.9238795325112867385, 1.000000000000000000, 0.9238795325112867385, 1.000000000000000000, 0.9238795325112867385, 1.000000000000000000, 0.9238795325112867385, 1.000000000000000000, 0.9238795325112867385, 1.000000000000000000, 0.9238795325112867385, 1.000000000000000000, 0.9238795325112867385, 1.000000000000000000, 0.9238795325112867385, 1.000000000000000000, 0.9238795325112867385, 1.000000000000000000, 0.9238795325112867385, 1.000000000000000000, 0.9238795325112867385, 1.000000000000000000, 0.9238795325112867385, 1.000000000000000000, 0.9238795325112867385, 1.000000000000000000, 0.9238795325112867385, 1.000000000000000000, 0.9238795325112867385, 1.000000000000000000, 0.9238795325112867385, 1.000000000000000000, 0.9238795325112867385, 1.000000000000000000, 0.9238795325112867385, 1.000000000000000000, 0.9238795325112867385, 1.000000000000000000, 0.9238795325112867385, 1.000000000000000000, 0.9238795325112867385, 1.000000000000000000, 0.9238795325112867385, 1.000000000000000000, 0.9238795325112867385, 1.000000000000000000, 0.9238795325112867385, 1.000000000000000000, 0.9238795325112867385, 1.000000000000000000, 0.9238795325112867385, 1.000000000000000000, 0.9238795325112867385, 1.000000000000000000, 0.9238795325112867385, 1.000000000000000000, 0.9238795325112867385, 1.000000000000000000, 0.9238795325112867385, 1.000000000000000000, 0.9238795325112867385, 1.000000000000000000, 0.9238795325112867385, 1.000000000000000000, 0.9238795325112867385, 1.000000000000000000, 0.9238795325112867385, 1.000000000000000000, 0.9238795325112867385, 1.000000000000000000, 0.9238795325112867385, 1.000000000000000000, 0.9238795325112867385, 1.000000000000000000, 0.9238795325112867385, 1.000000000000000000, 0.9238795325112867385, 1.000000000000000000, 0.9238795325112867385, 1.000000000000000000, 0.9238795325112867385, 1.000000000000000000, 0.9238795325112867385, 1.000000000000000000, 0.9238795325112867385, 1.000000000000000000, 0.9238795325112867385, 1.000000000000000000, 0.9238795325112867385, 1.000000000000000000, 0.9238795325112867385, 1.000000000000000000, 0.9238795325112867385, 1.000000000000000000, 0.9238795325112867385, 1.000000000000000000, 0.9238795325112867385, 1.000000000000000000, 0.9238795325112867385, 1.000000000000000000, 0.9238795325112867385, 1.000000000000000000, 0.9238795325112867385, 1.000000000000000000, 0.9238795325112867385, 1.000000000000000000, 0.9238795325112867385, 1.000000000000000000, 0.9238795325112867385, 1.000000000000000000, 0.9238795325112867385, 1.000000000000000000, 0.9238795325112867385, 1.000000000000000000, 0.9238795325112867385, 1.000000000000000000, 0.9238795325112867385, 1.000000000000000000, 0.9238795325112867385, 1.000000000000000000, 0.9238795325112867385, 1.000000000000000000, 0.9238795325112867385, 1.000000000000000000, 0.9238795325112867385, 1.000000000000000000, 0.9238795325112867385, 1.000000000000000000, 0.9238795325112867385, 1.000000000000000000, 0.9238795325112867385, 1.000000000000000000, 0.9238795325112867385, 1.000000000000000000, 0.9238795325112867385, 1.000000000000000000, 0.9238795325112867385, 1.000000000000000000, 0.9238795325112867385, 1.000000000000000000, 0.9238795325112867385, 1.000000000000000000, 0.9238795325112867385, 1.000000000000000000, 0.9238795325112867385, 1.000000000000000000, 0.9238795325112867385, 1.000000000000000000, 0.9238795325112867385, 1.000000000000000000, 0.9238795325112867385, 1.000000000000000000, 0.9238795325112867385, 1.000000000000000000, 0.9238795325112867385, 1.000000000000000000, 0.9238795325112867385, 1.000000000000000000, 0.9238795325112867385, 1.000000000000000000, 0.9238795325112867385, 1.000000000000000000, 0.9238795325112867385, 1.000000000000000000, 0.9238795325112867385, 1.000000000000000000, 0.9238795325112867385, 1.000000000000000000, 0.9238795325112867385, 1.000000000000000000, 0.9238795325112867385, 1.000000000000000000, 0.9238795325112867385, 1.000000000000000000, 0.9238795325112867385, 1.000000000000000000, 0.9238795325112867385, 1.000000000000000000, 0.9238795325112867385, 1.000000000000000000, 0.9238795325112867385, 1.000000000000000000, 0.9238795325112867385, 1.000000000000000000, 0.9238795325112867385, 1.000000000000000000, 0.9238795325112867385, 1.000000000000000000, 0.9238795325112867385, 1.000000000000000000, 0.9238795325112867385, 1.000000000000000000, 0.9238795325112867385, 1.000000000000000000, 0.9238795325112867385, 1.000000000000000000, 0.9238795325112867385, 1.000000000000000000, 0.9238795325112867385, 1.000000000000000000, 0.9238795325112867385, 1.000000000000000000, 0.9238795325112867385, 1.000000000000000000, 0.9238795325112867385, 1.000000000000000000, 0.9238795325112867385, 1.000000000000000000, 0.9238795325112867385, 1.000000000000000000, 0.9238795325112867385, 1.000000000000000000, 0.9238795325112867385, 1.000000000000000000, 0.9238795325112867385, 1.000000000000000000, 0.9238795325112867385, 1.000000000000000000, 0.9238795325112867385, 1.000000000000000000, 0.9238795325112867385, 1.000000000000000000, 0.9238795325112867385, 1.000000000000000000, 0.9238795325112867385, 1.000000000000000000, 0.9238795325112867385, 1.000000000000000000, 0.9238795325112867385, 1.000000000000000000, 0.9238795325112867385, 1.000000000000000000, 0.9238795325112867385, 1.000000000000000000, 0.9238795325112867385, 1.000000000000000000, 0.9238795325112867385, 1.000000000000000000, 0.9238795325112867385, 1.000000000000000000, 0.9238795325112867385, 1.000000000000000000, 0.9238795325112867385, 1.000000000000000000, 0.9238795325112867385, 1.000000000000000000, 0.9238795325112867385, 1.000000000000000000, 0.9238795325112867385, 1.000000000000000000, 0.9238795325112867385, 1.000000000000000000, 0.9238795325112867385, 1.000000000000000000, 0.9238795325112867385, 1.000000000000000000, 0.9238795325112867385, 1.000000000000000000, 0.9238795325112867385, 1.000000000000000000, 0.9238795325112867385, 1.000000000000000000, 0.9238795325112867385, 1.000000000000000000, 0.9238795325112867385, 1.000000000000000000, 0.9238795325112867385, 1.000000000000000000, 0.9238795325112867385, 1.000000000000000000, 0.9238795325112867385, 1.000000000000000000, 0.9238795325112867385, 1.000000000000000000, 0.9238795325112867385, 1.000000000000000000, 0.9238795325112867385, 1.000000000000000000, 0.9238795325112867385, 1.000000000000000000, 0.9238795325112867385, 1.000000000000000000, 0.9238795325112867385, 1.000000000000000000, 0.9238795325112867385, 1.000000000000000000, 0.9238795325112867385, 1.000000000000000000, 0.9238795325112867385, 1.000000000000000000, 0.9238795325112867385, 1.000000000000000000, 0.9238795325112867385, 1.000000000000000000, 0.9238795325112867385, 1.000000000000000000, 0.9238795325112867385, 1.000000000000000000, 0.9238795325112867385, 1.000000000000000000, 0.9238795325112867385, 1.000000000000000000, 0.9238795325112867385, 1.000000000000000000, 0.9238795325112867385, 1.000000000000000000, 0.9238795325112867385, 1.000000000000000000, 0.9238795325112867385, 1.000000000000000000, 0.9238795325112867385, 1.000000000000000000, 0.9238795325112867385, 1.000000000000000000, 0.9238795325112867385, 1.000000000000000000, 0.9238795325112867385, 1.000000000000000000, 0.9238795325112867385, 1.000000000000000000, 0.9238795325112867385, 1.000000000000000000, 0.9238795325112867385, 1.000000000000000000, 0.9238795325112867385, 1.000000000000000000, 0.9238795325112867385, 1.000000000000000000, 0.9238795325112867385, 1.000000000000000000, 0.9238795325112867385, 1.000000000000000000, 0.9238795325112867385, 1.000000000000000000, 0.9238795325112867385, 1.000000000000000000, 0.9238795325112867385, 1.000000000000000000, 0.9238795325112867385, 1.000000000000000000, 0.9238795325112867385, 1.000000000000000000, 0.9238795325112867385, 1.000000000000000000, 0.9238795325112867385, 1.000000000000000000, 0.9238795325112867385, 1.000000000000000000, 0.9238795325112867385, 1.000000000000000000, 0.9238795325112867385, 1.000000000000000000, 0.9238795325112867385, 1.000000000000000000, 0.9238795325112867385, 1.000000000000000000, 0.9238795325112867385, 1.000000000000000000, 0.9238795325112867385, 1.000000000000000000, 0.9238795325112867385, 1.000000000000000000, 0.9238795325112867385, 1.000000000000000000, 0.9238795325112867385, 1.000000000000000000, 0.9238795325112867385, 1.000000000000000000, 0.9238795325112867385, 1.000000000000000000, 0.9238795325112867385, 1.000000000000000000, 0.9238795325112867385, 1.000000000000000000, 0.9238795325112867385, 1.000000000000000000, 0.9238795325112867385, 1.000000000000000000, 0.9238795325112867385, 1.000000000000000000, 0.9238795325112867385, 1.000000000000000000, 0.9238795325112867385, 1.000000000000000000, 0.9238795325112867385, 1.000000000000000000, 0.9238795325112867385, 1.000000000000000000, 0.9238795325112867385, 1.000000000000000000, 0.9238795325112867385, 1.000000000000000000, 0.9238795325112867385, 1.000000000000000000, 0.9238795325112867385, 1.000000000000000000, 0.9238795325112867385, 1.000000000000000000, 0.9238795325112867385, 1.000000000000000000, 0.9238795325112867385, 1.000000000000000000, 0.9238795325112867385, 1.000000000000000000, 0.9238795325112867385, 1.000000000000000000, 0.9238795325112867385, 1.000000000000000000, 0.9238795325112867385, 1.000000000000000000, 0.9238795325112867385, 1.000000000000000000, 0.9238795325112867385, 1.000000000000000000, 0.9238795325112867385, 1.000000000000000000, 0.9238795325112867385, 1.000000000000000000, 0.9238795325112867385, 1.000000000000000000, 0.9238795325112867385, 1.000000000000000000, 0.9238795325112867385, 1.000000000000000000, 0.9238795325112867385, 1.000000000000000000, 0.9238795325112867385, 1.000000000000000000, 0.9238795325112867385, 1.000000000000000000, 0.9238795325112867385, 1.000000000000000000, 0.9238795325112867385, 1.000000000000000000, 0.9238795325112867385, 1.000000000000000000, 0.9238795325112867385, 1.000000000000000000, 0.9238795325112867385, 1.000000000000000000, 0.9238795325112867385, 1.000000000000000000, 0.9238795325112867385, 1.000000000000000000, 0.9238795325112867385, 1.000000000000000000, 0.9238795325112867385, 1.000000000000000000, 0.9238795325112867385, 1.000000000000000000, 0.9238795325112867385, 1.000000000000000000, 0.9238795325112867385, 1.000000000000000000, 0.9238795325112867385, 1.000000000000000000, 0.9238795325112867385, 1.000000000000000000, 0.9238795325112867385, 1.000000000000000000, 0.9238795325112867385, 1.000000000000000000, 0.9238795325112867385, 1.000000000000000000, 0.9238795325112867385, 1.000000000000000000, 0.9238795325112867385, 1.000000000000000000, 0.9238795325112867385, 1.000000000000000000, 0.9238795325112867385, 1.000000000000000000, 0.9238795325112867385, 1.000000000000000000, 0.9238795325112867385, 1.000000000000000000, 0.9238795325112867385, 1.000000000000000000, 0.9238795325112867385, 1.000000000000000000, 0.9238795325112867385, 1.000000000000000000, 0.9238795325112867385, 1.000000000000000000, 0.9238795325112867385, 1.000000000000000000, 0.9238795325112867385, 1.000000000000000000, 0.9238795325112867385, 1.000000000000000000, 0.9238795325112867385, 1.000000000000000000, 0.9238795325112867385, 1.000000000000000000, 0.9238795325112867385, 1.000000000000000000, 0.9238795325112867385, 1.000000000000000000, 0.9238795325112867385, 1.000000000000000000, 0.9493986900241293547, 0.9660721264009082265),
 ( 1.000000000000000000, 0.9238795325112867385, 1.000000000000000000, 0.9238795325112867385, 1.000000000000000000, 0.9238795325112867385, 1.000000000000000000, 0.9238795325112867385, 1.000000000000000000, 0.9238795325112867385, 1.000000000000000000, 0.9238795325112867385, 1.000000000000000000, 0.9238795325112867385, 1.000000000000000000, 0.9238795325112867385, 1.000000000000000000, 0.9238795325112867385, 1.000000000000000000, 0.9238795325112867385, 1.000000000000000000, 0.9238795325112867385, 1.000000000000000000, 0.9238795325112867385, 1.000000000000000000, 0.9238795325112867385, 1.000000000000000000, 0.9238795325112867385, 1.000000000000000000, 0.9238795325112867385, 1.000000000000000000, 0.9238795325112867385, 1.000000000000000000, 0.9238795325112867385, 1.000000000000000000, 0.9238795325112867385, 1.000000000000000000, 0.9238795325112867385, 1.000000000000000000, 0.9238795325112867385, 1.000000000000000000, 0.9238795325112867385, 1.000000000000000000, 0.9238795325112867385, 1.000000000000000000, 0.9238795325112867385, 1.000000000000000000, 0.9238795325112867385, 1.000000000000000000, 0.9238795325112867385, 1.000000000000000000, 0.9238795325112867385, 1.000000000000000000, 0.9238795325112867385, 1.000000000000000000, 0.9238795325112867385, 1.000000000000000000, 0.9238795325112867385, 1.000000000000000000, 0.9238795325112867385, 1.000000000000000000, 0.9238795325112867385, 1.000000000000000000, 0.9238795325112867385, 1.000000000000000000, 0.9238795325112867385, 1.000000000000000000, 0.9238795325112867385, 1.000000000000000000, 0.9238795325112867385, 1.000000000000000000, 0.9238795325112867385, 1.000000000000000000, 0.9238795325112867385, 1.000000000000000000, 0.9238795325112867385, 1.000000000000000000, 0.9238795325112867385, 1.000000000000000000, 0.9238795325112867385, 1.000000000000000000, 0.9238795325112867385, 1.000000000000000000, 0.9238795325112867385, 1.000000000000000000, 0.9238795325112867385, 1.000000000000000000, 0.9238795325112867385, 1.000000000000000000, 0.9238795325112867385, 1.000000000000000000, 0.9238795325112867385, 1.000000000000000000, 0.9238795325112867385, 1.000000000000000000, 0.9238795325112867385, 1.000000000000000000, 0.9238795325112867385, 1.000000000000000000, 0.9238795325112867385, 1.000000000000000000, 0.9238795325112867385, 1.000000000000000000, 0.9238795325112867385, 1.000000000000000000, 0.9238795325112867385, 1.000000000000000000, 0.9238795325112867385, 1.000000000000000000, 0.9238795325112867385, 1.000000000000000000, 0.9238795325112867385, 1.000000000000000000, 0.9238795325112867385, 1.000000000000000000, 0.9238795325112867385, 1.000000000000000000, 0.9238795325112867385, 1.000000000000000000, 0.9238795325112867385, 1.000000000000000000, 0.9238795325112867385, 1.000000000000000000, 0.9238795325112867385, 1.000000000000000000, 0.9238795325112867385, 1.000000000000000000, 0.9238795325112867385, 1.000000000000000000, 0.9238795325112867385, 1.000000000000000000, 0.9238795325112867385, 1.000000000000000000, 0.9238795325112867385, 1.000000000000000000, 0.9238795325112867385, 1.000000000000000000, 0.9238795325112867385, 1.000000000000000000, 0.9238795325112867385, 1.000000000000000000, 0.9238795325112867385, 1.000000000000000000, 0.9238795325112867385, 1.000000000000000000, 0.9238795325112867385, 1.000000000000000000, 0.9238795325112867385, 1.000000000000000000, 0.9238795325112867385, 1.000000000000000000, 0.9238795325112867385, 1.000000000000000000, 0.9238795325112867385, 1.000000000000000000, 0.9238795325112867385, 1.000000000000000000, 0.9238795325112867385, 1.000000000000000000, 0.9238795325112867385, 1.000000000000000000, 0.9238795325112867385, 1.000000000000000000, 0.9238795325112867385, 1.000000000000000000, 0.9238795325112867385, 1.000000000000000000, 0.9238795325112867385, 1.000000000000000000, 0.9238795325112867385, 1.000000000000000000, 0.9238795325112867385, 1.000000000000000000, 0.9238795325112867385, 1.000000000000000000, 0.9238795325112867385, 1.000000000000000000, 0.9238795325112867385, 1.000000000000000000, 0.9238795325112867385, 1.000000000000000000, 0.9238795325112867385, 1.000000000000000000, 0.9238795325112867385, 1.000000000000000000, 0.9238795325112867385, 1.000000000000000000, 0.9238795325112867385, 1.000000000000000000, 0.9238795325112867385, 1.000000000000000000, 0.9238795325112867385, 1.000000000000000000, 0.9238795325112867385, 1.000000000000000000, 0.9238795325112867385, 1.000000000000000000, 0.9238795325112867385, 1.000000000000000000, 0.9238795325112867385, 1.000000000000000000, 0.9238795325112867385, 1.000000000000000000, 0.9238795325112867385, 1.000000000000000000, 0.9238795325112867385, 1.000000000000000000, 0.9238795325112867385, 1.000000000000000000, 0.9238795325112867385, 1.000000000000000000, 0.9238795325112867385, 1.000000000000000000, 0.9238795325112867385, 1.000000000000000000, 0.9238795325112867385, 1.000000000000000000, 0.9238795325112867385, 1.000000000000000000, 0.9238795325112867385, 1.000000000000000000, 0.9238795325112867385, 1.000000000000000000, 0.9238795325112867385, 1.000000000000000000, 0.9238795325112867385, 1.000000000000000000, 0.9238795325112867385, 1.000000000000000000, 0.9238795325112867385, 1.000000000000000000, 0.9238795325112867385, 1.000000000000000000, 0.9238795325112867385, 1.000000000000000000, 0.9238795325112867385, 1.000000000000000000, 0.9238795325112867385, 1.000000000000000000, 0.9238795325112867385, 1.000000000000000000, 0.9238795325112867385, 1.000000000000000000, 0.9238795325112867385, 1.000000000000000000, 0.9238795325112867385, 1.000000000000000000, 0.9238795325112867385, 1.000000000000000000, 0.9238795325112867385, 1.000000000000000000, 0.9238795325112867385, 1.000000000000000000, 0.9238795325112867385, 1.000000000000000000, 0.9238795325112867385, 1.000000000000000000, 0.9238795325112867385, 1.000000000000000000, 0.9238795325112867385, 1.000000000000000000, 0.9238795325112867385, 1.000000000000000000, 0.9238795325112867385, 1.000000000000000000, 0.9238795325112867385, 1.000000000000000000, 0.9238795325112867385, 1.000000000000000000, 0.9238795325112867385, 1.000000000000000000, 0.9238795325112867385, 1.000000000000000000, 0.9238795325112867385, 1.000000000000000000, 0.9238795325112867385, 1.000000000000000000, 0.9238795325112867385, 1.000000000000000000, 0.9238795325112867385, 1.000000000000000000, 0.9238795325112867385, 1.000000000000000000, 0.9238795325112867385, 1.000000000000000000, 0.9238795325112867385, 1.000000000000000000, 0.9238795325112867385, 1.000000000000000000, 0.9238795325112867385, 1.000000000000000000, 0.9238795325112867385, 1.000000000000000000, 0.9238795325112867385, 1.000000000000000000, 0.9238795325112867385, 1.000000000000000000, 0.9238795325112867385, 1.000000000000000000, 0.9238795325112867385, 1.000000000000000000, 0.9238795325112867385, 1.000000000000000000, 0.9238795325112867385, 1.000000000000000000, 0.9238795325112867385, 1.000000000000000000, 0.9238795325112867385, 1.000000000000000000, 0.9238795325112867385, 1.000000000000000000, 0.9238795325112867385, 1.000000000000000000, 0.9238795325112867385, 1.000000000000000000, 0.9238795325112867385, 1.000000000000000000, 0.9238795325112867385, 1.000000000000000000, 0.9238795325112867385, 1.000000000000000000, 0.9238795325112867385, 1.000000000000000000, 0.9238795325112867385, 1.000000000000000000, 0.9238795325112867385, 1.000000000000000000, 0.9238795325112867385, 1.000000000000000000, 0.9238795325112867385, 1.000000000000000000, 0.9238795325112867385, 1.000000000000000000, 0.9238795325112867385, 1.000000000000000000, 0.9238795325112867385, 1.000000000000000000, 0.9238795325112867385, 1.000000000000000000, 0.9238795325112867385, 1.000000000000000000, 0.9238795325112867385, 1.000000000000000000, 0.9238795325112867385, 1.000000000000000000, 0.9238795325112867385, 1.000000000000000000, 0.9238795325112867385, 1.000000000000000000, 0.9238795325112867385, 1.000000000000000000, 0.9238795325112867385, 1.000000000000000000, 0.9238795325112867385, 1.000000000000000000, 0.9238795325112867385, 1.000000000000000000, 0.9238795325112867385, 1.000000000000000000, 0.9238795325112867385, 1.000000000000000000, 0.9238795325112867385, 1.000000000000000000, 0.9238795325112867385, 1.000000000000000000, 0.9238795325112867385, 1.000000000000000000, 0.9238795325112867385, 1.000000000000000000, 0.9238795325112867385, 1.000000000000000000, 0.9238795325112867385, 1.000000000000000000, 0.9238795325112867385, 1.000000000000000000, 0.9238795325112867385, 1.000000000000000000, 0.9238795325112867385, 1.000000000000000000, 0.9238795325112867385, 1.000000000000000000, 0.9238795325112867385, 1.000000000000000000, 0.9238795325112867385, 1.000000000000000000, 0.9238795325112867385, 1.000000000000000000, 0.9238795325112867385, 1.000000000000000000, 0.9238795325112867385, 1.000000000000000000, 0.9238795325112867385, 1.000000000000000000, 0.9238795325112867385, 1.000000000000000000, 0.9238795325112867385, 1.000000000000000000, 0.9238795325112867385, 1.000000000000000000, 0.9238795325112867385, 1.000000000000000000, 0.9238795325112867385, 1.000000000000000000, 0.9238795325112867385, 1.000000000000000000, 0.9238795325112867385, 1.000000000000000000, 0.9238795325112867385, 1.000000000000000000, 0.9238795325112867385, 1.000000000000000000, 0.9238795325112867385, 1.000000000000000000, 0.9238795325112867385, 1.000000000000000000, 0.9238795325112867385, 1.000000000000000000, 0.9238795325112867385, 1.000000000000000000, 0.9238795325112867385, 1.000000000000000000, 0.9238795325112867385, 1.000000000000000000, 0.9238795325112867385, 1.000000000000000000, 0.9238795325112867385, 1.000000000000000000, 0.9238795325112867385, 1.000000000000000000, 0.9238795325112867385, 1.000000000000000000, 0.9238795325112867385, 1.000000000000000000, 0.9238795325112867385, 1.000000000000000000, 0.9238795325112867385, 1.000000000000000000, 0.9238795325112867385, 1.000000000000000000, 0.9238795325112867385, 1.000000000000000000, 0.9238795325112867385, 1.000000000000000000, 0.9238795325112867385, 1.000000000000000000, 0.9238795325112867385, 1.000000000000000000, 0.9238795325112867385, 1.000000000000000000, 0.9238795325112867385, 1.000000000000000000, 0.9238795325112867385, 1.000000000000000000, 0.9238795325112867385, 1.000000000000000000, 0.9238795325112867385, 1.000000000000000000, 0.9238795325112867385, 1.000000000000000000, 0.9238795325112867385, 1.000000000000000000, 0.9238795325112867385, 1.000000000000000000, 0.9238795325112867385, 1.000000000000000000, 0.9238795325112867385, 1.000000000000000000, 0.9238795325112867385, 1.000000000000000000, 0.9238795325112867385, 1.000000000000000000, 0.9238795325112867385, 1.000000000000000000, 0.9238795325112867385, 1.000000000000000000, 0.9238795325112867385, 1.000000000000000000, 0.9238795325112867385, 1.000000000000000000, 0.9238795325112867385, 1.000000000000000000, 0.9238795325112867385, 1.000000000000000000, 0.9238795325112867385, 1.000000000000000000, 0.9238795325112867385, 1.000000000000000000, 0.9238795325112867385, 1.000000000000000000, 0.9238795325112867385, 1.000000000000000000, 0.9238795325112867385, 1.000000000000000000, 0.9238795325112867385, 1.000000000000000000, 0.9238795325112867385, 1.000000000000000000, 0.9238795325112867385, 1.000000000000000000, 0.9238795325112867385, 1.000000000000000000, 0.9238795325112867385, 1.000000000000000000, 0.9238795325112867385, 1.000000000000000000, 0.9238795325112867385, 1.000000000000000000, 0.9238795325112867385, 1.000000000000000000, 0.9238795325112867385, 1.000000000000000000, 0.9238795325112867385, 1.000000000000000000, 0.9238795325112867385, 1.000000000000000000, 0.9238795325112867385, 1.000000000000000000, 0.9238795325112867385, 1.000000000000000000, 0.9238795325112867385, 1.000000000000000000, 0.9238795325112867385, 1.000000000000000000, 0.9238795325112867385, 1.000000000000000000, 0.9238795325112867385, 1.000000000000000000, 0.9238795325112867385, 1.000000000000000000, 0.9238795325112867385, 1.000000000000000000, 0.9238795325112867385, 1.000000000000000000, 0.9493986900241293547, 0.9660721264009082265) ) ) 
 REPRESENTATION_ITEM ( '' )  SURFACE ( )  );
#12363=CARTESIAN_POINT ( 'NONE',  ( -4.220049686691935698, 10.18810118749999916, 70.37500000204838102 ) ) ;
#12366=CARTESIAN_POINT ( 'NONE',  ( -7.778174593052023411, 7.778174593052023411, 81.81249999999998579 ) ) ;
#12391=CARTESIAN_POINT ( 'NONE',  ( -11.00000000000000000, 0.000000000000000000, 80.68750000409677625 ) ) ;
#12393=CARTESIAN_POINT ( 'NONE',  ( -6.735557395310442023E-16, 11.00000000000000000, 69.81250000409677625 ) ) ;
#12404=CARTESIAN_POINT ( 'NONE',  ( -7.204075437095967871, 7.204075437095967871, 112.8437500020483810 ) ) ;
#12435=EDGE_CURVE ( 'NONE', #37130, #73625, #56899, .T. ) ;
#12440=CARTESIAN_POINT ( 'NONE',  ( -10.18810118749999916, 0.000000000000000000, 84.15625000204838102 ) ) ;
#12443=CARTESIAN_POINT ( 'NONE',  ( -7.778174593052020747, -7.778174593052023411, 101.6874999999999858 ) ) ;
#12474=CARTESIAN_POINT ( 'NONE',  ( 4.556349186104045934, 11.00000000000000000, 87.71875000409677625 ) ) ;
#12490=ORIENTED_EDGE ( 'NONE', *, *, #60922, .T. ) ;
#12491=CARTESIAN_POINT ( 'NONE',  ( 2.020667218593132706E-15, -11.00000000000000000, 100.3749999999999858 ) ) ;
#12499=CARTESIAN_POINT ( 'NONE',  ( 4.220049686691941027, -10.18810118749999738, 92.50000000204838102 ) ) ;
#12504=CARTESIAN_POINT ( 'NONE',  ( 10.18810118749999916, 4.220049686691935698, 109.0000000020483810 ) ) ;
#12513=CARTESIAN_POINT ( 'NONE',  ( -4.220049686691937474, -10.18810118749999738, 104.3125000020483810 ) ) ;
#12531=CARTESIAN_POINT ( 'NONE',  ( 4.220049686691941027, -10.18810118749999738, 104.1250000020483810 ) ) ;
#12537=ADVANCED_FACE ( 'NONE', ( #20512 ), #26170, .T. ) ;
#12538=ADVANCED_FACE ( 'NONE', ( #65052 ), #60515, .T. ) ;
#12551=CARTESIAN_POINT ( 'NONE',  ( -7.778174593052020747, -7.778174593052023411, 116.6875000000000000 ) ) ;
#12559=ORIENTED_EDGE ( 'NONE', *, *, #59652, .F. ) ;
#12563=CARTESIAN_POINT ( 'NONE',  ( -7.778174593052020747, -7.778174593052023411, 103.3750000040967763 ) ) ;
#12578=DIRECTION ( 'NONE',  ( -1.000000000000000000, 0.000000000000000000, 0.000000000000000000 ) ) ;
#12581=CARTESIAN_POINT ( 'NONE',  ( -4.220049686691935698, 10.18810118749999916, 82.37500000204838102 ) ) ;
#12585=CARTESIAN_POINT ( 'NONE',  ( 1.871523826299183495E-15, -10.18810118749999916, 107.4062500020483668 ) ) ;
#12589=CARTESIAN_POINT ( 'NONE',  ( -11.00000000000000000, 0.000000000000000000, 109.1875000040967763 ) ) ;
#12593=CARTESIAN_POINT ( 'NONE',  ( -10.18810118749999916, 0.000000000000000000, 75.53125000204836681 ) ) ;
#12606=CARTESIAN_POINT ( 'NONE',  ( -10.18810118749999916, 0.000000000000000000, 72.15625000204836681 ) ) ;
#12608=FACE_OUTER_BOUND ( 'NONE', #15191, .T. ) ;
#12618=ORIENTED_EDGE ( 'NONE', *, *, #10652, .T. ) ;
#12639=CARTESIAN_POINT ( 'NONE',  ( 2.020667218593132706E-15, -11.00000000000000000, 69.06250000409677625 ) ) ;
#12641=CARTESIAN_POINT ( 'NONE',  ( -11.00000000000010658, 4.556349186103942017, 76.09375000409676204 ) ) ;
#12665=VERTEX_POINT ( 'NONE', #31851 ) ;
#12667=CARTESIAN_POINT ( 'NONE',  ( 4.220049686691941027, -10.18810118749999738, 101.1250000020483810 ) ) ;
#12682=CARTESIAN_POINT ( 'NONE',  ( -10.18810118749999738, -4.220049686691941915, 93.62500000204838102 ) ) ;
#12686=CYLINDRICAL_SURFACE ( 'NONE', #7061, 11.00000000000000000 ) ;
#12688=CARTESIAN_POINT ( 'NONE',  ( 7.204075437095968759, -7.204075437095966983, 80.59375000204838102 ) ) ;
#12697=CARTESIAN_POINT ( 'NONE',  ( -4.220049686691937474, -10.18810118749999738, 91.93750000204836681 ) ) ;
#12708=CARTESIAN_POINT ( 'NONE',  ( -10.18810118749999738, -4.220049686691941915, 72.62500000204836681 ) ) ;
#12718=EDGE_CURVE ( 'NONE', #13626, #21890, #72751, .T. ) ;
#12724=CARTESIAN_POINT ( 'NONE',  ( 10.18810118749999916, 1.247682550866122264E-15, 69.90625000204836681 ) ) ;
#12728=CARTESIAN_POINT ( 'NONE',  ( -6.735557395310442023E-16, 11.00000000000000000, 80.12499999999998579 ) ) ;
#12732=ORIENTED_EDGE ( 'NONE', *, *, #46613, .F. ) ;
#12752=VERTEX_POINT ( 'NONE', #15230 ) ;
#12754=CARTESIAN_POINT ( 'NONE',  ( -7.778174593052020747, -7.778174593052023411, 80.87500000409677625 ) ) ;
#12756=CARTESIAN_POINT ( 'NONE',  ( -6.735557395310442023E-16, 11.00000000000000000, 66.81250000409677625 ) ) ;
#12765=CARTESIAN_POINT ( 'NONE',  ( -7.778174593052023411, 7.778174593052023411, 108.8124999999999858 ) ) ;
#12767=CARTESIAN_POINT ( 'NONE',  ( 1.871523826299183495E-15, -10.18810118749999916, 111.9062500020483810 ) ) ;
#12771=CARTESIAN_POINT ( 'NONE',  ( 5.094040948422622783, 8.823160013426731396, 67.15552388843440212 ) ) ;
#12782=VERTEX_POINT ( 'NONE', #39374 ) ;
#12794=EDGE_LOOP ( 'NONE', ( #9915, #55277, #62764, #42201 ) ) ;
#12806=ORIENTED_EDGE ( 'NONE', *, *, #54172, .F. ) ;
#12807=CARTESIAN_POINT ( 'NONE',  ( -7.204075437095967871, 7.204075437095967871, 88.46875000204838102 ) ) ;
#12809=CARTESIAN_POINT ( 'NONE',  ( -4.556349186104045934, 11.00000000000000000, 104.2187500000000000 ) ) ;
#12810=CARTESIAN_POINT ( 'NONE',  ( -4.556349186104048599, -10.99999999999999822, 104.7812499999999858 ) ) ;
#12815=DIRECTION ( 'NONE',  ( -0.4999978731667203413, -0.8660266317087230714, 0.000000000000000000 ) ) ;
#12831=CARTESIAN_POINT ( 'NONE',  ( 11.00000000000000000, 1.347111479062088405E-15, 99.24999999999998579 ) ) ;
#12835=CARTESIAN_POINT ( 'NONE',  ( 4.556349186104051263, -10.99999999999999822, 87.15625000409677625 ) ) ;
#12837=CARTESIAN_POINT ( 'NONE',  ( 4.556349186104052151, -10.99999999999999822, 111.1562500040967620 ) ) ;
#12858=CARTESIAN_POINT ( 'NONE',  ( 7.204075437095968759, -7.204075437095966983, 91.09375000204838102 ) ) ;
#12867=CARTESIAN_POINT ( 'NONE',  ( 4.220049686691934809, 10.18810118749999916, 98.68750000204838102 ) ) ;
#12875=EDGE_CURVE ( 'NONE', #36860, #15625, #64594, .T. ) ;
#12876=CARTESIAN_POINT ( 'NONE',  ( 10.18810118750000093, -4.220049686691933921, 106.1875000020483810 ) ) ;
#12882=CARTESIAN_POINT ( 'NONE',  ( 7.778174593052023411, -7.778174593052021635, 81.06249999999998579 ) ) ;
#12889=CARTESIAN_POINT ( 'NONE',  ( 2.947433605447500327, 11.00000000000000000, 68.06435453820057546 ) ) ;
#12893=CARTESIAN_POINT ( 'NONE',  ( -4.220049686691937474, -10.18810118749999738, 105.4375000020483810 ) ) ;
#12911=CARTESIAN_POINT ( 'NONE',  ( -10.18810118749999916, 0.000000000000000000, 68.03125000204838102 ) ) ;
#12922=CARTESIAN_POINT ( 'NONE',  ( -4.556349186104045934, 11.00000000000000000, 105.9062500040967763 ) ) ;
#12926=CARTESIAN_POINT ( 'NONE',  ( 4.556349186104045934, 11.00000000000000000, 71.21875000409676204 ) ) ;
#12927=DIRECTION ( 'NONE',  ( -0.000000000000000000, -0.000000000000000000, -1.000000000000000000 ) ) ;
#12928=DIRECTION ( 'NONE',  ( -0.000000000000000000, -0.000000000000000000, -1.000000000000000000 ) ) ;
#12942=CARTESIAN_POINT ( 'NONE',  ( 1.871523826299183495E-15, -10.18810118749999916, 86.03125000204836681 ) ) ;
#12946=CARTESIAN_POINT ( 'NONE',  ( -4.220049686691937474, -10.18810118749999738, 107.3125000020483668 ) ) ;
#12952=CARTESIAN_POINT ( 'NONE',  ( -7.204075437095967871, 7.204075437095967871, 70.84375000204836681 ) ) ;
#12966=CARTESIAN_POINT ( 'NONE',  ( -7.204075437095967871, 7.204075437095967871, 68.96875000204836681 ) ) ;
#12968=CARTESIAN_POINT ( 'NONE',  ( 11.00000000000000000, 1.347111479062088405E-15, 85.93750000409677625 ) ) ;
#13002=CARTESIAN_POINT ( 'NONE',  ( 4.556349186104052151, -10.99999999999999822, 69.15625000409676204 ) ) ;
#13031=CARTESIAN_POINT ( 'NONE',  ( -7.204075437095965206, -7.204075437095968759, 102.3437500020483668 ) ) ;
#13039=VERTEX_POINT ( 'NONE', #51429 ) ;
#13045=CARTESIAN_POINT ( 'NONE',  ( -7.204075437095967871, 7.204075437095967871, 94.84375000204838102 ) ) ;
#13048=DIRECTION ( 'NONE',  ( 0.000000000000000000, 0.000000000000000000, 1.000000000000000000 ) ) ;
#13049=DIRECTION ( 'NONE',  ( -1.000000000000000000, 0.000000000000000000, 0.000000000000000000 ) ) ;
#13051=CARTESIAN_POINT ( 'NONE',  ( -4.220049686691935698, 10.18810118749999916, 72.25000000204836681 ) ) ;
#13059=CARTESIAN_POINT ( 'NONE',  ( 4.220049686691941027, -10.18810118749999738, 90.62500000204836681 ) ) ;
#13066=AXIS2_PLACEMENT_3D ( 'NONE', #46699, #40305, #69348 ) ;
#13070=VECTOR ( 'NONE', #50223, 1000.000000000000000 ) ;
#13072=CARTESIAN_POINT ( 'NONE',  ( -6.238412754330611322E-16, 10.18810118749999916, 73.65625000204836681 ) ) ;
#13087=ORIENTED_EDGE ( 'NONE', *, *, #18005, .T. ) ;
#13088=CARTESIAN_POINT ( 'NONE',  ( -7.204075437095965206, -7.204075437095968759, 70.84375000204836681 ) ) ;
#13091=CARTESIAN_POINT ( 'NONE',  ( 2.020667218593132706E-15, -11.00000000000000000, 79.37499999999998579 ) ) ;
#13117=VECTOR ( 'NONE', #14254, 1000.000000000000000 ) ;
#13118=CARTESIAN_POINT ( 'NONE',  ( -11.00000000000000000, 4.556349186104045934, 67.09375000409677625 ) ) ;
#13130=EDGE_CURVE ( 'NONE', #30828, #47406, #24046, .T. ) ;
#13131=CARTESIAN_POINT ( 'NONE',  ( -10.18810118749999738, -4.220049686691941915, 111.6250000020483810 ) ) ;
#13144=EDGE_CURVE ( 'NONE', #40937, #8912, #43440, .T. ) ;
#13170=CARTESIAN_POINT ( 'NONE',  ( 10.18810118750000093, -4.220049686691933033, 89.31250000204838102 ) ) ;
#13172=CARTESIAN_POINT ( 'NONE',  ( -11.00000000000000000, 4.556349186104045934, 93.90625000000000000 ) ) ;
#13201=CARTESIAN_POINT ( 'NONE',  ( 11.00000000000000000, 1.347111479062088405E-15, 88.93750000409677625 ) ) ;
#13210=VECTOR ( 'NONE', #26932, 1000.000000000000000 ) ;
#13225=CARTESIAN_POINT ( 'NONE',  ( -4.556349186104045934, 11.00000000000000000, 90.90625000409677625 ) ) ;
#13228=CARTESIAN_POINT ( 'NONE',  ( 10.18810118749999916, 1.247682550866122264E-15, 94.28125000204836681 ) ) ;
#13229=ORIENTED_EDGE ( 'NONE', *, *, #22758, .F. ) ;
#13234=( BOUNDED_CURVE ( )  B_SPLINE_CURVE ( 2, ( #50091, #26317, #56139, #38785, #32380, #38037, #44065, #62153, #15374 ),
 .UNSPECIFIED., .F., .F. ) 
 B_SPLINE_CURVE_WITH_KNOTS ( ( 3, 2, 2, 2, 3 ),
 ( 0.8676470588235294379, 0.8713235294117647189, 0.8750000000000000000, 0.8786764705882352811, 0.8823529411764705621 ),
 .UNSPECIFIED. ) 
 CURVE ( )  GEOMETRIC_REPRESENTATION_ITEM ( )  RATIONAL_B_SPLINE_CURVE ( ( 1.000000000000000000, 0.9238795325112867385, 1.000000000000000000, 0.9238795325112867385, 1.000000000000000000, 0.9238795325112867385, 1.000000000000000000, 0.9238795325112867385, 1.000000000000000000 ) ) 
 REPRESENTATION_ITEM ( '' )  );
#13236=CARTESIAN_POINT ( 'NONE',  ( 10.18810118750000093, -4.220049686691933921, 102.8125000020483952 ) ) ;
#13245=CARTESIAN_POINT ( 'NONE',  ( -10.18810118749999916, 0.000000000000000000, 95.03125000204836681 ) ) ;
#13250=EDGE_LOOP ( 'NONE', ( #15524, #43299, #93, #17711 ) ) ;
#13259=ORIENTED_EDGE ( 'NONE', *, *, #44836, .F. ) ;
#13260=CARTESIAN_POINT ( 'NONE',  ( 7.204075437095966983, 7.204075437095967871, 103.0937500020483668 ) ) ;
#13261=CARTESIAN_POINT ( 'NONE',  ( -4.556349186104048599, -10.99999999999999822, 103.2812499999999858 ) ) ;
#13275=CARTESIAN_POINT ( 'NONE',  ( 2.020667218593132706E-15, -11.00000000000000000, 112.3749999999999858 ) ) ;
#13279=DIRECTION ( 'NONE',  ( -1.000000000000000000, 0.000000000000000000, 0.000000000000000000 ) ) ;
#13287=CARTESIAN_POINT ( 'NONE',  ( 4.556349186104051263, -10.99999999999999822, 106.6562500040967905 ) ) ;
#13291=CARTESIAN_POINT ( 'NONE',  ( -11.00000000000000000, 4.556349186104045934, 71.59375000409676204 ) ) ;
#13311=CARTESIAN_POINT ( 'NONE',  ( 10.18810118749999916, 4.220049686691935698, 110.8750000020483810 ) ) ;
#13314=CARTESIAN_POINT ( 'NONE',  ( 2.020667218593132706E-15, -11.00000000000000000, 109.5625000040967763 ) ) ;
#13318=CARTESIAN_POINT ( 'NONE',  ( -4.220049686691935698, 10.18810118749999916, 72.25000000204836681 ) ) ;
#13320=VERTEX_POINT ( 'NONE', #44578 ) ;
#13331=CARTESIAN_POINT ( 'NONE',  ( -4.220049686691935698, 10.18810118749999916, 67.37500000204838102 ) ) ;
#13362=CARTESIAN_POINT ( 'NONE',  ( -6.735557395310442023E-16, 11.00000000000000000, 116.3125000040967763 ) ) ;
#13365=CARTESIAN_POINT ( 'NONE',  ( 4.556349186104052151, -10.99999999999999822, 89.96875000000000000 ) ) ;
#13373=ORIENTED_EDGE ( 'NONE', *, *, #39301, .F. ) ;
#13385=CARTESIAN_POINT ( 'NONE',  ( -11.00000000000000000, 0.000000000000000000, 94.18750000409677625 ) ) ;
#13387=CARTESIAN_POINT ( 'NONE',  ( 7.778174593052021635, 7.778174593052023411, 101.1250000040967763 ) ) ;
#13391=VECTOR ( 'NONE', #26464, 1000.000000000000000 ) ;
#13397=CARTESIAN_POINT ( 'NONE',  ( -4.220049686691937474, -10.18810118749999738, 97.93750000204836681 ) ) ;
#13413=CARTESIAN_POINT ( 'NONE',  ( 4.220049686691934809, 10.18810118749999916, 88.56250000204838102 ) ) ;
#13419=CARTESIAN_POINT ( 'NONE',  ( 10.18810118749999916, 4.220049686691935698, 76.37500000204838102 ) ) ;
#13426=CARTESIAN_POINT ( 'NONE',  ( 10.18810118750000093, -4.220049686691933921, 83.31250000204836681 ) ) ;
#13438=( BOUNDED_CURVE ( )  B_SPLINE_CURVE ( 2, ( #71115, #7763, #37172, #53420, #64733, #65465, #47372, #54162, #2472 ),
 .UNSPECIFIED., .F., .F. ) 
 B_SPLINE_CURVE_WITH_KNOTS ( ( 3, 2, 2, 2, 3 ),
 ( 0.5882352941176468564, 0.5919117647058821374, 0.5955882352941175295, 0.5992647058823528106, 0.6029411764705880916 ),
 .UNSPECIFIED. ) 
 CURVE ( )  GEOMETRIC_REPRESENTATION_ITEM ( )  RATIONAL_B_SPLINE_CURVE ( ( 1.000000000000004663, 0.9238795325112821866, 1.000000000000000000, 0.9238795325112867385, 1.000000000000000000, 0.9238795325112867385, 1.000000000000000000, 0.9238795325112890700, 0.9999999999999976685 ) ) 
 REPRESENTATION_ITEM ( '' )  );
#13457=CARTESIAN_POINT ( 'NONE',  ( -10.99999999999999822, -4.556349186104052151, 74.59374999999998579 ) ) ;
#13469=CARTESIAN_POINT ( 'NONE',  ( -4.556349186104045934, 11.00000000000000000, 116.4062500040967905 ) ) ;
#13472=CARTESIAN_POINT ( 'NONE',  ( 11.00000000000000000, 1.347111479062088405E-15, 118.0000000000000000 ) ) ;
#13479=CARTESIAN_POINT ( 'NONE',  ( -15.99999999999999645, -16.00000000000000355, 20.00000000000000000 ) ) ;
#13485=CARTESIAN_POINT ( 'NONE',  ( -4.220049686691935698, 10.18810118749999916, 85.75000000204838102 ) ) ;
#13486=CARTESIAN_POINT ( 'NONE',  ( -11.00000000000000000, 4.556349186104045934, 70.09375000409676204 ) ) ;
#13498=CARTESIAN_POINT ( 'NONE',  ( -10.18810118749999916, 4.220049686691934809, 106.9375000020483810 ) ) ;
#13513=VECTOR ( 'NONE', #48023, 1000.000000000000000 ) ;
#13533=CARTESIAN_POINT ( 'NONE',  ( 7.204075437095966983, 7.204075437095967871, 80.59375000204838102 ) ) ;
#13535=CARTESIAN_POINT ( 'NONE',  ( 7.778174593052021635, 7.778174593052023411, 97.93749999999998579 ) ) ;
#13540=CARTESIAN_POINT ( 'NONE',  ( 11.00000000000000000, 1.347111479062088405E-15, 105.4375000040967763 ) ) ;
#13568=CARTESIAN_POINT ( 'NONE',  ( 4.556349186104045934, 11.00000000000000000, 84.71875000409676204 ) ) ;
#13588=CARTESIAN_POINT ( 'NONE',  ( 7.778174593052023411, -7.778174593052021635, 100.5625000000000000 ) ) ;
#13595=CARTESIAN_POINT ( 'NONE',  ( 10.18810118750000093, -4.220049686691933921, 89.68750000204836681 ) ) ;
#13597=EDGE_CURVE ( 'NONE', #7250, #62397, #21620, .T. ) ;
#13601=CARTESIAN_POINT ( 'NONE',  ( -4.220049686691937474, -10.18810118749999738, 99.43750000204836681 ) ) ;
#13609=CARTESIAN_POINT ( 'NONE',  ( -4.220049686691937474, -10.18810118749999738, 98.31250000204836681 ) ) ;
#13613=ORIENTED_EDGE ( 'NONE', *, *, #15324, .F. ) ;
#13626=VERTEX_POINT ( 'NONE', #43637 ) ;
#13627=CARTESIAN_POINT ( 'NONE',  ( -6.238412754330611322E-16, 10.18810118749999916, 104.7812500020483810 ) ) ;
#13637=CARTESIAN_POINT ( 'NONE',  ( -7.778174593052020747, -7.778174593052023411, 109.1875000000000000 ) ) ;
#13644=CARTESIAN_POINT ( 'NONE',  ( 11.00000000000000355, -4.556349186104045046, 115.6562500000000000 ) ) ;
#13655=CARTESIAN_POINT ( 'NONE',  ( -4.556349186104047710, -10.99999999999999822, 103.4687500040967763 ) ) ;
#13660=CARTESIAN_POINT ( 'NONE',  ( 0.000000000000000000, 0.000000000000000000, 118.0000000000000000 ) ) ;
#13666=FACE_OUTER_BOUND ( 'NONE', #71341, .T. ) ;
#13667=CARTESIAN_POINT ( 'NONE',  ( 4.556349186104052151, -10.99999999999999822, 67.65625000409677625 ) ) ;
#13669=VERTEX_POINT ( 'NONE', #28149 ) ;
#13672=DIRECTION ( 'NONE',  ( -0.000000000000000000, -0.000000000000000000, -1.000000000000000000 ) ) ;
#13677=CARTESIAN_POINT ( 'NONE',  ( 10.18810118749999916, 1.247682550866122264E-15, 112.2812500020483810 ) ) ;
#13678=ORIENTED_EDGE ( 'NONE', *, *, #18839, .T. ) ;
#13683=CARTESIAN_POINT ( 'NONE',  ( -4.220049686691937474, -10.18810118749999738, 69.81250000204835260 ) ) ;
#13695=CARTESIAN_POINT ( 'NONE',  ( 4.220049686691941027, -10.18810118749999738, 115.0000000020483668 ) ) ;
#13723=CARTESIAN_POINT ( 'NONE',  ( 10.99999999999995026, -4.556349186104096560, 94.65625000000001421 ) ) ;
#13738=CYLINDRICAL_SURFACE ( 'NONE', #2195, 11.00000000000000000 ) ;
#13745=AXIS2_PLACEMENT_3D ( 'NONE', #8721, #71704, #31734 ) ;
#13758=CARTESIAN_POINT ( 'NONE',  ( -6.238412754330611322E-16, 10.18810118749999916, 95.78125000204836681 ) ) ;
#13773=CARTESIAN_POINT ( 'NONE',  ( 10.18810118750000093, -4.220049686691933033, 88.18750000204838102 ) ) ;
#13778=CARTESIAN_POINT ( 'NONE',  ( -4.556349186104048599, -10.99999999999999822, 101.9687500040967620 ) ) ;
#13779=CARTESIAN_POINT ( 'NONE',  ( 1.871523826299183495E-15, -10.18810118749999916, 75.90625000204836681 ) ) ;
#13789=CARTESIAN_POINT ( 'NONE',  ( -6.238412754330611322E-16, 10.18810118749999916, 85.28125000204836681 ) ) ;
#13801=CARTESIAN_POINT ( 'NONE',  ( 7.204075437095968759, -7.204075437095966983, 70.09375000204836681 ) ) ;
#13821=CARTESIAN_POINT ( 'NONE',  ( 2.020667218593132706E-15, -11.00000000000000000, 77.87499999999998579 ) ) ;
#13846=CARTESIAN_POINT ( 'NONE',  ( -10.18810118749999916, 0.000000000000000000, 87.53125000204836681 ) ) ;
#13847=CARTESIAN_POINT ( 'NONE',  ( 7.204075437095968759, -7.204075437095966983, 111.7187500020483810 ) ) ;
#13852=AXIS2_PLACEMENT_3D ( 'NONE', #24154, #1175, #19601 ) ;
#13859=DIRECTION ( 'NONE',  ( -0.000000000000000000, -0.000000000000000000, -1.000000000000000000 ) ) ;
#13861=CARTESIAN_POINT ( 'NONE',  ( 10.18810118750000093, -4.220049686691933033, 107.6875000020483810 ) ) ;
#13877=EDGE_LOOP ( 'NONE', ( #10129, #54297, #18570, #59323 ) ) ;
#13898=VECTOR ( 'NONE', #48793, 1000.000000000000000 ) ;
#13902=CARTESIAN_POINT ( 'NONE',  ( 4.220049686691941027, -10.18810118749999738, 78.62500000204838102 ) ) ;
#13905=CARTESIAN_POINT ( 'NONE',  ( -6.735557395310442023E-16, 11.00000000000000000, 93.62499999999998579 ) ) ;
#13932=CARTESIAN_POINT ( 'NONE',  ( 11.00000000000000355, -4.556349186104045046, 78.34375000409677625 ) ) ;
#13946=ORIENTED_EDGE ( 'NONE', *, *, #5862, .T. ) ;
#13948=LINE ( 'NONE', #3408, #71491 ) ;
#13957=CARTESIAN_POINT ( 'NONE',  ( -7.204075437095965206, -7.204075437095968759, 86.21875000204836681 ) ) ;
#13962=CARTESIAN_POINT ( 'NONE',  ( -7.204075437095965206, -7.204075437095968759, 100.8437500020483668 ) ) ;
#13971=CARTESIAN_POINT ( 'NONE',  ( 7.204075437095968759, -7.204075437095966983, 97.09375000204836681 ) ) ;
#13989=CARTESIAN_POINT ( 'NONE',  ( -10.18810118749999916, 0.000000000000000000, 96.15625000204838102 ) ) ;
#13996=EDGE_CURVE ( 'NONE', #58474, #26634, #51149, .T. ) ;
#14011=CARTESIAN_POINT ( 'NONE',  ( 7.778174593052023411, -7.778174593052021635, 114.0625000000000000 ) ) ;
#14023=CARTESIAN_POINT ( 'NONE',  ( -7.778174593052023411, 7.778174593052023411, 103.0000000040967763 ) ) ;
#14037=CARTESIAN_POINT ( 'NONE',  ( -11.00000000000000000, 0.000000000000000000, 67.18750000409676204 ) ) ;
#14042=CARTESIAN_POINT ( 'NONE',  ( 0.000000000000000000, 0.000000000000000000, 118.0000000000000000 ) ) ;
#14048=CARTESIAN_POINT ( 'NONE',  ( -10.18810118749999738, -4.220049686691941915, 108.6250000020483668 ) ) ;
#14055=CARTESIAN_POINT ( 'NONE',  ( -6.238412754330611322E-16, 10.18810118749999916, 70.65625000204836681 ) ) ;
#14069=CARTESIAN_POINT ( 'NONE',  ( 10.18810118749999916, 4.220049686691935698, 116.8750000020483668 ) ) ;
#14073=ORIENTED_EDGE ( 'NONE', *, *, #26003, .T. ) ;
#14094=CARTESIAN_POINT ( 'NONE',  ( -11.00000000000000000, 0.000000000000000000, 101.5000000000000000 ) ) ;
#14097=DIRECTION ( 'NONE',  ( -0.000000000000000000, -0.000000000000000000, -1.000000000000000000 ) ) ;
#14104=( BOUNDED_CURVE ( )  B_SPLINE_CURVE ( 2, ( #38989, #41216, #52907, #6883, #46125, #13261, #873, #69143, #35200 ),
 .UNSPECIFIED., .F., .F. ) 
 B_SPLINE_CURVE_WITH_KNOTS ( ( 3, 2, 2, 2, 3 ),
 ( 0.2794117647058823040, 0.2830882352941175850, 0.2867647058823528661, 0.2904411764705882026, 0.2941176470588234837 ),
 .UNSPECIFIED. ) 
 CURVE ( )  GEOMETRIC_REPRESENTATION_ITEM ( )  RATIONAL_B_SPLINE_CURVE ( ( 1.000000000000001110, 0.9238795325112856283, 1.000000000000000000, 0.9238795325112867385, 1.000000000000000000, 0.9238795325112867385, 1.000000000000000000, 0.9238795325112878487, 0.9999999999999988898 ) ) 
 REPRESENTATION_ITEM ( '' )  );
#14136=CARTESIAN_POINT ( 'NONE',  ( -4.220049686691937474, -10.18810118749999738, 93.43750000204836681 ) ) ;
#14152=CARTESIAN_POINT ( 'NONE',  ( -10.18810118749999738, -4.220049686691941915, 87.62500000204836681 ) ) ;
#14160=CARTESIAN_POINT ( 'NONE',  ( -7.204075437095965206, -7.204075437095968759, 72.71875000204838102 ) ) ;
#14167=CARTESIAN_POINT ( 'NONE',  ( -6.238412754330611322E-16, 10.18810118749999916, 82.28125000204838102 ) ) ;
#14178=CARTESIAN_POINT ( 'NONE',  ( -4.220049686691937474, -10.18810118749999738, 68.31250000204838102 ) ) ;
#14199=CARTESIAN_POINT ( 'NONE',  ( -7.778174593052020747, -7.778174593052023411, 74.68749999999998579 ) ) ;
#14224=CARTESIAN_POINT ( 'NONE',  ( -7.204075437095967871, 7.204075437095967871, 87.34375000204836681 ) ) ;
#14225=CARTESIAN_POINT ( 'NONE',  ( 7.204075437095966983, 7.204075437095967871, 112.0937500020483810 ) ) ;
#14242=CARTESIAN_POINT ( 'NONE',  ( -10.18810118749999916, 0.000000000000000000, 108.5312500020483810 ) ) ;
#14254=DIRECTION ( 'NONE',  ( -0.000000000000000000, -0.000000000000000000, -1.000000000000000000 ) ) ;
#14268=CARTESIAN_POINT ( 'NONE',  ( 7.778174593052021635, 7.778174593052023411, 72.43749999999998579 ) ) ;
#14272=ORIENTED_EDGE ( 'NONE', *, *, #15324, .T. ) ;
#14278=CARTESIAN_POINT ( 'NONE',  ( 10.18810118749999916, 4.220049686691935698, 77.50000000204839523 ) ) ;
#14281=CARTESIAN_POINT ( 'NONE',  ( -6.735557395310442023E-16, 11.00000000000000000, 98.12499999999998579 ) ) ;
#14282=CARTESIAN_POINT ( 'NONE',  ( 4.556349186104052151, -10.99999999999999822, 104.9687500000000000 ) ) ;
#14299=CARTESIAN_POINT ( 'NONE',  ( -11.00000000000000000, 0.000000000000000000, 112.1875000040967763 ) ) ;
#14311=CARTESIAN_POINT ( 'NONE',  ( -6.735557395310442023E-16, 11.00000000000000000, 78.81250000409677625 ) ) ;
#14331=CARTESIAN_POINT ( 'NONE',  ( 10.18810118750000093, -4.220049686691933921, 75.81250000204838102 ) ) ;
#14340=CARTESIAN_POINT ( 'NONE',  ( 1.871523826299183495E-15, -10.18810118749999916, 83.40625000204838102 ) ) ;
#14346=CARTESIAN_POINT ( 'NONE',  ( -10.18810118749999738, -4.220049686691941915, 103.7500000020483668 ) ) ;
#14355=CARTESIAN_POINT ( 'NONE',  ( 7.204075437095966983, 7.204075437095967871, 95.96875000204838102 ) ) ;
#14364=CARTESIAN_POINT ( 'NONE',  ( -11.00000000000000000, 0.000000000000000000, 95.68750000409677625 ) ) ;
#14369=ORIENTED_EDGE ( 'NONE', *, *, #27919, .T. ) ;
#14370=CARTESIAN_POINT ( 'NONE',  ( -7.204075437095965206, -7.204075437095968759, 96.34375000204836681 ) ) ;
#14377=EDGE_CURVE ( 'NONE', #9171, #50622, #56450, .T. ) ;
#14391=CARTESIAN_POINT ( 'NONE',  ( -10.99999999999999822, -4.556349186104052151, 115.0937500000000000 ) ) ;
#14397=CARTESIAN_POINT ( 'NONE',  ( -11.00000000000000000, 0.000000000000000000, 118.0000000000000000 ) ) ;
#14399=CARTESIAN_POINT ( 'NONE',  ( 16.00000000000000711, 16.00000000000000355, 20.00000000000000000 ) ) ;
#14404=CARTESIAN_POINT ( 'NONE',  ( -7.778174593052023411, 7.778174593052023411, 100.0000000040967763 ) ) ;
#14405=CARTESIAN_POINT ( 'NONE',  ( 2.020667218593132706E-15, -11.00000000000000000, 106.5625000040967763 ) ) ;
#14427=CARTESIAN_POINT ( 'NONE',  ( 10.18810118749999916, 1.247682550866122264E-15, 104.7812500020483810 ) ) ;
#14432=CARTESIAN_POINT ( 'NONE',  ( -10.18810118749999916, 0.000000000000000000, 71.03125000204838102 ) ) ;
#14444=( BOUNDED_CURVE ( )  B_SPLINE_CURVE ( 2, ( #6093, #29099, #18517, #12837, #23429, #46808, #18147, #41162, #17769 ),
 .UNSPECIFIED., .F., .F. ) 
 B_SPLINE_CURVE_WITH_KNOTS ( ( 3, 2, 2, 2, 3 ),
 ( 0.1029411764705882998, 0.1066176470588235947, 0.1102941176470588897, 0.1139705882352941846, 0.1176470588235294795 ),
 .UNSPECIFIED. ) 
 CURVE ( )  GEOMETRIC_REPRESENTATION_ITEM ( )  RATIONAL_B_SPLINE_CURVE ( ( 0.9999999999999985567, 0.9238795325112881818, 1.000000000000000000, 0.9238795325112867385, 1.000000000000000000, 0.9238795325112867385, 1.000000000000000000, 0.9238795325112852952, 1.000000000000001332 ) ) 
 REPRESENTATION_ITEM ( '' )  );
#14445=CARTESIAN_POINT ( 'NONE',  ( 10.18810118749999916, 1.247682550866122264E-15, 113.7812500020483810 ) ) ;
#14446=EDGE_CURVE ( 'NONE', #32492, #55577, #45788, .T. ) ;
#14460=CARTESIAN_POINT ( 'NONE',  ( -10.18810118749999738, -4.220049686691941915, 114.2500000020483952 ) ) ;
#14474=LINE ( 'NONE', #2805, #40739 ) ;
#14486=ORIENTED_EDGE ( 'NONE', *, *, #58294, .F. ) ;
#14510=CARTESIAN_POINT ( 'NONE',  ( -10.18810118749999916, 4.220049686691934809, 97.56250000204836681 ) ) ;
#14511=CARTESIAN_POINT ( 'NONE',  ( 4.556349186104045934, 11.00000000000000000, 93.53125000000000000 ) ) ;
#14524=CARTESIAN_POINT ( 'NONE',  ( -10.18810118749999916, 4.220049686691934809, 90.43750000204838102 ) ) ;
#14537=CARTESIAN_POINT ( 'NONE',  ( 4.220049686691934809, 10.18810118749999916, 82.18750000204836681 ) ) ;
#14551=( BOUNDED_SURFACE ( )  B_SPLINE_SURFACE ( 1, 2, ( 
 ( #71781, #20097, #43111, #66129, #37468, #60469, #8798, #31811, #15559, #67264, #33691, #43870, #50640, #55955, #38220, #60849, #9916, #32569, #26886, #55578, #73658, #56316, #51018, #4265, #66885, #15192, #27255, #38598, #3893, #44994, #50271, #74026, #49903, #72917, #61225, #73293, #15931, #56694, #61597, #21226, #9555, #44252, #32948, #43487, #5011, #21595, #32186, #49526, #55207, #66499, #44621, #14810, #67636, #38961, #61964, #10292, #33318, #4635, #28009, #67998, #26502, #27631, #21967, #16294, #39334, #62331, #72547, #3512, #37851, #9169, #10658, #20852, #12138, #51386, #68739, #74399, #28746, #17423, #45725, #69863, #17052, #478, #28378, #34809, #23458, #40447, #69116, #12504, #46098, #58190, #6855, #57816, #40074, #52511, #18176, #849, #6494, #63079, #41191, #5746, #35535, #46840, #22708, #29501, #23834, #11404, #34441, #46471, #6123, #57064, #29868, #29128, #57440, #16668, #63446, #11771, #52144, #51762, #39699, #11036, #109, #69491, #23087, #17801, #40815, #64201, #34068, #52882, #22329, #63822, #35175, #68370, #58551, #45356, #62699, #5377, #43017, #41916, #36270, #24564, #18910, #7964, #25664, #14346, #36638, #71319, #54366, #30600, #1934, #24922, #7230, #37376, #31718, #13236, #47937, #42282, #31336, #30233, #60377, #30967, #1214, #2296, #53986, #66039, #48681, #19638, #59286, #25294, #42653, #47570, #65664, #8704, #58922, #53252, #13962, #59646, #1580, #8326, #47205, #7594, #64926, #70237, #53622, #70954, #19271, #37005, #48311, #24193, #65296, #13601, #60008, #64570, #2676, #71688, #20008, #18546, #41552, #12867, #35903, #70593, #72453, #61507, #5574, #68935, #15468, #51212, #34257, #9460, #55485, #3798, #60758, #17246, #11594, #66792, #26798, #21135, #11229, #9080, #40268, #9829, #54740, #56887, #32857, #22911, #28573, #74222, #38129, #5202, #22526, #3419, #45547, #45923, #37759, #32094, #68564, #38506, #55115, #62896, #26033, #61129, #20761, #49054, #32476, #49812, #72828, #16866, #28199, #63268, #43778, #44158, #15095, #43396, #39891, #57259, #26406, #66410, #72062, #3048, #67173, #51579, #74598, #49434, #20380, #14720, #41018, #29693, #58019, #7423, #29328, #12697, #40640, #47031, #35729, #52708, #6689, #24752, #58383, #70425, #19099, #70065, #52337, #64759, #30431, #13059, #18742, #6324, #53450, #18001, #47763, #59114, #63643, #41751, #36098, #11972, #675, #58746, #18372, #69313, #42104, #41387, #35004, #28947, #1041, #24021, #64398, #23661, #51966, #23283, #64026, #7055, #46666, #30064, #69686, #1770, #46293, #65116, #34630, #12338, #35371, #5948, #70785, #53077, #57636, #1412, #303, #24396, #47402, #17623, #60953, #31914, #71511, #66235, #54935, #36832, #8901, #55308, #71143, #19465, #3244, #48876, #13789, #20579, #59479, #19834, #54190, #7791, #65859, #37200, #31539, #26230, #71886, #72651, #2497, #60199, #25491, #2123, #37577, #60577, #42478, #25117, #30794, #13426, #48505, #54561, #49250, #65494, #59840, #8154, #42840, #8524, #31160, #9272, #14167, #14537, #2868, #25855, #72265, #20199, #43217, #3616, #43592, #66607, #20953, #14913, #37953, #32293, #26611, #49635, #43975, #36463, #53815, #48135, #57162, #16769, #73020, #28104, #51119, #21331, #61703, #45091, #27733, #26989, #74499, #4739, #44352, #61328, #39066, #62068, #33419, #38702, #9656, #55685, #73391, #10393, #10024, #50743, #33056, #62801, #4000, #22808, #66986, #56055, #4364, #38323, #27356, #74131, #73758, #50373, #34162, #21696, #44722, #15660, #67739, #22065, #39796, #5479, #68105, #62432, #45452, #16034, #56418, #16395, #67362, #28481, #15287, #39432, #10757, #33796, #56794, #5113, #11141, #22433, #50003, #68469, #51490, #32676, #46938, #52980, #35634, #68842, #12238, #36003, #63550, #59020, #17155, #948, #69967, #40545, #57546, #18647, #57919, #70332, #40919, #34910, #5854, #23929, #45829, #63928, #11875, #52243, #12606, #30334, #69217, #17904, #212, #7329, #23191, #41290, #35276, #41655, #64299, #6227, #577, #58289, #69592, #53353, #46203, #1313, #6591, #29231, #63179, #29598, #23559, #46570, #52612, #24297, #58648, #1677, #18275, #17528, #6956, #29966, #47308, #64665, #12966, #40176, #11506, #34539, #28848, #51871, #31444, #71790, #14818, #71417, #54089, #25021, #59748, #19368, #32196, #37860, #48411, #13331, #30701, #36367, #55217 ),
 ( #47668, #43122, #24657, #8426, #54841, #66140, #19008, #14069, #7696, #8060, #53719, #48039, #70689, #31821, #54469, #31062, #2399, #48783, #42382, #2033, #60479, #60108, #42014, #65398, #25397, #43496, #71048, #13695, #2776, #25762, #59383, #65020, #37106, #36739, #37479, #19742, #42750, #49157, #65767, #20110, #14445, #8809, #3150, #26137, #72165, #20476, #66507, #60857, #9178, #21235, #68379, #49536, #33326, #27640, #72925, #15200, #51027, #15568, #28016, #73303, #67274, #38229, #56325, #3522, #21603, #44261, #9925, #45004, #62708, #26895, #50281, #32579, #39707, #55587, #73667, #44629, #74035, #21975, #38605, #32958, #67643, #27263, #16678, #3903, #10668, #15940, #61607, #20861, #38969, #55963, #4273, #61973, #33699, #16303, #11046, #10301, #49911, #4647, #50647, #68007, #39341, #5021, #62339, #34076, #56704, #22337, #45364, #26510, #72555, #43878, #66894, #61235, #9563, #17432, #51771, #64578, #47212, #6131, #45733, #63088, #68747, #12876, #118, #57073, #28758, #46480, #23096, #17810, #40826, #40456, #18555, #6864, #40083, #63455, #69128, #41200, #12147, #5385, #857, #28387, #63832, #12513, #23843, #51395, #69500, #11412, #11781, #34449, #57450, #74410, #64209, #35183, #34819, #57826, #46108, #17061, #58198, #22717, #52153, #29137, #488, #46850, #41564, #5756, #23468, #6503, #29510, #52520, #69871, #18184, #29877, #35545, #58561, #52891, #1222, #24201, #70246, #36279, #43025, #48321, #30610, #53261, #2305, #24931, #19280, #47947, #66048, #48690, #43404, #71327, #59294, #7602, #19648, #59656, #70964, #37385, #42662, #66418, #42290, #65304, #53632, #65673, #8333, #26040, #7973, #13609, #1942, #36647, #30976, #35912, #49061, #53994, #24574, #41925, #47578, #58931, #25303, #7238, #13971, #37014, #60016, #31344, #54375, #2684, #72070, #60385, #18918, #25672, #71696, #20014, #14355, #30242, #8712, #1588, #31726, #54748, #3057, #70601, #20390, #64935, #13245, #49443, #43786, #37768, #61886, #55870, #55495, #26806, #27172, #38136, #72461, #15847, #9838, #60766, #61137, #55122, #38881, #14727, #15105, #50560, #66802, #20768, #67551, #9467, #32485, #21517, #56236, #10209, #32103, #32865, #16213, #3808, #39251, #3426, #50190, #44538, #49819, #72836, #73574, #21143, #21884, #38514, #73211, #9089, #4186, #44166, #15476, #4552, #26415, #33238, #44913, #27546, #67180, #67919, #61516, #48562, #54998, #2930, #42539, #36889, #54249, #31224, #72328, #7846, #14603, #19894, #2185, #24810, #71572, #71203, #65552, #19521, #37642, #20258, #14976, #42900, #30853, #53874, #65920, #2560, #13846, #8961, #14224, #38012, #59899, #8213, #25180, #37265, #54622, #20643, #25549, #60259, #48194, #8586, #31601, #7483, #43658, #25917, #70846, #13485, #19158, #30488, #48935, #53505, #71947, #43280, #66296, #60640, #31973, #3305, #66670, #26291, #65173, #49311, #1823, #47825, #42161, #36524, #59534, #34266, #33155, #45560, #11238, #68573, #74231, #38796, #62909, #73483, #5584, #39902, #21426, #51221, #22537, #44449, #10117, #68201, #50844, #50103, #22921, #27837, #16879, #57269, #4095, #10488, #56523, #61799, #9752, #27088, #21789, #62163, #56149, #73858, #4464, #28583, #73118, #45934, #15385, #27454, #50468, #61425, #44819, #51591, #22165, #67831, #74608, #16123, #39161, #33522, #4840, #45190, #16498, #39538, #62533, #38421, #67460, #10861, #32771, #55778, #33898, #15757, #56896, #5209, #28209, #17631, #41760, #52349, #59125, #18751, #315, #30072, #53087, #23293, #63655, #47041, #29703, #28956, #1779, #6698, #1422, #36107, #57647, #64036, #35381, #40650, #63277, #5955, #685, #41027, #11981, #52719, #35013, #64769, #51976, #24764, #68947, #58027, #6335, #40277, #29338, #24406, #1052, #23669, #7436, #46675, #69698, #18012, #12347, #24030, #13072, #30442, #70076, #64408, #47412, #58392, #18383, #41396, #46304, #53461, #17257, #12708, #35738, #58755, #70436, #69322, #11604, #7066, #34640, #49920, #55596, #15951, #21612, #67280, #31174, #26904, #15576, #71155, #44268, #38977, #30805, #53827, #38617, #9571, #48146, #55971, #19111, #54199, #13801, #42116, #25502, #71521, #65869, #61619, #32590, #33335, #36845, #19845, #59852, #36474, #72934, #21244, #2137, #59490, #65128, #47774, #8165, #14178, #9935, #25128, #19476, #42489, #2508, #42852, #65505, #44638, #48515 ) ),
 .UNSPECIFIED., .F., .F., .T. ) 
 B_SPLINE_SURFACE_WITH_KNOTS ( ( 2, 2 ),
 ( 3, 2, 2, 2, 2, 2, 2, 2, 2, 2, 2, 2, 2, 2, 2, 2, 2, 2, 2, 2, 2, 2, 2, 2, 2, 2, 2, 2, 2, 2, 2, 2, 2, 2, 2, 2, 2, 2, 2, 2, 2, 2, 2, 2, 2, 2, 2, 2, 2, 2, 2, 2, 2, 2, 2, 2, 2, 2, 2, 2, 2, 2, 2, 2, 2, 2, 2, 2, 2, 2, 2, 2, 2, 2, 2, 2, 2, 2, 2, 2, 2, 2, 2, 2, 2, 2, 2, 2, 2, 2, 2, 2, 2, 2, 2, 2, 2, 2, 2, 2, 2, 2, 2, 2, 2, 2, 2, 2, 2, 2, 2, 2, 2, 2, 2, 2, 2, 2, 2, 2, 2, 2, 2, 2, 2, 2, 2, 2, 2, 2, 2, 2, 2, 2, 2, 2, 2, 2, 2, 2, 2, 2, 2, 2, 2, 2, 2, 2, 2, 2, 2, 2, 2, 2, 2, 2, 2, 2, 2, 2, 2, 2, 2, 2, 2, 2, 2, 2, 2, 2, 2, 2, 2, 2, 2, 2, 2, 2, 2, 2, 2, 2, 2, 2, 2, 2, 2, 2, 2, 2, 2, 2, 2, 2, 2, 2, 2, 2, 2, 2, 2, 2, 2, 2, 2, 2, 2, 2, 2, 2, 2, 2, 2, 2, 2, 2, 2, 2, 2, 2, 2, 2, 2, 2, 2, 2, 2, 2, 2, 2, 2, 2, 2, 2, 2, 2, 2, 2, 2, 2, 2, 2, 2, 2, 2, 2, 2, 2, 2, 2, 2, 2, 2, 2, 2, 2, 2, 2, 2, 2, 2, 2, 2, 2, 2, 2, 2, 3 ),
 ( 0.000000000000000000, 1.000000000000000000 ),
 ( 0.000000000000000000, 0.003676470588235294067, 0.007352941176470588133, 0.01102941176470588307, 0.01470588235294117627, 0.01838235294117647120, 0.02205882352941176613, 0.02573529411764705760, 0.02941176470588235253, 0.03308823529411764747, 0.03676470588235294240, 0.04044117647058823733, 0.04411764705882353227, 0.04779411764705882026, 0.05147058823529411520, 0.05514705882352941013, 0.05882352941176470507, 0.06250000000000000000, 0.06617647058823529493, 0.06985294117647058987, 0.07352941176470588480, 0.07720588235294117974, 0.08088235294117647467, 0.08455882352941176960, 0.08823529411764706454, 0.09191176470588235947, 0.09558823529411764053, 0.09926470588235293546, 0.1029411764705882304, 0.1066176470588235253, 0.1102941176470588203, 0.1139705882352941152, 0.1176470588235294101, 0.1213235294117647051, 0.1250000000000000000, 0.1286764705882352811, 0.1323529411764705899, 0.1360294117647058709, 0.1397058823529411797, 0.1433823529411764608, 0.1470588235294117696, 0.1507352941176470507, 0.1544117647058823595, 0.1580882352941176405, 0.1617647058823529493, 0.1654411764705882304, 0.1691176470588235392, 0.1727941176470588203, 0.1764705882352941291, 0.1801470588235294101, 0.1838235294117647189, 0.1875000000000000000, 0.1911764705882352811, 0.1948529411764705899, 0.1985294117647058709, 0.2022058823529411797, 0.2058823529411764608, 0.2095588235294117696, 0.2132352941176470507, 0.2169117647058823595, 0.2205882352941176405, 0.2242647058823529493, 0.2279411764705882304, 0.2316176470588235392, 0.2352941176470588203, 0.2389705882352941291, 0.2426470588235294101, 0.2463235294117647189, 0.2500000000000000000, 0.2536764705882352811, 0.2573529411764705621, 0.2610294117647058987, 0.2647058823529411797, 0.2683823529411764608, 0.2720588235294117418, 0.2757352941176470784, 0.2794117647058823595, 0.2830882352941176405, 0.2867647058823529216, 0.2904411764705882582, 0.2941176470588235392, 0.2977941176470588203, 0.3014705882352941013, 0.3051470588235294379, 0.3088235294117647189, 0.3125000000000000000, 0.3161764705882352811, 0.3198529411764705621, 0.3235294117647058987, 0.3272058823529411797, 0.3308823529411764608, 0.3345588235294117418, 0.3382352941176470784, 0.3419117647058823595, 0.3455882352941176405, 0.3492647058823529216, 0.3529411764705882582, 0.3566176470588235392, 0.3602941176470588203, 0.3639705882352941013, 0.3676470588235294379, 0.3713235294117647189, 0.3750000000000000000, 0.3786764705882352811, 0.3823529411764705621, 0.3860294117647058987, 0.3897058823529411797, 0.3933823529411764608, 0.3970588235294117418, 0.4007352941176470784, 0.4044117647058823595, 0.4080882352941176405, 0.4117647058823529216, 0.4154411764705882582, 0.4191176470588235392, 0.4227941176470588203, 0.4264705882352941013, 0.4301470588235294379, 0.4338235294117647189, 0.4375000000000000000, 0.4411764705882352811, 0.4448529411764705621, 0.4485294117647058987, 0.4522058823529411797, 0.4558823529411764608, 0.4595588235294117418, 0.4632352941176470784, 0.4669117647058823595, 0.4705882352941176405, 0.4742647058823529216, 0.4779411764705882582, 0.4816176470588235392, 0.4852941176470588203, 0.4889705882352941013, 0.4926470588235294379, 0.4963235294117647189, 0.5000000000000000000, 0.5036764705882352811, 0.5073529411764705621, 0.5110294117647058432, 0.5147058823529411242, 0.5183823529411765163, 0.5220588235294117974, 0.5257352941176470784, 0.5294117647058823595, 0.5330882352941176405, 0.5367647058823529216, 0.5404411764705882026, 0.5441176470588234837, 0.5477941176470588758, 0.5514705882352941568, 0.5551470588235294379, 0.5588235294117647189, 0.5625000000000000000, 0.5661764705882352811, 0.5698529411764705621, 0.5735294117647058432, 0.5772058823529411242, 0.5808823529411765163, 0.5845588235294117974, 0.5882352941176470784, 0.5919117647058823595, 0.5955882352941176405, 0.5992647058823529216, 0.6029411764705882026, 0.6066176470588234837, 0.6102941176470588758, 0.6139705882352941568, 0.6176470588235294379, 0.6213235294117647189, 0.6250000000000000000, 0.6286764705882352811, 0.6323529411764705621, 0.6360294117647058432, 0.6397058823529411242, 0.6433823529411765163, 0.6470588235294117974, 0.6507352941176470784, 0.6544117647058823595, 0.6580882352941176405, 0.6617647058823529216, 0.6654411764705882026, 0.6691176470588234837, 0.6727941176470588758, 0.6764705882352941568, 0.6801470588235294379, 0.6838235294117647189, 0.6875000000000000000, 0.6911764705882352811, 0.6948529411764705621, 0.6985294117647058432, 0.7022058823529411242, 0.7058823529411765163, 0.7095588235294117974, 0.7132352941176470784, 0.7169117647058823595, 0.7205882352941176405, 0.7242647058823529216, 0.7279411764705882026, 0.7316176470588234837, 0.7352941176470588758, 0.7389705882352941568, 0.7426470588235294379, 0.7463235294117647189, 0.7500000000000000000, 0.7536764705882352811, 0.7573529411764705621, 0.7610294117647058432, 0.7647058823529411242, 0.7683823529411765163, 0.7720588235294117974, 0.7757352941176470784, 0.7794117647058823595, 0.7830882352941176405, 0.7867647058823529216, 0.7904411764705882026, 0.7941176470588234837, 0.7977941176470588758, 0.8014705882352941568, 0.8051470588235294379, 0.8088235294117647189, 0.8125000000000000000, 0.8161764705882352811, 0.8198529411764705621, 0.8235294117647058432, 0.8272058823529411242, 0.8308823529411765163, 0.8345588235294117974, 0.8382352941176470784, 0.8419117647058823595, 0.8455882352941176405, 0.8492647058823529216, 0.8529411764705882026, 0.8566176470588234837, 0.8602941176470588758, 0.8639705882352941568, 0.8676470588235294379, 0.8713235294117647189, 0.8750000000000000000, 0.8786764705882352811, 0.8823529411764705621, 0.8860294117647058432, 0.8897058823529411242, 0.8933823529411765163, 0.8970588235294117974, 0.9007352941176470784, 0.9044117647058823595, 0.9080882352941176405, 0.9117647058823529216, 0.9154411764705882026, 0.9191176470588234837, 0.9227941176470588758, 0.9264705882352941568, 0.9301470588235294379, 0.9338235294117647189, 0.9375000000000000000, 0.9411764705882352811, 0.9448529411764705621, 0.9485294117647058432, 0.9522058823529411242, 0.9558823529411765163, 0.9595588235294117974, 0.9632352941176470784, 0.9669117647058823595, 0.9705882352941176405, 0.9742647058823529216, 0.9779411764705882026, 0.9803851272776890058 ),
 .UNSPECIFIED. ) 
 GEOMETRIC_REPRESENTATION_ITEM ( )  RATIONAL_B_SPLINE_SURFACE ( (
 ( 1.000000000000000000, 0.9238795325112867385, 1.000000000000000000, 0.9238795325112867385, 1.000000000000000000, 0.9238795325112867385, 1.000000000000000000, 0.9238795325112867385, 1.000000000000000000, 0.9238795325112867385, 1.000000000000000000, 0.9238795325112867385, 1.000000000000000000, 0.9238795325112867385, 1.000000000000000000, 0.9238795325112867385, 1.000000000000000000, 0.9238795325112867385, 1.000000000000000000, 0.9238795325112867385, 1.000000000000000000, 0.9238795325112867385, 1.000000000000000000, 0.9238795325112867385, 1.000000000000000000, 0.9238795325112867385, 1.000000000000000000, 0.9238795325112867385, 1.000000000000000000, 0.9238795325112867385, 1.000000000000000000, 0.9238795325112867385, 1.000000000000000000, 0.9238795325112867385, 1.000000000000000000, 0.9238795325112867385, 1.000000000000000000, 0.9238795325112867385, 1.000000000000000000, 0.9238795325112867385, 1.000000000000000000, 0.9238795325112867385, 1.000000000000000000, 0.9238795325112867385, 1.000000000000000000, 0.9238795325112867385, 1.000000000000000000, 0.9238795325112867385, 1.000000000000000000, 0.9238795325112867385, 1.000000000000000000, 0.9238795325112867385, 1.000000000000000000, 0.9238795325112867385, 1.000000000000000000, 0.9238795325112867385, 1.000000000000000000, 0.9238795325112867385, 1.000000000000000000, 0.9238795325112867385, 1.000000000000000000, 0.9238795325112867385, 1.000000000000000000, 0.9238795325112867385, 1.000000000000000000, 0.9238795325112867385, 1.000000000000000000, 0.9238795325112867385, 1.000000000000000000, 0.9238795325112867385, 1.000000000000000000, 0.9238795325112867385, 1.000000000000000000, 0.9238795325112867385, 1.000000000000000000, 0.9238795325112867385, 1.000000000000000000, 0.9238795325112867385, 1.000000000000000000, 0.9238795325112867385, 1.000000000000000000, 0.9238795325112867385, 1.000000000000000000, 0.9238795325112867385, 1.000000000000000000, 0.9238795325112867385, 1.000000000000000000, 0.9238795325112867385, 1.000000000000000000, 0.9238795325112867385, 1.000000000000000000, 0.9238795325112867385, 1.000000000000000000, 0.9238795325112867385, 1.000000000000000000, 0.9238795325112867385, 1.000000000000000000, 0.9238795325112867385, 1.000000000000000000, 0.9238795325112867385, 1.000000000000000000, 0.9238795325112867385, 1.000000000000000000, 0.9238795325112867385, 1.000000000000000000, 0.9238795325112867385, 1.000000000000000000, 0.9238795325112867385, 1.000000000000000000, 0.9238795325112867385, 1.000000000000000000, 0.9238795325112867385, 1.000000000000000000, 0.9238795325112867385, 1.000000000000000000, 0.9238795325112867385, 1.000000000000000000, 0.9238795325112867385, 1.000000000000000000, 0.9238795325112867385, 1.000000000000000000, 0.9238795325112867385, 1.000000000000000000, 0.9238795325112867385, 1.000000000000000000, 0.9238795325112867385, 1.000000000000000000, 0.9238795325112867385, 1.000000000000000000, 0.9238795325112867385, 1.000000000000000000, 0.9238795325112867385, 1.000000000000000000, 0.9238795325112867385, 1.000000000000000000, 0.9238795325112867385, 1.000000000000000000, 0.9238795325112867385, 1.000000000000000000, 0.9238795325112867385, 1.000000000000000000, 0.9238795325112867385, 1.000000000000000000, 0.9238795325112867385, 1.000000000000000000, 0.9238795325112867385, 1.000000000000000000, 0.9238795325112867385, 1.000000000000000000, 0.9238795325112867385, 1.000000000000000000, 0.9238795325112867385, 1.000000000000000000, 0.9238795325112867385, 1.000000000000000000, 0.9238795325112867385, 1.000000000000000000, 0.9238795325112867385, 1.000000000000000000, 0.9238795325112867385, 1.000000000000000000, 0.9238795325112867385, 1.000000000000000000, 0.9238795325112867385, 1.000000000000000000, 0.9238795325112867385, 1.000000000000000000, 0.9238795325112867385, 1.000000000000000000, 0.9238795325112867385, 1.000000000000000000, 0.9238795325112867385, 1.000000000000000000, 0.9238795325112867385, 1.000000000000000000, 0.9238795325112867385, 1.000000000000000000, 0.9238795325112867385, 1.000000000000000000, 0.9238795325112867385, 1.000000000000000000, 0.9238795325112867385, 1.000000000000000000, 0.9238795325112867385, 1.000000000000000000, 0.9238795325112867385, 1.000000000000000000, 0.9238795325112867385, 1.000000000000000000, 0.9238795325112867385, 1.000000000000000000, 0.9238795325112867385, 1.000000000000000000, 0.9238795325112867385, 1.000000000000000000, 0.9238795325112867385, 1.000000000000000000, 0.9238795325112867385, 1.000000000000000000, 0.9238795325112867385, 1.000000000000000000, 0.9238795325112867385, 1.000000000000000000, 0.9238795325112867385, 1.000000000000000000, 0.9238795325112867385, 1.000000000000000000, 0.9238795325112867385, 1.000000000000000000, 0.9238795325112867385, 1.000000000000000000, 0.9238795325112867385, 1.000000000000000000, 0.9238795325112867385, 1.000000000000000000, 0.9238795325112867385, 1.000000000000000000, 0.9238795325112867385, 1.000000000000000000, 0.9238795325112867385, 1.000000000000000000, 0.9238795325112867385, 1.000000000000000000, 0.9238795325112867385, 1.000000000000000000, 0.9238795325112867385, 1.000000000000000000, 0.9238795325112867385, 1.000000000000000000, 0.9238795325112867385, 1.000000000000000000, 0.9238795325112867385, 1.000000000000000000, 0.9238795325112867385, 1.000000000000000000, 0.9238795325112867385, 1.000000000000000000, 0.9238795325112867385, 1.000000000000000000, 0.9238795325112867385, 1.000000000000000000, 0.9238795325112867385, 1.000000000000000000, 0.9238795325112867385, 1.000000000000000000, 0.9238795325112867385, 1.000000000000000000, 0.9238795325112867385, 1.000000000000000000, 0.9238795325112867385, 1.000000000000000000, 0.9238795325112867385, 1.000000000000000000, 0.9238795325112867385, 1.000000000000000000, 0.9238795325112867385, 1.000000000000000000, 0.9238795325112867385, 1.000000000000000000, 0.9238795325112867385, 1.000000000000000000, 0.9238795325112867385, 1.000000000000000000, 0.9238795325112867385, 1.000000000000000000, 0.9238795325112867385, 1.000000000000000000, 0.9238795325112867385, 1.000000000000000000, 0.9238795325112867385, 1.000000000000000000, 0.9238795325112867385, 1.000000000000000000, 0.9238795325112867385, 1.000000000000000000, 0.9238795325112867385, 1.000000000000000000, 0.9238795325112867385, 1.000000000000000000, 0.9238795325112867385, 1.000000000000000000, 0.9238795325112867385, 1.000000000000000000, 0.9238795325112867385, 1.000000000000000000, 0.9238795325112867385, 1.000000000000000000, 0.9238795325112867385, 1.000000000000000000, 0.9238795325112867385, 1.000000000000000000, 0.9238795325112867385, 1.000000000000000000, 0.9238795325112867385, 1.000000000000000000, 0.9238795325112867385, 1.000000000000000000, 0.9238795325112867385, 1.000000000000000000, 0.9238795325112867385, 1.000000000000000000, 0.9238795325112867385, 1.000000000000000000, 0.9238795325112867385, 1.000000000000000000, 0.9238795325112867385, 1.000000000000000000, 0.9238795325112867385, 1.000000000000000000, 0.9238795325112867385, 1.000000000000000000, 0.9238795325112867385, 1.000000000000000000, 0.9238795325112867385, 1.000000000000000000, 0.9238795325112867385, 1.000000000000000000, 0.9238795325112867385, 1.000000000000000000, 0.9238795325112867385, 1.000000000000000000, 0.9238795325112867385, 1.000000000000000000, 0.9238795325112867385, 1.000000000000000000, 0.9238795325112867385, 1.000000000000000000, 0.9238795325112867385, 1.000000000000000000, 0.9238795325112867385, 1.000000000000000000, 0.9238795325112867385, 1.000000000000000000, 0.9238795325112867385, 1.000000000000000000, 0.9238795325112867385, 1.000000000000000000, 0.9238795325112867385, 1.000000000000000000, 0.9238795325112867385, 1.000000000000000000, 0.9238795325112867385, 1.000000000000000000, 0.9238795325112867385, 1.000000000000000000, 0.9238795325112867385, 1.000000000000000000, 0.9238795325112867385, 1.000000000000000000, 0.9238795325112867385, 1.000000000000000000, 0.9238795325112867385, 1.000000000000000000, 0.9238795325112867385, 1.000000000000000000, 0.9238795325112867385, 1.000000000000000000, 0.9238795325112867385, 1.000000000000000000, 0.9238795325112867385, 1.000000000000000000, 0.9238795325112867385, 1.000000000000000000, 0.9238795325112867385, 1.000000000000000000, 0.9238795325112867385, 1.000000000000000000, 0.9238795325112867385, 1.000000000000000000, 0.9238795325112867385, 1.000000000000000000, 0.9238795325112867385, 1.000000000000000000, 0.9238795325112867385, 1.000000000000000000, 0.9238795325112867385, 1.000000000000000000, 0.9238795325112867385, 1.000000000000000000, 0.9238795325112867385, 1.000000000000000000, 0.9238795325112867385, 1.000000000000000000, 0.9238795325112867385, 1.000000000000000000, 0.9238795325112867385, 1.000000000000000000, 0.9238795325112867385, 1.000000000000000000, 0.9238795325112867385, 1.000000000000000000, 0.9238795325112867385, 1.000000000000000000, 0.9238795325112867385, 1.000000000000000000, 0.9238795325112867385, 1.000000000000000000, 0.9238795325112867385, 1.000000000000000000, 0.9238795325112867385, 1.000000000000000000, 0.9238795325112867385, 1.000000000000000000, 0.9238795325112867385, 1.000000000000000000, 0.9238795325112867385, 1.000000000000000000, 0.9238795325112867385, 1.000000000000000000, 0.9238795325112867385, 1.000000000000000000, 0.9238795325112867385, 1.000000000000000000, 0.9238795325112867385, 1.000000000000000000, 0.9238795325112867385, 1.000000000000000000, 0.9238795325112867385, 1.000000000000000000, 0.9238795325112867385, 1.000000000000000000, 0.9238795325112867385, 1.000000000000000000, 0.9238795325112867385, 1.000000000000000000, 0.9238795325112867385, 1.000000000000000000, 0.9238795325112867385, 1.000000000000000000, 0.9238795325112867385, 1.000000000000000000, 0.9238795325112867385, 1.000000000000000000, 0.9238795325112867385, 1.000000000000000000, 0.9238795325112867385, 1.000000000000000000, 0.9238795325112867385, 1.000000000000000000, 0.9238795325112867385, 1.000000000000000000, 0.9238795325112867385, 1.000000000000000000, 0.9238795325112867385, 1.000000000000000000, 0.9238795325112867385, 1.000000000000000000, 0.9238795325112867385, 1.000000000000000000, 0.9238795325112867385, 1.000000000000000000, 0.9238795325112867385, 1.000000000000000000, 0.9238795325112867385, 1.000000000000000000, 0.9238795325112867385, 1.000000000000000000, 0.9238795325112867385, 1.000000000000000000, 0.9238795325112867385, 1.000000000000000000, 0.9238795325112867385, 1.000000000000000000, 0.9238795325112867385, 1.000000000000000000, 0.9238795325112867385, 1.000000000000000000, 0.9238795325112867385, 1.000000000000000000, 0.9238795325112867385, 1.000000000000000000, 0.9238795325112867385, 1.000000000000000000, 0.9238795325112867385, 1.000000000000000000, 0.9238795325112867385, 1.000000000000000000, 0.9238795325112867385, 1.000000000000000000, 0.9238795325112867385, 1.000000000000000000, 0.9238795325112867385, 1.000000000000000000, 0.9238795325112867385, 1.000000000000000000, 0.9238795325112867385, 1.000000000000000000, 0.9238795325112867385, 1.000000000000000000, 0.9238795325112867385, 1.000000000000000000, 0.9238795325112867385, 1.000000000000000000, 0.9238795325112867385, 1.000000000000000000, 0.9238795325112867385, 1.000000000000000000, 0.9238795325112867385, 1.000000000000000000, 0.9238795325112867385, 1.000000000000000000, 0.9238795325112867385, 1.000000000000000000, 0.9238795325112867385, 1.000000000000000000, 0.9238795325112867385, 1.000000000000000000, 0.9238795325112867385, 1.000000000000000000, 0.9238795325112867385, 1.000000000000000000, 0.9238795325112867385, 1.000000000000000000, 0.9238795325112867385, 1.000000000000000000, 0.9238795325112867385, 1.000000000000000000, 0.9238795325112867385, 1.000000000000000000, 0.9238795325112867385, 1.000000000000000000, 0.9238795325112867385, 1.000000000000000000, 0.9238795325112867385, 1.000000000000000000, 0.9238795325112867385, 1.000000000000000000, 0.9238795325112867385, 1.000000000000000000, 0.9238795325112867385, 1.000000000000000000, 0.9238795325112867385, 1.000000000000000000, 0.9493985675959865089, 0.9660722070829228514),
 ( 1.000000000000000000, 0.9238795325112867385, 1.000000000000000000, 0.9238795325112867385, 1.000000000000000000, 0.9238795325112867385, 1.000000000000000000, 0.9238795325112867385, 1.000000000000000000, 0.9238795325112867385, 1.000000000000000000, 0.9238795325112867385, 1.000000000000000000, 0.9238795325112867385, 1.000000000000000000, 0.9238795325112867385, 1.000000000000000000, 0.9238795325112867385, 1.000000000000000000, 0.9238795325112867385, 1.000000000000000000, 0.9238795325112867385, 1.000000000000000000, 0.9238795325112867385, 1.000000000000000000, 0.9238795325112867385, 1.000000000000000000, 0.9238795325112867385, 1.000000000000000000, 0.9238795325112867385, 1.000000000000000000, 0.9238795325112867385, 1.000000000000000000, 0.9238795325112867385, 1.000000000000000000, 0.9238795325112867385, 1.000000000000000000, 0.9238795325112867385, 1.000000000000000000, 0.9238795325112867385, 1.000000000000000000, 0.9238795325112867385, 1.000000000000000000, 0.9238795325112867385, 1.000000000000000000, 0.9238795325112867385, 1.000000000000000000, 0.9238795325112867385, 1.000000000000000000, 0.9238795325112867385, 1.000000000000000000, 0.9238795325112867385, 1.000000000000000000, 0.9238795325112867385, 1.000000000000000000, 0.9238795325112867385, 1.000000000000000000, 0.9238795325112867385, 1.000000000000000000, 0.9238795325112867385, 1.000000000000000000, 0.9238795325112867385, 1.000000000000000000, 0.9238795325112867385, 1.000000000000000000, 0.9238795325112867385, 1.000000000000000000, 0.9238795325112867385, 1.000000000000000000, 0.9238795325112867385, 1.000000000000000000, 0.9238795325112867385, 1.000000000000000000, 0.9238795325112867385, 1.000000000000000000, 0.9238795325112867385, 1.000000000000000000, 0.9238795325112867385, 1.000000000000000000, 0.9238795325112867385, 1.000000000000000000, 0.9238795325112867385, 1.000000000000000000, 0.9238795325112867385, 1.000000000000000000, 0.9238795325112867385, 1.000000000000000000, 0.9238795325112867385, 1.000000000000000000, 0.9238795325112867385, 1.000000000000000000, 0.9238795325112867385, 1.000000000000000000, 0.9238795325112867385, 1.000000000000000000, 0.9238795325112867385, 1.000000000000000000, 0.9238795325112867385, 1.000000000000000000, 0.9238795325112867385, 1.000000000000000000, 0.9238795325112867385, 1.000000000000000000, 0.9238795325112867385, 1.000000000000000000, 0.9238795325112867385, 1.000000000000000000, 0.9238795325112867385, 1.000000000000000000, 0.9238795325112867385, 1.000000000000000000, 0.9238795325112867385, 1.000000000000000000, 0.9238795325112867385, 1.000000000000000000, 0.9238795325112867385, 1.000000000000000000, 0.9238795325112867385, 1.000000000000000000, 0.9238795325112867385, 1.000000000000000000, 0.9238795325112867385, 1.000000000000000000, 0.9238795325112867385, 1.000000000000000000, 0.9238795325112867385, 1.000000000000000000, 0.9238795325112867385, 1.000000000000000000, 0.9238795325112867385, 1.000000000000000000, 0.9238795325112867385, 1.000000000000000000, 0.9238795325112867385, 1.000000000000000000, 0.9238795325112867385, 1.000000000000000000, 0.9238795325112867385, 1.000000000000000000, 0.9238795325112867385, 1.000000000000000000, 0.9238795325112867385, 1.000000000000000000, 0.9238795325112867385, 1.000000000000000000, 0.9238795325112867385, 1.000000000000000000, 0.9238795325112867385, 1.000000000000000000, 0.9238795325112867385, 1.000000000000000000, 0.9238795325112867385, 1.000000000000000000, 0.9238795325112867385, 1.000000000000000000, 0.9238795325112867385, 1.000000000000000000, 0.9238795325112867385, 1.000000000000000000, 0.9238795325112867385, 1.000000000000000000, 0.9238795325112867385, 1.000000000000000000, 0.9238795325112867385, 1.000000000000000000, 0.9238795325112867385, 1.000000000000000000, 0.9238795325112867385, 1.000000000000000000, 0.9238795325112867385, 1.000000000000000000, 0.9238795325112867385, 1.000000000000000000, 0.9238795325112867385, 1.000000000000000000, 0.9238795325112867385, 1.000000000000000000, 0.9238795325112867385, 1.000000000000000000, 0.9238795325112867385, 1.000000000000000000, 0.9238795325112867385, 1.000000000000000000, 0.9238795325112867385, 1.000000000000000000, 0.9238795325112867385, 1.000000000000000000, 0.9238795325112867385, 1.000000000000000000, 0.9238795325112867385, 1.000000000000000000, 0.9238795325112867385, 1.000000000000000000, 0.9238795325112867385, 1.000000000000000000, 0.9238795325112867385, 1.000000000000000000, 0.9238795325112867385, 1.000000000000000000, 0.9238795325112867385, 1.000000000000000000, 0.9238795325112867385, 1.000000000000000000, 0.9238795325112867385, 1.000000000000000000, 0.9238795325112867385, 1.000000000000000000, 0.9238795325112867385, 1.000000000000000000, 0.9238795325112867385, 1.000000000000000000, 0.9238795325112867385, 1.000000000000000000, 0.9238795325112867385, 1.000000000000000000, 0.9238795325112867385, 1.000000000000000000, 0.9238795325112867385, 1.000000000000000000, 0.9238795325112867385, 1.000000000000000000, 0.9238795325112867385, 1.000000000000000000, 0.9238795325112867385, 1.000000000000000000, 0.9238795325112867385, 1.000000000000000000, 0.9238795325112867385, 1.000000000000000000, 0.9238795325112867385, 1.000000000000000000, 0.9238795325112867385, 1.000000000000000000, 0.9238795325112867385, 1.000000000000000000, 0.9238795325112867385, 1.000000000000000000, 0.9238795325112867385, 1.000000000000000000, 0.9238795325112867385, 1.000000000000000000, 0.9238795325112867385, 1.000000000000000000, 0.9238795325112867385, 1.000000000000000000, 0.9238795325112867385, 1.000000000000000000, 0.9238795325112867385, 1.000000000000000000, 0.9238795325112867385, 1.000000000000000000, 0.9238795325112867385, 1.000000000000000000, 0.9238795325112867385, 1.000000000000000000, 0.9238795325112867385, 1.000000000000000000, 0.9238795325112867385, 1.000000000000000000, 0.9238795325112867385, 1.000000000000000000, 0.9238795325112867385, 1.000000000000000000, 0.9238795325112867385, 1.000000000000000000, 0.9238795325112867385, 1.000000000000000000, 0.9238795325112867385, 1.000000000000000000, 0.9238795325112867385, 1.000000000000000000, 0.9238795325112867385, 1.000000000000000000, 0.9238795325112867385, 1.000000000000000000, 0.9238795325112867385, 1.000000000000000000, 0.9238795325112867385, 1.000000000000000000, 0.9238795325112867385, 1.000000000000000000, 0.9238795325112867385, 1.000000000000000000, 0.9238795325112867385, 1.000000000000000000, 0.9238795325112867385, 1.000000000000000000, 0.9238795325112867385, 1.000000000000000000, 0.9238795325112867385, 1.000000000000000000, 0.9238795325112867385, 1.000000000000000000, 0.9238795325112867385, 1.000000000000000000, 0.9238795325112867385, 1.000000000000000000, 0.9238795325112867385, 1.000000000000000000, 0.9238795325112867385, 1.000000000000000000, 0.9238795325112867385, 1.000000000000000000, 0.9238795325112867385, 1.000000000000000000, 0.9238795325112867385, 1.000000000000000000, 0.9238795325112867385, 1.000000000000000000, 0.9238795325112867385, 1.000000000000000000, 0.9238795325112867385, 1.000000000000000000, 0.9238795325112867385, 1.000000000000000000, 0.9238795325112867385, 1.000000000000000000, 0.9238795325112867385, 1.000000000000000000, 0.9238795325112867385, 1.000000000000000000, 0.9238795325112867385, 1.000000000000000000, 0.9238795325112867385, 1.000000000000000000, 0.9238795325112867385, 1.000000000000000000, 0.9238795325112867385, 1.000000000000000000, 0.9238795325112867385, 1.000000000000000000, 0.9238795325112867385, 1.000000000000000000, 0.9238795325112867385, 1.000000000000000000, 0.9238795325112867385, 1.000000000000000000, 0.9238795325112867385, 1.000000000000000000, 0.9238795325112867385, 1.000000000000000000, 0.9238795325112867385, 1.000000000000000000, 0.9238795325112867385, 1.000000000000000000, 0.9238795325112867385, 1.000000000000000000, 0.9238795325112867385, 1.000000000000000000, 0.9238795325112867385, 1.000000000000000000, 0.9238795325112867385, 1.000000000000000000, 0.9238795325112867385, 1.000000000000000000, 0.9238795325112867385, 1.000000000000000000, 0.9238795325112867385, 1.000000000000000000, 0.9238795325112867385, 1.000000000000000000, 0.9238795325112867385, 1.000000000000000000, 0.9238795325112867385, 1.000000000000000000, 0.9238795325112867385, 1.000000000000000000, 0.9238795325112867385, 1.000000000000000000, 0.9238795325112867385, 1.000000000000000000, 0.9238795325112867385, 1.000000000000000000, 0.9238795325112867385, 1.000000000000000000, 0.9238795325112867385, 1.000000000000000000, 0.9238795325112867385, 1.000000000000000000, 0.9238795325112867385, 1.000000000000000000, 0.9238795325112867385, 1.000000000000000000, 0.9238795325112867385, 1.000000000000000000, 0.9238795325112867385, 1.000000000000000000, 0.9238795325112867385, 1.000000000000000000, 0.9238795325112867385, 1.000000000000000000, 0.9238795325112867385, 1.000000000000000000, 0.9238795325112867385, 1.000000000000000000, 0.9238795325112867385, 1.000000000000000000, 0.9238795325112867385, 1.000000000000000000, 0.9238795325112867385, 1.000000000000000000, 0.9238795325112867385, 1.000000000000000000, 0.9238795325112867385, 1.000000000000000000, 0.9238795325112867385, 1.000000000000000000, 0.9238795325112867385, 1.000000000000000000, 0.9238795325112867385, 1.000000000000000000, 0.9238795325112867385, 1.000000000000000000, 0.9238795325112867385, 1.000000000000000000, 0.9238795325112867385, 1.000000000000000000, 0.9238795325112867385, 1.000000000000000000, 0.9238795325112867385, 1.000000000000000000, 0.9238795325112867385, 1.000000000000000000, 0.9238795325112867385, 1.000000000000000000, 0.9238795325112867385, 1.000000000000000000, 0.9238795325112867385, 1.000000000000000000, 0.9238795325112867385, 1.000000000000000000, 0.9238795325112867385, 1.000000000000000000, 0.9238795325112867385, 1.000000000000000000, 0.9238795325112867385, 1.000000000000000000, 0.9238795325112867385, 1.000000000000000000, 0.9238795325112867385, 1.000000000000000000, 0.9238795325112867385, 1.000000000000000000, 0.9238795325112867385, 1.000000000000000000, 0.9238795325112867385, 1.000000000000000000, 0.9238795325112867385, 1.000000000000000000, 0.9238795325112867385, 1.000000000000000000, 0.9238795325112867385, 1.000000000000000000, 0.9238795325112867385, 1.000000000000000000, 0.9238795325112867385, 1.000000000000000000, 0.9238795325112867385, 1.000000000000000000, 0.9238795325112867385, 1.000000000000000000, 0.9238795325112867385, 1.000000000000000000, 0.9238795325112867385, 1.000000000000000000, 0.9238795325112867385, 1.000000000000000000, 0.9238795325112867385, 1.000000000000000000, 0.9238795325112867385, 1.000000000000000000, 0.9238795325112867385, 1.000000000000000000, 0.9238795325112867385, 1.000000000000000000, 0.9238795325112867385, 1.000000000000000000, 0.9238795325112867385, 1.000000000000000000, 0.9238795325112867385, 1.000000000000000000, 0.9238795325112867385, 1.000000000000000000, 0.9238795325112867385, 1.000000000000000000, 0.9238795325112867385, 1.000000000000000000, 0.9238795325112867385, 1.000000000000000000, 0.9238795325112867385, 1.000000000000000000, 0.9238795325112867385, 1.000000000000000000, 0.9238795325112867385, 1.000000000000000000, 0.9238795325112867385, 1.000000000000000000, 0.9238795325112867385, 1.000000000000000000, 0.9238795325112867385, 1.000000000000000000, 0.9238795325112867385, 1.000000000000000000, 0.9238795325112867385, 1.000000000000000000, 0.9238795325112867385, 1.000000000000000000, 0.9238795325112867385, 1.000000000000000000, 0.9238795325112867385, 1.000000000000000000, 0.9238795325112867385, 1.000000000000000000, 0.9238795325112867385, 1.000000000000000000, 0.9238795325112867385, 1.000000000000000000, 0.9238795325112867385, 1.000000000000000000, 0.9238795325112867385, 1.000000000000000000, 0.9238795325112867385, 1.000000000000000000, 0.9238795325112867385, 1.000000000000000000, 0.9238795325112867385, 1.000000000000000000, 0.9238795325112867385, 1.000000000000000000, 0.9238795325112867385, 1.000000000000000000, 0.9238795325112867385, 1.000000000000000000, 0.9493985675959865089, 0.9660722070829228514) ) ) 
 REPRESENTATION_ITEM ( '' )  SURFACE ( )  );
#14576=CARTESIAN_POINT ( 'NONE',  ( 7.778174593052023411, -7.778174593052021635, 70.56249999999998579 ) ) ;
#14577=AXIS2_PLACEMENT_3D ( 'NONE', #32623, #14861, #3566 ) ;
#14603=CARTESIAN_POINT ( 'NONE',  ( -10.18810118749999916, 0.000000000000000000, 89.03125000204836681 ) ) ;
#14604=CARTESIAN_POINT ( 'NONE',  ( -4.220049686691937474, -10.18810118749999738, 115.9375000020483668 ) ) ;
#14617=CARTESIAN_POINT ( 'NONE',  ( 10.18810118749999916, 1.247682550866122264E-15, 106.2812500020483810 ) ) ;
#14639=( BOUNDED_CURVE ( )  B_SPLINE_CURVE ( 2, ( #11652, #29003, #730, #57693, #47458, #359, #23712, #70121, #23341 ),
 .UNSPECIFIED., .F., .F. ) 
 B_SPLINE_CURVE_WITH_KNOTS ( ( 3, 2, 2, 2, 3 ),
 ( 0.01470588235294118667, 0.01838235294117648508, 0.02205882352941178348, 0.02573529411764707842, 0.02941176470588237335 ),
 .UNSPECIFIED. ) 
 CURVE ( )  GEOMETRIC_REPRESENTATION_ITEM ( )  RATIONAL_B_SPLINE_CURVE ( ( 0.9999999999999998890, 0.9238795325112869605, 1.000000000000000000, 0.9238795325112867385, 1.000000000000000000, 0.9238795325112867385, 1.000000000000000000, 0.9238795325112862944, 1.000000000000000444 ) ) 
 REPRESENTATION_ITEM ( '' )  );
#14654=CARTESIAN_POINT ( 'NONE',  ( -4.220049686691937474, -10.18810118749999738, 81.43750000204836681 ) ) ;
#14657=CARTESIAN_POINT ( 'NONE',  ( 11.00000000000000000, 1.347111479062088405E-15, 96.24999999999998579 ) ) ;
#14684=CARTESIAN_POINT ( 'NONE',  ( -11.00000000000010658, 4.556349186103942017, 80.59375000409677625 ) ) ;
#14686=CARTESIAN_POINT ( 'NONE',  ( -7.778174593052020747, -7.778174593052023411, 82.37500000409677625 ) ) ;
#14700=EDGE_LOOP ( 'NONE', ( #51412, #38234, #7943, #73829 ) ) ;
#14706=CARTESIAN_POINT ( 'NONE',  ( 10.18810118749999916, 1.247682550866122264E-15, 78.90625000204836681 ) ) ;
#14714=CARTESIAN_POINT ( 'NONE',  ( 4.220049686691941027, -10.18810118749999738, 85.00000000204838102 ) ) ;
#14720=CARTESIAN_POINT ( 'NONE',  ( 10.18810118749999916, 4.220049686691935698, 92.50000000204838102 ) ) ;
#14727=CARTESIAN_POINT ( 'NONE',  ( -10.18810118749999916, 4.220049686691934809, 93.43750000204836681 ) ) ;
#14729=EDGE_CURVE ( 'NONE', #46864, #24549, #51594, .T. ) ;
#14745=CARTESIAN_POINT ( 'NONE',  ( 4.220049686691941027, -10.18810118749999738, 96.62500000204838102 ) ) ;
#14764=CARTESIAN_POINT ( 'NONE',  ( -6.735557395310442023E-16, 11.00000000000000000, 111.6249999999999858 ) ) ;
#14773=DIRECTION ( 'NONE',  ( -0.000000000000000000, -0.000000000000000000, -1.000000000000000000 ) ) ;
#14777=CARTESIAN_POINT ( 'NONE',  ( 11.00000000000000000, 1.347111479062088405E-15, 100.9375000040967763 ) ) ;
#14778=CARTESIAN_POINT ( 'NONE',  ( -11.00000000000012967, -4.556349186103920701, 106.2812500040967763 ) ) ;
#14799=CARTESIAN_POINT ( 'NONE',  ( 4.556349186104052151, -10.99999999999999822, 70.65625000409676204 ) ) ;
#14800=CARTESIAN_POINT ( 'NONE',  ( 10.18810118749999916, 4.220049686691935698, 104.8750000020483668 ) ) ;
#14810=CARTESIAN_POINT ( 'NONE',  ( -4.220049686691935698, 10.18810118749999916, 112.3750000020483810 ) ) ;
#14818=CARTESIAN_POINT ( 'NONE',  ( 7.204075437095968759, -7.204075437095966983, 68.21875000204836681 ) ) ;
#14834=CARTESIAN_POINT ( 'NONE',  ( -4.220049686691937474, -10.18810118749999738, 115.9375000020483810 ) ) ;
#14835=CARTESIAN_POINT ( 'NONE',  ( 11.00000000000000000, 1.347111479062088405E-15, 84.43750000409677625 ) ) ;
#14846=LINE ( 'NONE', #4302, #42431 ) ;
#14848=FACE_OUTER_BOUND ( 'NONE', #30799, .T. ) ;
#14861=DIRECTION ( 'NONE',  ( -0.000000000000000000, -0.000000000000000000, -1.000000000000000000 ) ) ;
#14862=ORIENTED_EDGE ( 'NONE', *, *, #71991, .F. ) ;
#14875=CARTESIAN_POINT ( 'NONE',  ( 0.000000000000000000, 0.000000000000000000, 118.0000000000000000 ) ) ;
#14884=CARTESIAN_POINT ( 'NONE',  ( -4.220049686691935698, 10.18810118749999916, 94.37500000204839523 ) ) ;
#14892=( BOUNDED_CURVE ( )  B_SPLINE_CURVE ( 2, ( #59420, #12641, #70005, #30007, #42050, #2440, #25433, #36776, #6996 ),
 .UNSPECIFIED., .F., .F. ) 
 B_SPLINE_CURVE_WITH_KNOTS ( ( 3, 2, 2, 2, 3 ),
 ( 0.7941176470588233727, 0.7977941176470587648, 0.8014705882352940458, 0.8051470588235293269, 0.8088235294117646079 ),
 .UNSPECIFIED. ) 
 CURVE ( )  GEOMETRIC_REPRESENTATION_ITEM ( )  RATIONAL_B_SPLINE_CURVE ( ( 1.000000000000002220, 0.9238795325112844070, 1.000000000000000000, 0.9238795325112867385, 1.000000000000000000, 0.9238795325112867385, 1.000000000000000000, 0.9238795325112890700, 0.9999999999999976685 ) ) 
 REPRESENTATION_ITEM ( '' )  );
#14899=CARTESIAN_POINT ( 'NONE',  ( 1.871523826299183495E-15, -10.18810118749999916, 90.90625000204838102 ) ) ;
#14913=CARTESIAN_POINT ( 'NONE',  ( -10.18810118749999738, -4.220049686691941915, 81.25000000204836681 ) ) ;
#14917=EDGE_LOOP ( 'NONE', ( #58711, #1436, #44820, #39508, #10148 ) ) ;
#14939=VECTOR ( 'NONE', #62916, 1000.000000000000000 ) ;
#14948=CARTESIAN_POINT ( 'NONE',  ( -4.556349186104045934, 11.00000000000000000, 69.71875000000000000 ) ) ;
#14958=CARTESIAN_POINT ( 'NONE',  ( -4.556349186104045934, 11.00000000000000000, 114.9062500040967763 ) ) ;
#14962=DIRECTION ( 'NONE',  ( 1.577021341797097560E-16, -1.000000000000000000, 0.000000000000000000 ) ) ;
#14968=ORIENTED_EDGE ( 'NONE', *, *, #31139, .F. ) ;
#14969=CARTESIAN_POINT ( 'NONE',  ( 11.00000000000000000, 1.347111479062088405E-15, 81.24999999999998579 ) ) ;
#14976=CARTESIAN_POINT ( 'NONE',  ( 7.204075437095968759, -7.204075437095966983, 88.09375000204836681 ) ) ;
#14977=CARTESIAN_POINT ( 'NONE',  ( 4.220049686691941027, -10.18810118749999738, 116.1250000020483810 ) ) ;
#14989=CARTESIAN_POINT ( 'NONE',  ( 4.220049686691941027, -10.18810118749999738, 107.5000000020483668 ) ) ;
#14991=ORIENTED_EDGE ( 'NONE', *, *, #36552, .F. ) ;
#15013=VERTEX_POINT ( 'NONE', #68249 ) ;
#15033=CARTESIAN_POINT ( 'NONE',  ( 7.204075437095968759, -7.204075437095966983, 81.71875000204836681 ) ) ;
#15036=CARTESIAN_POINT ( 'NONE',  ( -4.556349186104047710, -10.99999999999999822, 88.28124999999998579 ) ) ;
#15060=ORIENTED_EDGE ( 'NONE', *, *, #10232, .T. ) ;
#15064=CARTESIAN_POINT ( 'NONE',  ( 11.00000000000000000, 1.347111479062088405E-15, 78.43750000409677625 ) ) ;
#15081=CARTESIAN_POINT ( 'NONE',  ( 10.18810118749999916, 4.220049686691935698, 79.00000000204838102 ) ) ;
#15083=CYLINDRICAL_SURFACE ( 'NONE', #5000, 11.00000000000000000 ) ;
#15089=CARTESIAN_POINT ( 'NONE',  ( 7.204075437095966983, 7.204075437095967871, 83.96875000204836681 ) ) ;
#15093=CARTESIAN_POINT ( 'NONE',  ( -11.00000000000010658, 4.556349186103942017, 105.9062500000000142 ) ) ;
#15095=CARTESIAN_POINT ( 'NONE',  ( 7.204075437095968759, -7.204075437095966983, 93.71875000204838102 ) ) ;
#15105=CARTESIAN_POINT ( 'NONE',  ( -7.204075437095967871, 7.204075437095967871, 93.34375000204838102 ) ) ;
#15117=( BOUNDED_CURVE ( )  B_SPLINE_CURVE ( 2, ( #4428, #45897, #27800, #56119, #22499, #67803, #50813, #28174, #68167 ),
 .UNSPECIFIED., .F., .F. ) 
 B_SPLINE_CURVE_WITH_KNOTS ( ( 3, 2, 2, 2, 3 ),
 ( 0.3970588235294117418, 0.4007352941176470784, 0.4044117647058823595, 0.4080882352941176405, 0.4117647058823529216 ),
 .UNSPECIFIED. ) 
 CURVE ( )  GEOMETRIC_REPRESENTATION_ITEM ( )  RATIONAL_B_SPLINE_CURVE ( ( 1.000000000000000000, 0.9238795325112867385, 1.000000000000000000, 0.9238795325112867385, 1.000000000000000000, 0.9238795325112867385, 1.000000000000000000, 0.9238795325112867385, 1.000000000000000000 ) ) 
 REPRESENTATION_ITEM ( '' )  );
#15121=EDGE_LOOP ( 'NONE', ( #54117, #55937, #48209, #68828, #41316 ) ) ;
#15123=CARTESIAN_POINT ( 'NONE',  ( 7.204075437095966983, 7.204075437095967871, 95.59375000204836681 ) ) ;
#15126=CARTESIAN_POINT ( 'NONE',  ( 4.556349186104045934, 11.00000000000000000, 107.0312500000000000 ) ) ;
#15134=PLANE ( 'NONE',  #65068 ) ;
#15140=LINE ( 'NONE', #44575, #13070 ) ;
#15148=DIRECTION ( 'NONE',  ( -0.000000000000000000, -0.000000000000000000, -1.000000000000000000 ) ) ;
#15156=CARTESIAN_POINT ( 'NONE',  ( -7.778174593052023411, 7.778174593052023411, 101.5000000040967763 ) ) ;
#15180=CARTESIAN_POINT ( 'NONE',  ( -7.204075437095967871, 7.204075437095967871, 102.3437500020483668 ) ) ;
#15191=EDGE_LOOP ( 'NONE', ( #13229, #20740, #18201, #13613 ) ) ;
#15192=CARTESIAN_POINT ( 'NONE',  ( 10.18810118750000093, -4.220049686691933921, 114.8125000020483668 ) ) ;
#15200=CARTESIAN_POINT ( 'NONE',  ( 10.18810118749999916, 4.220049686691935698, 112.3750000020483810 ) ) ;
#15214=CARTESIAN_POINT ( 'NONE',  ( -4.220049686691935698, 10.18810118749999916, 115.3750000020483810 ) ) ;
#15215=CARTESIAN_POINT ( 'NONE',  ( -4.556349186104048599, -10.99999999999999822, 83.96875000409677625 ) ) ;
#15227=CARTESIAN_POINT ( 'NONE',  ( 2.020667218593132706E-15, -11.00000000000000000, 77.87499999999998579 ) ) ;
#15230=CARTESIAN_POINT ( 'NONE',  ( -11.00000000000000000, 0.000000000000000000, 104.5000000000000000 ) ) ;
#15262=CARTESIAN_POINT ( 'NONE',  ( -6.238412754330611322E-16, 10.18810118749999916, 89.78125000204836681 ) ) ;
#15265=CARTESIAN_POINT ( 'NONE',  ( -11.00000000000000000, 0.000000000000000000, 72.99999999999998579 ) ) ;
#15274=CARTESIAN_POINT ( 'NONE',  ( 4.220049686691934809, 10.18810118749999916, 81.06250000204836681 ) ) ;
#15279=CARTESIAN_POINT ( 'NONE',  ( -10.99999999999978684, -4.556349186104264426, 85.28125000409679046 ) ) ;
#15282=ADVANCED_FACE ( 'NONE', ( #57317 ), #68619, .T. ) ;
#15287=CARTESIAN_POINT ( 'NONE',  ( 1.871523826299183495E-15, -10.18810118749999916, 75.53125000204836681 ) ) ;
#15291=ORIENTED_EDGE ( 'NONE', *, *, #43108, .T. ) ;
#15299=VECTOR ( 'NONE', #26542, 1000.000000000000000 ) ;
#15303=LINE ( 'NONE', #32694, #2818 ) ;
#15310=CARTESIAN_POINT ( 'NONE',  ( -11.00000000000010303, -4.556349186103947346, 92.59374999999997158 ) ) ;
#15314=CARTESIAN_POINT ( 'NONE',  ( 4.556349186104052151, -10.99999999999999822, 115.6562500040967905 ) ) ;
#15319=CARTESIAN_POINT ( 'NONE',  ( 11.00000000000000355, -4.556349186104045046, 69.15624999999998579 ) ) ;
#15324=EDGE_CURVE ( 'NONE', #26210, #17226, #59312, .T. ) ;
#15331=CARTESIAN_POINT ( 'NONE',  ( -4.556349186104045934, 11.00000000000000000, 108.9062500040967763 ) ) ;
#15350=CARTESIAN_POINT ( 'NONE',  ( 7.204075437095968759, -7.204075437095966983, 114.7187500020483810 ) ) ;
#15364=CARTESIAN_POINT ( 'NONE',  ( 7.204075437095966983, 7.204075437095967871, 103.4687500020483668 ) ) ;
#15374=CARTESIAN_POINT ( 'NONE',  ( -11.00000000000000000, 0.000000000000000000, 71.68750000409676204 ) ) ;
#15385=CARTESIAN_POINT ( 'NONE',  ( 1.871523826299183495E-15, -10.18810118749999916, 80.40625000204838102 ) ) ;
#15394=CARTESIAN_POINT ( 'NONE',  ( -10.68301270189220098, 0.000000000000000000, 117.8169872981077617 ) ) ;
#15402=CARTESIAN_POINT ( 'NONE',  ( 10.18810118749999916, 1.247682550866122264E-15, 77.40625000204836681 ) ) ;
#15404=CARTESIAN_POINT ( 'NONE',  ( -7.778174593052020747, -7.778174593052023411, 88.18749999999998579 ) ) ;
#15435=CARTESIAN_POINT ( 'NONE',  ( -7.778174593052020747, -7.778174593052023411, 77.87500000409677625 ) ) ;
#15442=CARTESIAN_POINT ( 'NONE',  ( 7.778174593052021635, 7.778174593052023411, 98.12500000409676204 ) ) ;
#15454=CARTESIAN_POINT ( 'NONE',  ( -6.238412754330611322E-16, 10.18810118749999916, 79.28125000204836681 ) ) ;
#15462=CARTESIAN_POINT ( 'NONE',  ( 7.204075437095968759, -7.204075437095966983, 83.59375000204838102 ) ) ;
#15468=CARTESIAN_POINT ( 'NONE',  ( 1.871523826299183495E-15, -10.18810118749999916, 98.03125000204838102 ) ) ;
#15476=CARTESIAN_POINT ( 'NONE',  ( -7.204075437095965206, -7.204075437095968759, 90.71875000204838102 ) ) ;
#15495=CARTESIAN_POINT ( 'NONE',  ( 10.18810118749999916, 1.247682550866122264E-15, 99.90625000204838102 ) ) ;
#15498=CARTESIAN_POINT ( 'NONE',  ( 7.778174593052021635, 7.778174593052023411, 106.9374999999999858 ) ) ;
#15519=FACE_OUTER_BOUND ( 'NONE', #59940, .T. ) ;
#15524=ORIENTED_EDGE ( 'NONE', *, *, #37103, .T. ) ;
#15527=CARTESIAN_POINT ( 'NONE',  ( 11.00000000000000000, 1.347111479062088405E-15, 96.43750000409677625 ) ) ;
#15550=CARTESIAN_POINT ( 'NONE',  ( -10.18810118749999916, 0.000000000000000000, 105.5312500020483810 ) ) ;
#15559=CARTESIAN_POINT ( 'NONE',  ( 10.18810118749999916, 1.247682550866122264E-15, 116.4062500020483810 ) ) ;
#15561=VERTEX_POINT ( 'NONE', #21383 ) ;
#15566=CARTESIAN_POINT ( 'NONE',  ( 11.00000000000013323, -4.556349186103911819, 103.8437500040967763 ) ) ;
#15568=CARTESIAN_POINT ( 'NONE',  ( 10.18810118750000093, -4.220049686691933921, 112.1875000020483810 ) ) ;
#15576=CARTESIAN_POINT ( 'NONE',  ( -7.204075437095965206, -7.204075437095968759, 71.21875000204836681 ) ) ;
#15585=CARTESIAN_POINT ( 'NONE',  ( -10.18810118749999916, 4.220049686691934809, 114.0625000020483668 ) ) ;
#15597=CARTESIAN_POINT ( 'NONE',  ( -7.778174593052023411, 7.778174593052023411, 88.00000000409677625 ) ) ;
#15615=CARTESIAN_POINT ( 'NONE',  ( -10.18810118749999916, 0.000000000000000000, 117.1562500020483810 ) ) ;
#15617=CARTESIAN_POINT ( 'NONE',  ( -4.556349186104048599, -10.99999999999999822, 79.28125000000000000 ) ) ;
#15625=VERTEX_POINT ( 'NONE', #38760 ) ;
#15626=ORIENTED_EDGE ( 'NONE', *, *, #66984, .F. ) ;
#15634=CARTESIAN_POINT ( 'NONE',  ( -10.18810118749999738, -4.220049686691941915, 91.75000000204836681 ) ) ;
#15646=CARTESIAN_POINT ( 'NONE',  ( -7.204075437095967871, 7.204075437095967871, 84.34375000204836681 ) ) ;
#15660=CARTESIAN_POINT ( 'NONE',  ( -10.18810118749999738, -4.220049686691941915, 76.75000000204838102 ) ) ;
#15688=CARTESIAN_POINT ( 'NONE',  ( -7.778174593052020747, -7.778174593052023411, 92.68749999999998579 ) ) ;
#15693=CARTESIAN_POINT ( 'NONE',  ( 10.99999999999999467, -4.556349186104053040, 115.8437500040967763 ) ) ;
#15698=CARTESIAN_POINT ( 'NONE',  ( -4.556349186104047710, -10.99999999999999822, 70.28124999999998579 ) ) ;
#15723=CARTESIAN_POINT ( 'NONE',  ( 1.871523826299183495E-15, -10.18810118749999916, 110.0312500020483668 ) ) ;
#15732=AXIS2_PLACEMENT_3D ( 'NONE', #74634, #58414, #69720 ) ;
#15738=CARTESIAN_POINT ( 'NONE',  ( -4.220049686691937474, -10.18810118749999738, 98.31250000204836681 ) ) ;
#15757=CARTESIAN_POINT ( 'NONE',  ( -4.220049686691935698, 10.18810118749999916, 78.25000000204836681 ) ) ;
#15773=ORIENTED_EDGE ( 'NONE', *, *, #52687, .F. ) ;
#15779=CARTESIAN_POINT ( 'NONE',  ( -4.220049686691937474, -10.18810118749999738, 76.93750000204838102 ) ) ;
#15782=CARTESIAN_POINT ( 'NONE',  ( 11.00000000000000000, 4.556349186104045934, 90.34375000000000000 ) ) ;
#15809=CARTESIAN_POINT ( 'NONE',  ( -11.00000000000000000, 4.556349186104045934, 73.09375000409676204 ) ) ;
#15826=CARTESIAN_POINT ( 'NONE',  ( -10.18810118749999738, -4.220049686691941915, 76.75000000204838102 ) ) ;
#15835=CARTESIAN_POINT ( 'NONE',  ( -4.220049686691935698, 10.18810118749999916, 81.25000000204836681 ) ) ;
#15838=CARTESIAN_POINT ( 'NONE',  ( 11.00000000000000000, 1.347111479062088405E-15, 96.24999999999998579 ) ) ;
#15847=CARTESIAN_POINT ( 'NONE',  ( 4.220049686691941027, -10.18810118749999738, 94.00000000204838102 ) ) ;
#15860=CARTESIAN_POINT ( 'NONE',  ( -11.00000000000000000, 0.000000000000000000, 118.0000000000000000 ) ) ;
#15861=VECTOR ( 'NONE', #64198, 1000.000000000000000 ) ;
#15866=CARTESIAN_POINT ( 'NONE',  ( 10.18810118749999916, 1.247682550866122264E-15, 90.90625000204836681 ) ) ;
#15869=CARTESIAN_POINT ( 'NONE',  ( 2.020667218593132706E-15, -11.00000000000000000, 104.8750000000000000 ) ) ;
#15884=CARTESIAN_POINT ( 'NONE',  ( 4.556349186104045934, 11.00000000000000000, 111.5312500000000142 ) ) ;
#15900=CARTESIAN_POINT ( 'NONE',  ( -7.778174593052020747, -7.778174593052023411, 97.37500000409676204 ) ) ;
#15921=CARTESIAN_POINT ( 'NONE',  ( 7.204075437095968759, -7.204075437095966983, 104.5937500020483810 ) ) ;
#15931=CARTESIAN_POINT ( 'NONE',  ( -6.238412754330611322E-16, 10.18810118749999916, 113.7812500020483810 ) ) ;
#15935=CARTESIAN_POINT ( 'NONE',  ( -11.00000000000000000, 0.000000000000000000, 95.49999999999998579 ) ) ;
#15940=CARTESIAN_POINT ( 'NONE',  ( 4.220049686691934809, 10.18810118749999916, 109.5625000020483810 ) ) ;
#15951=CARTESIAN_POINT ( 'NONE',  ( 10.18810118750000093, -4.220049686691933921, 71.68750000204836681 ) ) ;
#15954=CARTESIAN_POINT ( 'NONE',  ( 11.00000000000000000, 1.347111479062088405E-15, 72.24999999999998579 ) ) ;
#15959=CARTESIAN_POINT ( 'NONE',  ( 10.18810118749999916, 1.247682550866122264E-15, 110.4062500020483668 ) ) ;
#15984=CARTESIAN_POINT ( 'NONE',  ( 16.00000000000000711, -16.00000000000000000, 7.387219678533747391 ) ) ;
#15996=CARTESIAN_POINT ( 'NONE',  ( -11.00000000000000000, 0.000000000000000000, 118.0000000000000000 ) ) ;
#16009=CARTESIAN_POINT ( 'NONE',  ( 10.18810118750000093, -4.220049686691933921, 87.81250000204838102 ) ) ;
#16016=CARTESIAN_POINT ( 'NONE',  ( 11.00000000000000000, 1.347111479062088405E-15, 108.4375000040967763 ) ) ;
#16021=CARTESIAN_POINT ( 'NONE',  ( -10.18810118749999738, -4.220049686691941915, 83.12500000204836681 ) ) ;
#16026=LINE ( 'NONE', #61322, #21476 ) ;
#16034=CARTESIAN_POINT ( 'NONE',  ( 10.18810118749999916, 4.220049686691935698, 76.00000000204838102 ) ) ;
#16043=VERTEX_POINT ( 'NONE', #46995 ) ;
#16062=CARTESIAN_POINT ( 'NONE',  ( 7.778174593052023411, -7.778174593052021635, 115.7500000040967905 ) ) ;
#16067=CARTESIAN_POINT ( 'NONE',  ( -7.778174593052020747, -7.778174593052023411, 70.18749999999998579 ) ) ;
#16090=CARTESIAN_POINT ( 'NONE',  ( 4.220049686691941027, -10.18810118749999738, 110.1250000020483810 ) ) ;
#16104=CARTESIAN_POINT ( 'NONE',  ( -6.238412754330611322E-16, 10.18810118749999916, 103.6562500020483810 ) ) ;
#16106=ORIENTED_EDGE ( 'NONE', *, *, #32337, .F. ) ;
#16123=CARTESIAN_POINT ( 'NONE',  ( 4.220049686691934809, 10.18810118749999916, 79.56250000204836681 ) ) ;
#16137=ORIENTED_EDGE ( 'NONE', *, *, #18609, .F. ) ;
#16139=CARTESIAN_POINT ( 'NONE',  ( 1.871523826299183495E-15, -10.18810118749999916, 77.03125000204836681 ) ) ;
#16142=CARTESIAN_POINT ( 'NONE',  ( 11.00000000000000000, 1.347111479062088405E-15, 90.25000000000000000 ) ) ;
#16168=CARTESIAN_POINT ( 'NONE',  ( 4.556349186104052151, -10.99999999999999822, 81.15625000409676204 ) ) ;
#16170=CARTESIAN_POINT ( 'NONE',  ( -6.735557395310442023E-16, 11.00000000000000000, 75.81250000409677625 ) ) ;
#16189=CARTESIAN_POINT ( 'NONE',  ( 4.220049686691941027, -10.18810118749999738, 69.62500000204838102 ) ) ;
#16196=EDGE_CURVE ( 'NONE', #8706, #15013, #30444, .T. ) ;
#16197=EDGE_CURVE ( 'NONE', #69954, #29602, #54011, .T. ) ;
#16200=CARTESIAN_POINT ( 'NONE',  ( 1.871523826299183495E-15, -10.18810118749999916, 80.40625000204838102 ) ) ;
#16205=ORIENTED_EDGE ( 'NONE', *, *, #35947, .T. ) ;
#16206=ORIENTED_EDGE ( 'NONE', *, *, #18839, .F. ) ;
#16213=CARTESIAN_POINT ( 'NONE',  ( -7.204075437095965206, -7.204075437095968759, 92.21875000204838102 ) ) ;
#16224=CARTESIAN_POINT ( 'NONE',  ( -4.556349186104045934, 11.00000000000000000, 78.90625000409676204 ) ) ;
#16231=CARTESIAN_POINT ( 'NONE',  ( 4.220049686691934809, 10.18810118749999916, 94.18750000204836681 ) ) ;
#16234=CARTESIAN_POINT ( 'NONE',  ( 4.556349186104045934, 11.00000000000000000, 108.5312500000000142 ) ) ;
#16264=CARTESIAN_POINT ( 'NONE',  ( -11.00000000000000000, 4.556349186104045934, 95.59375000409677625 ) ) ;
#16283=EDGE_CURVE ( 'NONE', #60666, #55449, #66570, .T. ) ;
#16286=CARTESIAN_POINT ( 'NONE',  ( -10.18810118749999738, -4.220049686691941915, 98.12500000204836681 ) ) ;
#16289=CYLINDRICAL_SURFACE ( 'NONE', #41333, 11.00000000000000000 ) ;
#16290=CARTESIAN_POINT ( 'NONE',  ( -6.735557395310442023E-16, 11.00000000000000000, 98.12499999999998579 ) ) ;
#16294=CARTESIAN_POINT ( 'NONE',  ( -10.18810118749999738, -4.220049686691941915, 111.2500000020483952 ) ) ;
#16303=CARTESIAN_POINT ( 'NONE',  ( -4.220049686691937474, -10.18810118749999738, 108.8125000020484094 ) ) ;
#16321=CARTESIAN_POINT ( 'NONE',  ( 10.18810118750000093, -4.220049686691933033, 108.8125000020483952 ) ) ;
#16369=CARTESIAN_POINT ( 'NONE',  ( -4.220049686691937474, -10.18810118749999738, 87.43750000204838102 ) ) ;
#16373=CARTESIAN_POINT ( 'NONE',  ( 11.00000000000000000, 1.347111479062088405E-15, 112.7499999999999858 ) ) ;
#16374=CARTESIAN_POINT ( 'NONE',  ( -7.204075437095967871, 7.204075437095967871, 115.8437500020483810 ) ) ;
#16382=CARTESIAN_POINT ( 'NONE',  ( 7.204075437095966983, 7.204075437095967871, 85.46875000204836681 ) ) ;
#16387=LINE ( 'NONE', #38315, #7717 ) ;
#16395=CARTESIAN_POINT ( 'NONE',  ( 10.18810118750000093, -4.220049686691933921, 75.81250000204838102 ) ) ;
#16396=EDGE_CURVE ( 'NONE', #12752, #68202, #71405, .T. ) ;
#16424=CARTESIAN_POINT ( 'NONE',  ( -11.00000000000000000, 0.000000000000000000, 92.49999999999998579 ) ) ;
#16437=CARTESIAN_POINT ( 'NONE',  ( -6.735557395310442023E-16, 11.00000000000000000, 110.3125000040967763 ) ) ;
#16441=EDGE_CURVE ( 'NONE', #60482, #69418, #57133, .T. ) ;
#16442=CARTESIAN_POINT ( 'NONE',  ( 10.99999999999999822, 1.347111479062088405E-15, 112.9375000040967763 ) ) ;
#16462=CARTESIAN_POINT ( 'NONE',  ( -4.220049686691935698, 10.18810118749999916, 109.3750000020483810 ) ) ;
#16479=CARTESIAN_POINT ( 'NONE',  ( 4.220049686691941027, -10.18810118749999738, 103.0000000020483668 ) ) ;
#16498=CARTESIAN_POINT ( 'NONE',  ( 7.204075437095968759, -7.204075437095966983, 79.09375000204838102 ) ) ;
#16516=EDGE_LOOP ( 'NONE', ( #14991, #3416, #16205, #38811 ) ) ;
#16517=CARTESIAN_POINT ( 'NONE',  ( -10.18810118749999916, 0.000000000000000000, 73.65625000204836681 ) ) ;
#16520=CARTESIAN_POINT ( 'NONE',  ( -7.778174593052023411, 7.778174593052023411, 87.81249999999998579 ) ) ;
#16524=CARTESIAN_POINT ( 'NONE',  ( 0.000000000000000000, 0.000000000000000000, 20.00000000000000000 ) ) ;
#16525=EDGE_CURVE ( 'NONE', #24773, #50622, #64270, .T. ) ;
#16532=CARTESIAN_POINT ( 'NONE',  ( -4.556349186104048599, -10.99999999999999822, 98.96875000409676204 ) ) ;
#16539=ADVANCED_FACE ( 'NONE', ( #40890 ), #24996, .T. ) ;
#16547=CARTESIAN_POINT ( 'NONE',  ( -4.556349186104045934, 11.00000000000000000, 75.90625000409677625 ) ) ;
#16554=CARTESIAN_POINT ( 'NONE',  ( 4.556349186104045934, 11.00000000000000000, 98.21875000409679046 ) ) ;
#16565=CARTESIAN_POINT ( 'NONE',  ( -10.18810118749999738, -4.220049686691941915, 72.25000000204836681 ) ) ;
#16574=CARTESIAN_POINT ( 'NONE',  ( 4.220049686691941027, -10.18810118749999738, 77.50000000204839523 ) ) ;
#16582=ADVANCED_FACE ( 'NONE', ( #35245 ), #52581, .F. ) ;
#16595=CARTESIAN_POINT ( 'NONE',  ( -6.735557395310442023E-16, 11.00000000000000000, 78.81250000409677625 ) ) ;
#16597=ADVANCED_FACE ( 'NONE', ( #36343 ), #8031, .T. ) ;
#16603=CARTESIAN_POINT ( 'NONE',  ( 10.18810118749999916, 1.247682550866122264E-15, 93.90625000204836681 ) ) ;
#16606=CARTESIAN_POINT ( 'NONE',  ( 11.00000000000000000, 1.347111479062088405E-15, 109.7499999999999858 ) ) ;
#16609=CARTESIAN_POINT ( 'NONE',  ( -7.778174593052023411, 7.778174593052023411, 113.5000000040967763 ) ) ;
#16636=CARTESIAN_POINT ( 'NONE',  ( 11.00000000000000000, 4.556349186104045934, 95.03125000409677625 ) ) ;
#16648=CARTESIAN_POINT ( 'NONE',  ( -11.00000000000000000, 0.000000000000000000, 69.99999999999998579 ) ) ;
#16654=DIRECTION ( 'NONE',  ( 1.000000000000000000, 0.000000000000000000, 0.000000000000000000 ) ) ;
#16658=CARTESIAN_POINT ( 'NONE',  ( -7.204075437095965206, -7.204075437095968759, 95.21875000204838102 ) ) ;
#16668=CARTESIAN_POINT ( 'NONE',  ( -10.18810118749999916, 4.220049686691934809, 106.5625000020483668 ) ) ;
#16678=CARTESIAN_POINT ( 'NONE',  ( -7.204075437095967871, 7.204075437095967871, 109.8437500020483810 ) ) ;
#16683=ADVANCED_FACE ( 'NONE', ( #46913 ), #69938, .T. ) ;
#16692=CARTESIAN_POINT ( 'NONE',  ( 10.18810118749999916, 4.220049686691935698, 112.0000000020483810 ) ) ;
#16702=CARTESIAN_POINT ( 'NONE',  ( -11.00000000000000000, 0.000000000000000000, 113.4999999999999858 ) ) ;
#16721=CARTESIAN_POINT ( 'NONE',  ( 7.778174593052023411, -7.778174593052021635, 109.7500000040967763 ) ) ;
#16736=ORIENTED_EDGE ( 'NONE', *, *, #62692, .T. ) ;
#16737=CARTESIAN_POINT ( 'NONE',  ( -10.99999999999997868, 4.556349186104065474, 116.4062499999999716 ) ) ;
#16742=ORIENTED_EDGE ( 'NONE', *, *, #42007, .T. ) ;
#16744=CARTESIAN_POINT ( 'NONE',  ( 10.18810118749999916, 1.247682550866122264E-15, 87.90625000204838102 ) ) ;
#16745=LINE ( 'NONE', #17505, #48943 ) ;
#16749=CARTESIAN_POINT ( 'NONE',  ( 10.18810118749999916, 1.247682550866122264E-15, 113.7812500020483810 ) ) ;
#16757=CARTESIAN_POINT ( 'NONE',  ( 10.18810118750000093, -4.220049686691933033, 83.68750000204836681 ) ) ;
#16769=CARTESIAN_POINT ( 'NONE',  ( 10.18810118750000093, -4.220049686691933921, 80.31250000204836681 ) ) ;
#16827=EDGE_LOOP ( 'NONE', ( #54601, #6329, #57186, #5093 ) ) ;
#16837=CARTESIAN_POINT ( 'NONE',  ( -7.204075437095965206, -7.204075437095968759, 108.3437500020483810 ) ) ;
#16849=ADVANCED_FACE ( 'NONE', ( #26873 ), #55191, .T. ) ;
#16850=CYLINDRICAL_SURFACE ( 'NONE', #73798, 11.00000000000000000 ) ;
#16854=CARTESIAN_POINT ( 'NONE',  ( 4.220049686691941027, -10.18810118749999738, 98.50000000204838102 ) ) ;
#16866=CARTESIAN_POINT ( 'NONE',  ( 4.220049686691934809, 10.18810118749999916, 94.18750000204836681 ) ) ;
#16879=CARTESIAN_POINT ( 'NONE',  ( 1.871523826299183495E-15, -10.18810118749999916, 81.90625000204838102 ) ) ;
#16899=CARTESIAN_POINT ( 'NONE',  ( -6.238412754330611322E-16, 10.18810118749999916, 76.28125000204836681 ) ) ;
#16902=CARTESIAN_POINT ( 'NONE',  ( 7.778174593052023411, -7.778174593052021635, 85.56249999999998579 ) ) ;
#16929=CARTESIAN_POINT ( 'NONE',  ( 11.00000000000000000, 1.347111479062088405E-15, 79.93750000409677625 ) ) ;
#16931=CARTESIAN_POINT ( 'NONE',  ( 7.778174593052023411, -7.778174593052021635, 73.75000000409676204 ) ) ;
#16943=CARTESIAN_POINT ( 'NONE',  ( 11.00000000000013145, 4.556349186103913596, 108.3437499999999716 ) ) ;
#16948=CARTESIAN_POINT ( 'NONE',  ( -11.00000000000000533, -11.00000000000000355, 41.99999999999999289 ) ) ;
#16949=CARTESIAN_POINT ( 'NONE',  ( 4.220049686691934809, 10.18810118749999916, 71.68750000204836681 ) ) ;
#16971=EDGE_CURVE ( 'NONE', #74244, #39873, #39896, .T. ) ;
#16985=CARTESIAN_POINT ( 'NONE',  ( -7.204075437095965206, -7.204075437095968759, 90.34375000204838102 ) ) ;
#16988=CARTESIAN_POINT ( 'NONE',  ( 11.00000000000000000, 4.556349186104045934, 102.3437499999999858 ) ) ;
#17019=CARTESIAN_POINT ( 'NONE',  ( -10.99999999999999822, -4.556349186104052151, 92.78125000409679046 ) ) ;
#17043=MANIFOLD_SOLID_BREP ( 'Cut-Revolve1', #9296 ) ;
#17044=CARTESIAN_POINT ( 'NONE',  ( 10.18810118750000093, -4.220049686691933921, 97.18750000204836681 ) ) ;
#17052=CARTESIAN_POINT ( 'NONE',  ( -10.18810118749999916, 0.000000000000000000, 109.6562500020483668 ) ) ;
#17061=CARTESIAN_POINT ( 'NONE',  ( 4.220049686691941027, -10.18810118749999738, 103.0000000020483668 ) ) ;
#17077=CARTESIAN_POINT ( 'NONE',  ( 10.18810118749999916, 4.220049686691935698, 109.0000000020483810 ) ) ;
#17084=ORIENTED_EDGE ( 'NONE', *, *, #30340, .F. ) ;
#17092=CARTESIAN_POINT ( 'NONE',  ( 10.18810118749999916, 1.247682550866122264E-15, 70.28125000204838102 ) ) ;
#17102=CARTESIAN_POINT ( 'NONE',  ( -7.778174593052020747, -7.778174593052023411, 112.3750000040967763 ) ) ;
#17120=CARTESIAN_POINT ( 'NONE',  ( 11.00000000000000000, 1.347111479062088405E-15, 115.7499999999999858 ) ) ;
#17126=CARTESIAN_POINT ( 'NONE',  ( -4.220049686691937474, -10.18810118749999738, 82.93750000204838102 ) ) ;
#17132=CARTESIAN_POINT ( 'NONE',  ( -7.778174593052023411, 7.778174593052023411, 109.0000000040967763 ) ) ;
#17138=CARTESIAN_POINT ( 'NONE',  ( -10.18810118749999738, -4.220049686691941915, 77.12500000204838102 ) ) ;
#17155=CARTESIAN_POINT ( 'NONE',  ( -10.18810118749999916, 0.000000000000000000, 73.65625000204836681 ) ) ;
#17190=CARTESIAN_POINT ( 'NONE',  ( 5.499987861550172497, 9.526286449755788865, 67.99927393035380874 ) ) ;
#17196=FACE_OUTER_BOUND ( 'NONE', #43042, .T. ) ;
#17218=CARTESIAN_POINT ( 'NONE',  ( 4.220049686691934809, 10.18810118749999916, 107.6875000020483810 ) ) ;
#17226=VERTEX_POINT ( 'NONE', #43007 ) ;
#17233=CARTESIAN_POINT ( 'NONE',  ( 10.18810118750000093, -4.220049686691933033, 92.68750000204838102 ) ) ;
#17246=CARTESIAN_POINT ( 'NONE',  ( -4.220049686691935698, 10.18810118749999916, 97.37500000204839523 ) ) ;
#17249=VERTEX_POINT ( 'NONE', #43385 ) ;
#17257=CARTESIAN_POINT ( 'NONE',  ( -7.204075437095965206, -7.204075437095968759, 72.71875000204838102 ) ) ;
#17262=CARTESIAN_POINT ( 'NONE',  ( 7.778174593052023411, -7.778174593052021635, 112.5625000000000000 ) ) ;
#17277=CARTESIAN_POINT ( 'NONE',  ( -7.204075437095967871, 7.204075437095967871, 67.46875000204836681 ) ) ;
#17280=CARTESIAN_POINT ( 'NONE',  ( -11.00000000000000000, 0.000000000000000000, 80.49999999999998579 ) ) ;
#17285=CARTESIAN_POINT ( 'NONE',  ( 5.499987861550171608, 9.526286449755788865, 67.99927393035380874 ) ) ;
#17286=DIRECTION ( 'NONE',  ( -1.000000000000000000, 0.000000000000000000, 0.000000000000000000 ) ) ;
#17305=CARTESIAN_POINT ( 'NONE',  ( -10.99999999999999822, -4.556349186104052151, 71.78125000409679046 ) ) ;
#17321=CARTESIAN_POINT ( 'NONE',  ( 7.204075437095966983, 7.204075437095967871, 73.09375000204838102 ) ) ;
#17358=ADVANCED_FACE ( 'NONE', ( #71402 ), #31049, .T. ) ;
#17360=CARTESIAN_POINT ( 'NONE',  ( -7.204075437095967871, 7.204075437095967871, 92.96875000204838102 ) ) ;
#17361=CARTESIAN_POINT ( 'NONE',  ( -4.556349186104045934, 11.00000000000000000, 92.21874999999998579 ) ) ;
#17363=CARTESIAN_POINT ( 'NONE',  ( 7.778174593052023411, -7.778174593052021635, 103.5624999999999858 ) ) ;
#17392=CARTESIAN_POINT ( 'NONE',  ( 11.00000000000000355, -4.556349186104045046, 94.84375000409679046 ) ) ;
#17416=CARTESIAN_POINT ( 'NONE',  ( 7.204075437095966983, 7.204075437095967871, 100.4687500020483810 ) ) ;
#17423=CARTESIAN_POINT ( 'NONE',  ( -4.220049686691937474, -10.18810118749999738, 109.9375000020483952 ) ) ;
#17432=CARTESIAN_POINT ( 'NONE',  ( -10.18810118749999916, 4.220049686691934809, 106.9375000020483810 ) ) ;
#17448=EDGE_LOOP ( 'NONE', ( #33156, #15060, #49289, #64374 ) ) ;
#17449=CARTESIAN_POINT ( 'NONE',  ( -10.18810118749999916, 0.000000000000000000, 112.6562500020483810 ) ) ;
#17468=CARTESIAN_POINT ( 'NONE',  ( 10.18810118750000093, -4.220049686691933921, 70.18750000204838102 ) ) ;
#17479=CARTESIAN_POINT ( 'NONE',  ( 7.778174593052023411, -7.778174593052021635, 108.2500000040967763 ) ) ;
#17484=CARTESIAN_POINT ( 'NONE',  ( 4.556349186104052151, -10.99999999999999822, 108.1562500040967763 ) ) ;
#17489=VECTOR ( 'NONE', #25799, 1000.000000000000000 ) ;
#17504=CARTESIAN_POINT ( 'NONE',  ( -10.18810118749999738, -4.220049686691941915, 81.25000000204836681 ) ) ;
#17505=CARTESIAN_POINT ( 'NONE',  ( -11.00000000000000000, 0.000000000000000000, 118.0000000000000000 ) ) ;
#17508=CARTESIAN_POINT ( 'NONE',  ( -7.204075437095967871, 7.204075437095967871, 114.3437500020483810 ) ) ;
#17515=CARTESIAN_POINT ( 'NONE',  ( -10.18810118749999916, 0.000000000000000000, 77.03125000204836681 ) ) ;
#17528=CARTESIAN_POINT ( 'NONE',  ( -4.220049686691937474, -10.18810118749999738, 69.43750000204838102 ) ) ;
#17551=LINE ( 'NONE', #28502, #10891 ) ;
#17565=LINE ( 'NONE', #5889, #51679 ) ;
#17591=ORIENTED_EDGE ( 'NONE', *, *, #25734, .T. ) ;
#17593=CARTESIAN_POINT ( 'NONE',  ( -10.18810118749999738, -4.220049686691941915, 99.25000000204838102 ) ) ;
#17610=CARTESIAN_POINT ( 'NONE',  ( -6.238412754330611322E-16, 10.18810118749999916, 97.65625000204838102 ) ) ;
#17613=DIRECTION ( 'NONE',  ( 1.000000000000000000, 0.000000000000000000, 0.000000000000000000 ) ) ;
#17623=CARTESIAN_POINT ( 'NONE',  ( 10.18810118749999916, 4.220049686691935698, 86.50000000204838102 ) ) ;
#17631=CARTESIAN_POINT ( 'NONE',  ( 10.18810118749999916, 4.220049686691935698, 77.87500000204838102 ) ) ;
#17648=CARTESIAN_POINT ( 'NONE',  ( 7.204075437095968759, -7.204075437095966983, 69.71875000204836681 ) ) ;
#17651=CARTESIAN_POINT ( 'NONE',  ( -11.00000000000000000, 0.000000000000000000, 84.99999999999998579 ) ) ;
#17655=EDGE_LOOP ( 'NONE', ( #57364, #4726, #70376, #14968 ) ) ;
#17680=CARTESIAN_POINT ( 'NONE',  ( 11.00000000000000355, -4.556349186104045046, 69.34375000409679046 ) ) ;
#17692=CARTESIAN_POINT ( 'NONE',  ( 4.220049686691934809, 10.18810118749999916, 112.5625000020483810 ) ) ;
#17695=CARTESIAN_POINT ( 'NONE',  ( -4.220049686691937474, -10.18810118749999738, 73.93750000204838102 ) ) ;
#17711=ORIENTED_EDGE ( 'NONE', *, *, #68278, .F. ) ;
#17719=CARTESIAN_POINT ( 'NONE',  ( 11.00000000000010836, -4.556349186103939353, 78.34375000409676204 ) ) ;
#17731=CARTESIAN_POINT ( 'NONE',  ( -4.220049686691937474, -10.18810118749999738, 87.43750000204838102 ) ) ;
#17734=CARTESIAN_POINT ( 'NONE',  ( -11.00000000000000000, 0.000000000000000000, 98.49999999999998579 ) ) ;
#17764=ORIENTED_EDGE ( 'NONE', *, *, #22786, .F. ) ;
#17767=CARTESIAN_POINT ( 'NONE',  ( -7.778174593052020747, -7.778174593052023411, 88.37500000409677625 ) ) ;
#17769=CARTESIAN_POINT ( 'NONE',  ( -11.00000000000000000, 0.000000000000000000, 110.6875000040967763 ) ) ;
#17781=CARTESIAN_POINT ( 'NONE',  ( 4.556349186104045934, 11.00000000000000000, 102.7187500040967620 ) ) ;
#17793=CARTESIAN_POINT ( 'NONE',  ( -10.18810118749999738, -4.220049686691941915, 95.12500000204836681 ) ) ;
#17801=CARTESIAN_POINT ( 'NONE',  ( 4.220049686691941027, -10.18810118749999738, 105.6250000020483668 ) ) ;
#17808=CARTESIAN_POINT ( 'NONE',  ( 11.00000000000005151, 4.556349186103993532, 96.34374999999998579 ) ) ;
#17810=CARTESIAN_POINT ( 'NONE',  ( -10.18810118749999738, -4.220049686691941915, 105.6250000020483668 ) ) ;
#17814=ORIENTED_EDGE ( 'NONE', *, *, #68172, .T. ) ;
#17828=CARTESIAN_POINT ( 'NONE',  ( 7.204075437095968759, -7.204075437095966983, 107.2187500020483810 ) ) ;
#17837=ORIENTED_EDGE ( 'NONE', *, *, #28984, .T. ) ;
#17845=CARTESIAN_POINT ( 'NONE',  ( 11.00000000000000355, -4.556349186104045046, 117.1562499999999858 ) ) ;
#17851=CARTESIAN_POINT ( 'NONE',  ( -11.00000000000000533, -11.00000000000000355, 41.99999999999999289 ) ) ;
#17855=CARTESIAN_POINT ( 'NONE',  ( 11.00000000000000000, 4.556349186104045934, 110.0312500040967620 ) ) ;
#17877=CARTESIAN_POINT ( 'NONE',  ( -10.18810118749999916, 4.220049686691934809, 82.56250000204836681 ) ) ;
#17881=DIRECTION ( 'NONE',  ( -1.000000000000000000, 0.000000000000000000, 0.000000000000000000 ) ) ;
#17882=FACE_OUTER_BOUND ( 'NONE', #27471, .T. ) ;
#17890=CARTESIAN_POINT ( 'NONE',  ( 1.871523826299183495E-15, -10.18810118749999916, 77.40625000204836681 ) ) ;
#17894=CARTESIAN_POINT ( 'NONE',  ( 11.00000000000000000, 1.347111479062088405E-15, 94.93750000409677625 ) ) ;
#17904=CARTESIAN_POINT ( 'NONE',  ( -4.220049686691935698, 10.18810118749999916, 71.87500000204836681 ) ) ;
#17906=CARTESIAN_POINT ( 'NONE',  ( 11.00000000000000000, 1.347111479062088405E-15, 109.7499999999999858 ) ) ;
#17916=CARTESIAN_POINT ( 'NONE',  ( -4.556349186104045934, 11.00000000000000000, 93.90625000409679046 ) ) ;
#17925=AXIS2_PLACEMENT_3D ( 'NONE', #6679, #23275, #13049 ) ;
#17950=CARTESIAN_POINT ( 'NONE',  ( 11.00000000000000000, 4.556349186104045934, 68.03125000409676204 ) ) ;
#17968=CARTESIAN_POINT ( 'NONE',  ( -6.238412754330611322E-16, 10.18810118749999916, 101.7812500020483810 ) ) ;
#17985=CARTESIAN_POINT ( 'NONE',  ( 4.220049686691941027, -10.18810118749999738, 95.50000000204838102 ) ) ;
#17991=CARTESIAN_POINT ( 'NONE',  ( -10.18810118749999738, -4.220049686691941915, 77.12500000204838102 ) ) ;
#18001=CARTESIAN_POINT ( 'NONE',  ( -10.18810118749999738, -4.220049686691941915, 90.25000000204838102 ) ) ;
#18005=EDGE_CURVE ( 'NONE', #74545, #69418, #69011, .T. ) ;
#18012=CARTESIAN_POINT ( 'NONE',  ( -10.18810118749999916, 4.220049686691934809, 73.93750000204838102 ) ) ;
#18028=CARTESIAN_POINT ( 'NONE',  ( 4.220049686691941027, -10.18810118749999738, 69.62500000204836681 ) ) ;
#18031=CARTESIAN_POINT ( 'NONE',  ( -10.99999999999999822, -4.556349186104052151, 80.59374999999998579 ) ) ;
#18058=CARTESIAN_POINT ( 'NONE',  ( -6.238412754330611322E-16, 10.18810118749999916, 116.7812500020483810 ) ) ;
#18059=CARTESIAN_POINT ( 'NONE',  ( -11.00000000000000000, 0.000000000000000000, 118.0000000000000000 ) ) ;
#18069=CARTESIAN_POINT ( 'NONE',  ( 10.18810118750000093, -4.220049686691933033, 115.1875000020483668 ) ) ;
#18073=DIRECTION ( 'NONE',  ( 0.000000000000000000, 0.000000000000000000, -1.000000000000000000 ) ) ;
#18084=CARTESIAN_POINT ( 'NONE',  ( 11.00000000000000000, 1.347111479062088405E-15, 105.2500000000000000 ) ) ;
#18090=EDGE_CURVE ( 'NONE', #63637, #66203, #20743, .T. ) ;
#18112=CARTESIAN_POINT ( 'NONE',  ( 7.204075437095968759, -7.204075437095966983, 87.71875000204836681 ) ) ;
#18114=CARTESIAN_POINT ( 'NONE',  ( 7.778174593052023411, -7.778174593052021635, 102.0624999999999858 ) ) ;
#18145=CARTESIAN_POINT ( 'NONE',  ( 4.556349186104045934, 11.00000000000000000, 89.21875000409680467 ) ) ;
#18147=CARTESIAN_POINT ( 'NONE',  ( -7.778174593052020747, -7.778174593052023411, 110.8750000040967763 ) ) ;
#18169=CARTESIAN_POINT ( 'NONE',  ( -6.238412754330611322E-16, 10.18810118749999916, 94.65625000204836681 ) ) ;
#18170=ORIENTED_EDGE ( 'NONE', *, *, #12718, .F. ) ;
#18173=CARTESIAN_POINT ( 'NONE',  ( 7.778174593052023411, -7.778174593052021635, 100.7500000040967763 ) ) ;
#18176=CARTESIAN_POINT ( 'NONE',  ( -7.204075437095965206, -7.204075437095968759, 108.3437500020483810 ) ) ;
#18184=CARTESIAN_POINT ( 'NONE',  ( 10.18810118750000093, -4.220049686691933921, 101.6875000020483810 ) ) ;
#18185=EDGE_CURVE ( 'NONE', #20942, #2612, #12134, .T. ) ;
#18201=ORIENTED_EDGE ( 'NONE', *, *, #70693, .T. ) ;
#18202=CARTESIAN_POINT ( 'NONE',  ( -7.204075437095965206, -7.204075437095968759, 102.3437500020483668 ) ) ;
#18213=CARTESIAN_POINT ( 'NONE',  ( -11.00000000000000533, 11.00000000000000000, 41.99999999999999289 ) ) ;
#18220=CARTESIAN_POINT ( 'NONE',  ( -4.220049686691935698, 10.18810118749999916, 67.75000000204836681 ) ) ;
#18231=CARTESIAN_POINT ( 'NONE',  ( -4.556349186104045934, 11.00000000000000000, 107.4062500040967620 ) ) ;
#18246=CARTESIAN_POINT ( 'NONE',  ( 0.000000000000000000, 0.000000000000000000, 118.0000000000000000 ) ) ;
#18249=CARTESIAN_POINT ( 'NONE',  ( -10.18810118749999916, 0.000000000000000000, 82.65625000204838102 ) ) ;
#18253=CARTESIAN_POINT ( 'NONE',  ( 4.220049686691941027, -10.18810118749999738, 107.5000000020483668 ) ) ;
#18261=CARTESIAN_POINT ( 'NONE',  ( 7.204075437095968759, -7.204075437095966983, 77.59375000204838102 ) ) ;
#18275=CARTESIAN_POINT ( 'NONE',  ( 1.871523826299183495E-15, -10.18810118749999916, 69.53125000204838102 ) ) ;
#18321=CARTESIAN_POINT ( 'NONE',  ( 7.778174593052021635, 7.778174593052023411, 68.12500000409677625 ) ) ;
#18337=VECTOR ( 'NONE', #8225, 1000.000000000000000 ) ;
#18339=EDGE_LOOP ( 'NONE', ( #17814, #1519, #43206, #32133 ) ) ;
#18340=CARTESIAN_POINT ( 'NONE',  ( -6.911667950094911639, 8.332266638136186288, 117.6845864511994932 ) ) ;
#18341=CARTESIAN_POINT ( 'NONE',  ( 4.220049686691934809, 10.18810118749999916, 98.68750000204838102 ) ) ;
#18344=CARTESIAN_POINT ( 'NONE',  ( -4.556349186104048599, -10.99999999999999822, 68.78125000000000000 ) ) ;
#18351=VERTEX_POINT ( 'NONE', #54738 ) ;
#18358=CARTESIAN_POINT ( 'NONE',  ( -6.238412754330611322E-16, 10.18810118749999916, 94.65625000204836681 ) ) ;
#18365=CARTESIAN_POINT ( 'NONE',  ( -7.204075437095967871, 7.204075437095967871, 76.84375000204838102 ) ) ;
#18372=CARTESIAN_POINT ( 'NONE',  ( 10.18810118749999916, 1.247682550866122264E-15, 89.40625000204838102 ) ) ;
#18383=CARTESIAN_POINT ( 'NONE',  ( 7.204075437095968759, -7.204075437095966983, 73.09375000204838102 ) ) ;
#18402=CARTESIAN_POINT ( 'NONE',  ( -10.99999999999999822, -4.556349186104052151, 85.09375000000000000 ) ) ;
#18405=CARTESIAN_POINT ( 'NONE',  ( 11.00000000000000000, 1.347111479062088405E-15, 114.2499999999999858 ) ) ;
#18408=CYLINDRICAL_SURFACE ( 'NONE', #13066, 11.00000000000000000 ) ;
#18427=CARTESIAN_POINT ( 'NONE',  ( -10.99999999999989342, 4.556349186104152515, 67.09375000409677625 ) ) ;
#18429=CARTESIAN_POINT ( 'NONE',  ( 11.00000000000000000, 4.556349186104045934, 68.03125000409676204 ) ) ;
#18442=CARTESIAN_POINT ( 'NONE',  ( 10.18810118749999916, 4.220049686691935698, 113.8750000020483810 ) ) ;
#18446=CARTESIAN_POINT ( 'NONE',  ( 2.729887517050593182, 10.18810118749999916, 67.22060451829246119 ) ) ;
#18467=CARTESIAN_POINT ( 'NONE',  ( 11.00000000000000000, 1.347111479062088405E-15, 78.43750000409677625 ) ) ;
#18481=CARTESIAN_POINT ( 'NONE',  ( 10.18810118750000093, -4.220049686691933033, 87.81250000204838102 ) ) ;
#18484=CARTESIAN_POINT ( 'NONE',  ( 4.556349186104051263, -10.99999999999999822, 98.96875000000000000 ) ) ;
#18515=CARTESIAN_POINT ( 'NONE',  ( 11.00000000000000000, 1.347111479062088405E-15, 87.43750000409677625 ) ) ;
#18517=CARTESIAN_POINT ( 'NONE',  ( 7.778174593052023411, -7.778174593052021635, 111.2500000040967763 ) ) ;
#18528=VERTEX_POINT ( 'NONE', #15838 ) ;
#18540=CARTESIAN_POINT ( 'NONE',  ( 7.204075437095966983, 7.204075437095967871, 91.46875000204838102 ) ) ;
#18546=CARTESIAN_POINT ( 'NONE',  ( -4.220049686691935698, 10.18810118749999916, 98.87500000204836681 ) ) ;
#18550=VECTOR ( 'NONE', #35017, 1000.000000000000000 ) ;
#18554=CARTESIAN_POINT ( 'NONE',  ( 4.556349186104045934, 11.00000000000000000, 96.53125000000000000 ) ) ;
#18555=CARTESIAN_POINT ( 'NONE',  ( -7.204075437095967871, 7.204075437095967871, 105.3437500020483810 ) ) ;
#18570=ORIENTED_EDGE ( 'NONE', *, *, #56439, .F. ) ;
#18571=CARTESIAN_POINT ( 'NONE',  ( -4.220049686691935698, 10.18810118749999916, 104.8750000020483668 ) ) ;
#18588=CARTESIAN_POINT ( 'NONE',  ( 11.00000000000000000, 4.556349186104045934, 72.53125000409677625 ) ) ;
#18589=CARTESIAN_POINT ( 'NONE',  ( -10.18810118749999916, 0.000000000000000000, 71.03125000204838102 ) ) ;
#18602=CARTESIAN_POINT ( 'NONE',  ( 4.556349186104045934, 11.00000000000000000, 104.2187500040968047 ) ) ;
#18609=EDGE_CURVE ( 'NONE', #45292, #49304, #38607, .T. ) ;
#18613=CARTESIAN_POINT ( 'NONE',  ( 0.000000000000000000, 0.000000000000000000, 118.0000000000000000 ) ) ;
#18622=CARTESIAN_POINT ( 'NONE',  ( 10.18810118750000093, -4.220049686691933921, 80.31250000204836681 ) ) ;
#18627=CARTESIAN_POINT ( 'NONE',  ( 4.220049686691941027, -10.18810118749999738, 109.0000000020483810 ) ) ;
#18635=CARTESIAN_POINT ( 'NONE',  ( 10.18810118749999916, 4.220049686691935698, 76.37500000204838102 ) ) ;
#18638=CARTESIAN_POINT ( 'NONE',  ( -11.00000000000000000, 0.000000000000000000, 94.18750000409677625 ) ) ;
#18647=CARTESIAN_POINT ( 'NONE',  ( 4.220049686691934809, 10.18810118749999916, 73.18750000204838102 ) ) ;
#18694=CARTESIAN_POINT ( 'NONE',  ( -6.735557395310442023E-16, 11.00000000000000000, 68.31250000409677625 ) ) ;
#18710=ORIENTED_EDGE ( 'NONE', *, *, #31139, .T. ) ;
#18711=CARTESIAN_POINT ( 'NONE',  ( 3.294287002270811282, 10.47076035885145018, 117.5334525074227798 ) ) ;
#18712=CARTESIAN_POINT ( 'NONE',  ( 10.18810118749999916, 4.220049686691935698, 101.5000000020483810 ) ) ;
#18723=CARTESIAN_POINT ( 'NONE',  ( -11.00000000000000000, 0.000000000000000000, 72.99999999999998579 ) ) ;
#18728=CARTESIAN_POINT ( 'NONE',  ( -7.204075437095965206, -7.204075437095968759, 93.71875000204838102 ) ) ;
#18735=CARTESIAN_POINT ( 'NONE',  ( -4.220049686691937474, -10.18810118749999738, 72.81250000204836681 ) ) ;
#18740=CARTESIAN_POINT ( 'NONE',  ( 0.000000000000000000, 0.000000000000000000, 118.0000000000000000 ) ) ;
#18742=CARTESIAN_POINT ( 'NONE',  ( 1.871523826299183495E-15, -10.18810118749999916, 90.53125000204836681 ) ) ;
#18751=CARTESIAN_POINT ( 'NONE',  ( 4.220049686691941027, -10.18810118749999738, 77.50000000204839523 ) ) ;
#18774=CARTESIAN_POINT ( 'NONE',  ( -10.99999999999999822, -4.556349186104052151, 79.09375000000000000 ) ) ;
#18798=EDGE_LOOP ( 'NONE', ( #26994, #67847, #14486, #6125, #50252 ) ) ;
#18800=CARTESIAN_POINT ( 'NONE',  ( -6.735557395310442023E-16, 11.00000000000000000, 66.81250000409677625 ) ) ;
#18802=CARTESIAN_POINT ( 'NONE',  ( 10.18810118749999916, 1.247682550866122264E-15, 116.4062500020483810 ) ) ;
#18813=CARTESIAN_POINT ( 'NONE',  ( 4.220049686691941027, -10.18810118749999738, 113.5000000020483810 ) ) ;
#18818=CARTESIAN_POINT ( 'NONE',  ( -4.220049686691937474, -10.18810118749999738, 67.93750000204838102 ) ) ;
#18836=ORIENTED_EDGE ( 'NONE', *, *, #13996, .T. ) ;
#18839=EDGE_CURVE ( 'NONE', #24549, #71006, #24265, .T. ) ;
#18846=VERTEX_POINT ( 'NONE', #21974 ) ;
#18848=EDGE_LOOP ( 'NONE', ( #3494, #73389, #67895, #46540 ) ) ;
#18849=CARTESIAN_POINT ( 'NONE',  ( -10.18810118749999916, 0.000000000000000000, 87.15625000204838102 ) ) ;
#18851=CARTESIAN_POINT ( 'NONE',  ( -11.00000000000000000, 4.556349186104045934, 96.90624999999998579 ) ) ;
#18852=CARTESIAN_POINT ( 'NONE',  ( 2.020667218593132706E-15, -11.00000000000000000, 104.8750000000000000 ) ) ;
#18856=CARTESIAN_POINT ( 'NONE',  ( -6.735557395310442023E-16, 11.00000000000000000, 105.8125000040967763 ) ) ;
#18870=LINE ( 'NONE', #70919, #39569 ) ;
#18875=LINE ( 'NONE', #7193, #5766 ) ;
#18876=ORIENTED_EDGE ( 'NONE', *, *, #45345, .F. ) ;
#18877=CARTESIAN_POINT ( 'NONE',  ( 4.556349186104045934, 11.00000000000000000, 104.2187500040967905 ) ) ;
#18880=CARTESIAN_POINT ( 'NONE',  ( -11.00000000000000000, 0.000000000000000000, 85.18750000409677625 ) ) ;
#18904=CARTESIAN_POINT ( 'NONE',  ( 7.204075437095966983, 7.204075437095967871, 89.96875000204838102 ) ) ;
#18905=ORIENTED_EDGE ( 'NONE', *, *, #68172, .F. ) ;
#18910=CARTESIAN_POINT ( 'NONE',  ( 1.871523826299183495E-15, -10.18810118749999916, 104.0312500020483810 ) ) ;
#18912=ORIENTED_EDGE ( 'NONE', *, *, #54378, .F. ) ;
#18918=CARTESIAN_POINT ( 'NONE',  ( -7.204075437095967871, 7.204075437095967871, 96.34375000204836681 ) ) ;
#18919=EDGE_CURVE ( 'NONE', #40106, #18528, #68116, .T. ) ;
#18936=CARTESIAN_POINT ( 'NONE',  ( -6.238412754330611322E-16, 10.18810118749999916, 106.2812500020483810 ) ) ;
#18954=CARTESIAN_POINT ( 'NONE',  ( 7.778174593052021635, 7.778174593052023411, 112.9375000000000000 ) ) ;
#18966=CARTESIAN_POINT ( 'NONE',  ( 2.020667218593132706E-15, -11.00000000000000000, 105.0625000040967763 ) ) ;
#18972=CARTESIAN_POINT ( 'NONE',  ( -7.778174593052023411, 7.778174593052023411, 87.81249999999998579 ) ) ;
#18983=CARTESIAN_POINT ( 'NONE',  ( -11.00000000000000000, 0.000000000000000000, 118.0000000000000000 ) ) ;
#18987=DIRECTION ( 'NONE',  ( -0.000000000000000000, -0.000000000000000000, -1.000000000000000000 ) ) ;
#18988=CARTESIAN_POINT ( 'NONE',  ( -7.204075437095967871, 7.204075437095967871, 106.8437500020483810 ) ) ;
#18995=CARTESIAN_POINT ( 'NONE',  ( 10.18810118749999916, 4.220049686691935698, 68.87500000204838102 ) ) ;
#19001=EDGE_CURVE ( 'NONE', #48097, #20942, #71268, .T. ) ;
#19007=AXIS2_PLACEMENT_3D ( 'NONE', #38183, #48734, #49107 ) ;
#19008=CARTESIAN_POINT ( 'NONE',  ( 7.204075437095966983, 7.204075437095967871, 116.9687500020483810 ) ) ;
#19011=ORIENTED_EDGE ( 'NONE', *, *, #40010, .F. ) ;
#19055=CARTESIAN_POINT ( 'NONE',  ( -4.556349186104045934, 11.00000000000000000, 68.40625000409677625 ) ) ;
#19062=CARTESIAN_POINT ( 'NONE',  ( 2.020667218593132706E-15, -11.00000000000000000, 85.37499999999997158 ) ) ;
#19072=CARTESIAN_POINT ( 'NONE',  ( 10.18810118750000093, -4.220049686691933921, 95.31250000204838102 ) ) ;
#19073=CARTESIAN_POINT ( 'NONE',  ( -11.00000000000000000, 0.000000000000000000, 118.0000000000000000 ) ) ;
#19087=CARTESIAN_POINT ( 'NONE',  ( -7.204075437095967871, 7.204075437095967871, 88.84375000204838102 ) ) ;
#19092=CARTESIAN_POINT ( 'NONE',  ( -10.18810118749999916, 0.000000000000000000, 72.53125000204838102 ) ) ;
#19098=( BOUNDED_CURVE ( )  B_SPLINE_CURVE ( 2, ( #39206, #55075, #61092, #9420, #32439, #33199, #67506, #56195, #61470 ),
 .UNSPECIFIED., .F., .F. ) 
 B_SPLINE_CURVE_WITH_KNOTS ( ( 3, 2, 2, 2, 3 ),
 ( 0.8970588235294119084, 0.9007352941176471894, 0.9044117647058824705, 0.9080882352941177516, 0.9117647058823530326 ),
 .UNSPECIFIED. ) 
 CURVE ( )  GEOMETRIC_REPRESENTATION_ITEM ( )  RATIONAL_B_SPLINE_CURVE ( ( 0.9999999999999976685, 0.9238795325112890700, 1.000000000000000000, 0.9238795325112867385, 1.000000000000000000, 0.9238795325112867385, 1.000000000000000000, 0.9238795325112844070, 1.000000000000002220 ) ) 
 REPRESENTATION_ITEM ( '' )  );
#19099=CARTESIAN_POINT ( 'NONE',  ( 7.204075437095966983, 7.204075437095967871, 91.09375000204838102 ) ) ;
#19111=CARTESIAN_POINT ( 'NONE',  ( 10.18810118749999916, 1.247682550866122264E-15, 70.28125000204838102 ) ) ;
#19124=CARTESIAN_POINT ( 'NONE',  ( 11.00000000000010658, 4.556349186103942017, 91.84374999999998579 ) ) ;
#19131=CARTESIAN_POINT ( 'NONE',  ( -6.735557395310442023E-16, 11.00000000000000000, 75.62499999999998579 ) ) ;
#19141=CARTESIAN_POINT ( 'NONE',  ( -11.00000000000000000, 0.000000000000000000, 116.6875000040967763 ) ) ;
#19152=DIRECTION ( 'NONE',  ( -1.000000000000000000, -1.084202172485504434E-16, 0.000000000000000000 ) ) ;
#19158=CARTESIAN_POINT ( 'NONE',  ( -6.238412754330611322E-16, 10.18810118749999916, 85.65625000204838102 ) ) ;
#19160=CARTESIAN_POINT ( 'NONE',  ( 5.499989586027935751, 9.526285454130809072, 66.68677389048281157 ) ) ;
#19171=CARTESIAN_POINT ( 'NONE',  ( -7.204075437095965206, -7.204075437095968759, 108.7187500020483810 ) ) ;
#19184=EDGE_CURVE ( 'NONE', #15561, #58474, #4011, .T. ) ;
#19212=CARTESIAN_POINT ( 'NONE',  ( -4.220049686691935698, 10.18810118749999916, 86.87500000204836681 ) ) ;
#19214=CARTESIAN_POINT ( 'NONE',  ( 7.778174593052023411, -7.778174593052021635, 96.06250000000000000 ) ) ;
#19240=CARTESIAN_POINT ( 'NONE',  ( 2.020667218593132706E-15, -11.00000000000000000, 85.56250000409676204 ) ) ;
#19253=ORIENTED_EDGE ( 'NONE', *, *, #40888, .T. ) ;
#19265=CARTESIAN_POINT ( 'NONE',  ( -4.220049686691935698, 10.18810118749999916, 93.25000000204838102 ) ) ;
#19271=CARTESIAN_POINT ( 'NONE',  ( 10.18810118749999916, 1.247682550866122264E-15, 99.90625000204838102 ) ) ;
#19274=ORIENTED_EDGE ( 'NONE', *, *, #56766, .T. ) ;
#19280=CARTESIAN_POINT ( 'NONE',  ( 10.18810118749999916, 1.247682550866122264E-15, 100.2812500020483810 ) ) ;
#19291=AXIS2_PLACEMENT_3D ( 'NONE', #28308, #68669, #57742 ) ;
#19296=CARTESIAN_POINT ( 'NONE',  ( -4.220049686691935698, 10.18810118749999916, 101.8750000020483810 ) ) ;
#19297=CARTESIAN_POINT ( 'NONE',  ( -4.556349186104045934, 11.00000000000000000, 114.9062500040967763 ) ) ;
#19307=CARTESIAN_POINT ( 'NONE',  ( -11.00000000000000000, 0.000000000000000000, 74.49999999999998579 ) ) ;
#19313=CARTESIAN_POINT ( 'NONE',  ( 4.556349186104051263, -10.99999999999999822, 110.9687500000000142 ) ) ;
#19325=CARTESIAN_POINT ( 'NONE',  ( 7.778174593052021635, 7.778174593052023411, 105.6250000040967763 ) ) ;
#19328=CARTESIAN_POINT ( 'NONE',  ( 11.00000000000000000, 4.556349186104045934, 95.03125000409677625 ) ) ;
#19339=CARTESIAN_POINT ( 'NONE',  ( 2.020667218593132706E-15, -11.00000000000000000, 67.56250000409677625 ) ) ;
#19348=CARTESIAN_POINT ( 'NONE',  ( -7.204075437095965206, -7.204075437095968759, 111.7187500020483810 ) ) ;
#19350=VECTOR ( 'NONE', #58857, 1000.000000000000000 ) ;
#19352=CARTESIAN_POINT ( 'NONE',  ( 0.000000000000000000, 0.000000000000000000, 118.0000000000000000 ) ) ;
#19356=CARTESIAN_POINT ( 'NONE',  ( -7.204075437095967871, 7.204075437095967871, 73.84375000204838102 ) ) ;
#19368=CARTESIAN_POINT ( 'NONE',  ( -10.18810118749999738, -4.220049686691941915, 67.75000000204836681 ) ) ;
#19390=DIRECTION ( 'NONE',  ( -0.000000000000000000, -0.000000000000000000, -1.000000000000000000 ) ) ;
#19405=DIRECTION ( 'NONE',  ( -1.000000000000000000, 0.000000000000000000, 0.000000000000000000 ) ) ;
#19422=CARTESIAN_POINT ( 'NONE',  ( -11.00000000000000000, 0.000000000000000000, 84.99999999999998579 ) ) ;
#19435=CARTESIAN_POINT ( 'NONE',  ( -4.220049686691937474, -10.18810118749999738, 96.43750000204836681 ) ) ;
#19451=CARTESIAN_POINT ( 'NONE',  ( 10.18810118749999916, 1.247682550866122264E-15, 88.28125000204836681 ) ) ;
#19456=CARTESIAN_POINT ( 'NONE',  ( -1.734723475976807489E-15, 11.00000000000000178, 41.99999999999999289 ) ) ;
#19457=CARTESIAN_POINT ( 'NONE',  ( -7.204075437095965206, -7.204075437095968759, 75.71875000204836681 ) ) ;
#19465=CARTESIAN_POINT ( 'NONE',  ( -10.18810118749999916, 4.220049686691934809, 85.56250000204838102 ) ) ;
#19476=CARTESIAN_POINT ( 'NONE',  ( -10.18810118749999916, 0.000000000000000000, 68.03125000204838102 ) ) ;
#19495=CARTESIAN_POINT ( 'NONE',  ( -11.00000000000000000, 0.000000000000000000, 74.49999999999998579 ) ) ;
#19506=CARTESIAN_POINT ( 'NONE',  ( 4.556349186104045934, 11.00000000000000000, 114.7187500040967620 ) ) ;
#19516=PLANE ( 'NONE',  #68847 ) ;
#19521=CARTESIAN_POINT ( 'NONE',  ( 10.18810118749999916, 4.220049686691935698, 88.37500000204839523 ) ) ;
#19523=CARTESIAN_POINT ( 'NONE',  ( 10.18810118749999916, 1.247682550866122264E-15, 111.9062500020483810 ) ) ;
#19533=CARTESIAN_POINT ( 'NONE',  ( 0.000000000000000000, 0.000000000000000000, 118.0000000000000000 ) ) ;
#19535=CARTESIAN_POINT ( 'NONE',  ( -6.238412754330611322E-16, 10.18810118749999916, 105.1562500020483810 ) ) ;
#19553=AXIS2_PLACEMENT_3D ( 'NONE', #19352, #48395, #71399 ) ;
#19574=CARTESIAN_POINT ( 'NONE',  ( -4.220049686691935698, 10.18810118749999916, 82.37500000204838102 ) ) ;
#19576=CARTESIAN_POINT ( 'NONE',  ( 7.778174593052023411, -7.778174593052021635, 93.06249999999998579 ) ) ;
#19601=DIRECTION ( 'NONE',  ( 0.000000000000000000, 1.000000000000000000, 0.000000000000000000 ) ) ;
#19608=CARTESIAN_POINT ( 'NONE',  ( 11.00000000000000355, -4.556349186104045046, 81.34375000409677625 ) ) ;
#19633=CARTESIAN_POINT ( 'NONE',  ( 1.871523826299183495E-15, -10.18810118749999916, 87.90625000204838102 ) ) ;
#19638=CARTESIAN_POINT ( 'NONE',  ( 4.220049686691934809, 10.18810118749999916, 101.6875000020483810 ) ) ;
#19643=ORIENTED_EDGE ( 'NONE', *, *, #59179, .T. ) ;
#19648=CARTESIAN_POINT ( 'NONE',  ( -10.18810118749999916, 0.000000000000000000, 99.53125000204838102 ) ) ;
#19660=CARTESIAN_POINT ( 'NONE',  ( 11.00000000000000000, 1.347111479062088405E-15, 84.24999999999998579 ) ) ;
#19662=ORIENTED_EDGE ( 'NONE', *, *, #24212, .F. ) ;
#19665=CARTESIAN_POINT ( 'NONE',  ( -6.238412754330611322E-16, 10.18810118749999916, 97.28125000204838102 ) ) ;
#19684=CARTESIAN_POINT ( 'NONE',  ( -4.556349186104047710, -10.99999999999999822, 115.2812500000000000 ) ) ;
#19692=DIRECTION ( 'NONE',  ( -0.000000000000000000, -0.000000000000000000, -1.000000000000000000 ) ) ;
#19696=CARTESIAN_POINT ( 'NONE',  ( 11.00000000000000000, 1.347111479062088405E-15, 105.4375000040967763 ) ) ;
#19711=ORIENTED_EDGE ( 'NONE', *, *, #831, .F. ) ;
#19718=LINE ( 'NONE', #52958, #47693 ) ;
#19720=CARTESIAN_POINT ( 'NONE',  ( 11.00000000000000000, 1.347111479062088405E-15, 69.24999999999997158 ) ) ;
#19721=CARTESIAN_POINT ( 'NONE',  ( 10.18810118749999916, 4.220049686691935698, 109.3750000020483810 ) ) ;
#19724=CARTESIAN_POINT ( 'NONE',  ( 11.00000000000000000, 1.347111479062088405E-15, 90.25000000000000000 ) ) ;
#19728=CARTESIAN_POINT ( 'NONE',  ( -10.18810118749999916, 0.000000000000000000, 72.53125000204838102 ) ) ;
#19742=CARTESIAN_POINT ( 'NONE',  ( -4.220049686691935698, 10.18810118749999916, 114.2500000020483952 ) ) ;
#19774=CARTESIAN_POINT ( 'NONE',  ( 4.556349186104045934, 11.00000000000000000, 116.2187500040967763 ) ) ;
#19786=CARTESIAN_POINT ( 'NONE',  ( -11.00000000000000000, 4.556349186104045934, 77.59375000409676204 ) ) ;
#19787=CARTESIAN_POINT ( 'NONE',  ( -11.00000000000000000, 0.000000000000000000, 85.18750000409677625 ) ) ;
#19800=CARTESIAN_POINT ( 'NONE',  ( -6.735557395310442023E-16, 11.00000000000000000, 81.81250000409677625 ) ) ;
#19805=CARTESIAN_POINT ( 'NONE',  ( 0.9859162824928909830, 10.93016620314303999, 117.5662746148575906 ) ) ;
#19806=CARTESIAN_POINT ( 'NONE',  ( 10.18810118750000093, -4.220049686691933921, 93.81250000204839523 ) ) ;
#19815=CARTESIAN_POINT ( 'NONE',  ( 11.00000000000000000, 4.556349186104045934, 76.84374999999998579 ) ) ;
#19820=CARTESIAN_POINT ( 'NONE',  ( -7.204075437095967871, 7.204075437095967871, 87.34375000204836681 ) ) ;
#19825=CARTESIAN_POINT ( 'NONE',  ( -11.00000000000000000, 0.000000000000000000, 101.6875000040967763 ) ) ;
#19826=CARTESIAN_POINT ( 'NONE',  ( -10.18810118749999916, 0.000000000000000000, 74.03125000204838102 ) ) ;
#19831=DIRECTION ( 'NONE',  ( -1.000000000000000000, 0.000000000000000000, 0.000000000000000000 ) ) ;
#19834=CARTESIAN_POINT ( 'NONE',  ( 10.18810118749999916, 4.220049686691935698, 85.00000000204838102 ) ) ;
#19845=CARTESIAN_POINT ( 'NONE',  ( -4.220049686691935698, 10.18810118749999916, 69.25000000204836681 ) ) ;
#19868=CARTESIAN_POINT ( 'NONE',  ( 11.00000000000000000, 4.556349186104045934, 79.84374999999998579 ) ) ;
#19894=CARTESIAN_POINT ( 'NONE',  ( -10.18810118749999916, 4.220049686691934809, 88.93750000204839523 ) ) ;
#19895=CARTESIAN_POINT ( 'NONE',  ( 7.204075437095966983, 7.204075437095967871, 110.5937500020483810 ) ) ;
#19909=CARTESIAN_POINT ( 'NONE',  ( 1.871523826299183495E-15, -10.18810118749999916, 108.9062500020483668 ) ) ;
#19934=LINE ( 'NONE', #71989, #40275 ) ;
#19940=EDGE_CURVE ( 'NONE', #6126, #60666, #61841, .T. ) ;
#19946=CARTESIAN_POINT ( 'NONE',  ( -4.220049686691935698, 10.18810118749999916, 77.87500000204838102 ) ) ;
#19949=CARTESIAN_POINT ( 'NONE',  ( -11.00000000000000000, 4.556349186104045934, 92.40624999999998579 ) ) ;
#19963=DIRECTION ( 'NONE',  ( 1.000000000000000000, 3.154042683594195121E-16, 0.000000000000000000 ) ) ;
#19978=CARTESIAN_POINT ( 'NONE',  ( 4.556349186104045934, 11.00000000000000000, 80.21875000409679046 ) ) ;
#19981=DIRECTION ( 'NONE',  ( -0.000000000000000000, -0.000000000000000000, -1.000000000000000000 ) ) ;
#19995=CARTESIAN_POINT ( 'NONE',  ( -4.220049686691935698, 10.18810118749999916, 76.37500000204838102 ) ) ;
#20002=CARTESIAN_POINT ( 'NONE',  ( 10.18810118749999916, 1.247682550866122264E-15, 85.28125000204836681 ) ) ;
#20008=CARTESIAN_POINT ( 'NONE',  ( -7.204075437095967871, 7.204075437095967871, 98.96875000204838102 ) ) ;
#20014=CARTESIAN_POINT ( 'NONE',  ( 4.220049686691934809, 10.18810118749999916, 96.06250000204836681 ) ) ;
#20017=DIRECTION ( 'NONE',  ( 1.000000000000000000, 1.991032627040250683E-16, 0.000000000000000000 ) ) ;
#20031=CARTESIAN_POINT ( 'NONE',  ( 10.18810118750000093, -4.220049686691933033, 101.3125000020483810 ) ) ;
#20039=ORIENTED_EDGE ( 'NONE', *, *, #37412, .T. ) ;
#20040=ADVANCED_FACE ( 'NONE', ( #53131 ), #29742, .T. ) ;
#20047=CARTESIAN_POINT ( 'NONE',  ( 11.00000000000000000, 1.347111479062088405E-15, 114.2499999999999858 ) ) ;
#20055=DIRECTION ( 'NONE',  ( 1.000000000000000000, -3.552713678800500929E-15, 0.000000000000000000 ) ) ;
#20060=CARTESIAN_POINT ( 'NONE',  ( -7.778174593052023411, 7.778174593052023411, 97.00000000409677625 ) ) ;
#20066=CARTESIAN_POINT ( 'NONE',  ( 10.99999999999989342, 4.556349186104152515, 87.34374999999998579 ) ) ;
#20087=CARTESIAN_POINT ( 'NONE',  ( 4.220049686691941027, -10.18810118749999738, 103.0000000020483668 ) ) ;
#20094=CARTESIAN_POINT ( 'NONE',  ( -6.238412754330611322E-16, 10.18810118749999916, 72.15625000204836681 ) ) ;
#20097=CARTESIAN_POINT ( 'NONE',  ( -10.18810118749999916, 4.220049686691934809, 117.0625000020483668 ) ) ;
#20110=CARTESIAN_POINT ( 'NONE',  ( 10.18810118749999916, 4.220049686691935698, 113.8750000020483668 ) ) ;
#20125=CARTESIAN_POINT ( 'NONE',  ( -10.18810118749999738, -4.220049686691941915, 115.7500000020483810 ) ) ;
#20126=CARTESIAN_POINT ( 'NONE',  ( -10.49999999999998224, 0.000000000000000000, 118.0000000000000000 ) ) ;
#20133=CARTESIAN_POINT ( 'NONE',  ( -6.735557395310442023E-16, 11.00000000000000000, 113.3125000040967763 ) ) ;
#20136=DIRECTION ( 'NONE',  ( -1.000000000000000000, 0.000000000000000000, 0.000000000000000000 ) ) ;
#20156=VECTOR ( 'NONE', #4770, 1000.000000000000000 ) ;
#20162=DIRECTION ( 'NONE',  ( -0.000000000000000000, -0.000000000000000000, -1.000000000000000000 ) ) ;
#20171=CARTESIAN_POINT ( 'NONE',  ( 7.204075437095966983, 7.204075437095967871, 97.09375000204836681 ) ) ;
#20185=CARTESIAN_POINT ( 'NONE',  ( 10.18810118749999916, 4.220049686691935698, 86.87500000204836681 ) ) ;
#20199=CARTESIAN_POINT ( 'NONE',  ( 10.18810118750000093, -4.220049686691933921, 81.81250000204838102 ) ) ;
#20201=ADVANCED_FACE ( 'NONE', ( #35053 ), #63693, .T. ) ;
#20216=VECTOR ( 'NONE', #41074, 1000.000000000000000 ) ;
#20234=CARTESIAN_POINT ( 'NONE',  ( -11.00000000000000000, 4.556349186104045934, 77.40624999999997158 ) ) ;
#20240=CARTESIAN_POINT ( 'NONE',  ( -11.00000000000000000, 0.000000000000000000, 113.6875000040967763 ) ) ;
#20246=FACE_OUTER_BOUND ( 'NONE', #14917, .T. ) ;
#20258=CARTESIAN_POINT ( 'NONE',  ( 10.18810118750000093, -4.220049686691933921, 88.18750000204838102 ) ) ;
#20259=CARTESIAN_POINT ( 'NONE',  ( -4.220049686691937474, -10.18810118749999738, 114.4375000020483668 ) ) ;
#20274=CARTESIAN_POINT ( 'NONE',  ( 4.220049686691934809, 10.18810118749999916, 109.5625000020483810 ) ) ;
#20302=CARTESIAN_POINT ( 'NONE',  ( 11.00000000000000000, 1.347111479062088405E-15, 72.24999999999998579 ) ) ;
#20314=CARTESIAN_POINT ( 'NONE',  ( 10.18810118749999916, 4.220049686691935698, 79.00000000204838102 ) ) ;
#20317=CARTESIAN_POINT ( 'NONE',  ( -11.00000000000000000, 0.000000000000000000, 92.49999999999998579 ) ) ;
#20323=CARTESIAN_POINT ( 'NONE',  ( 7.778174593052023411, -7.778174593052021635, 84.06249999999998579 ) ) ;
#20346=CARTESIAN_POINT ( 'NONE',  ( -7.778174593052023411, 7.778174593052023411, 83.50000000409677625 ) ) ;
#20363=CARTESIAN_POINT ( 'NONE',  ( -11.00000000000000000, 0.000000000000000000, 118.0000000000000000 ) ) ;
#20364=CARTESIAN_POINT ( 'NONE',  ( -4.220049686691937474, -10.18810118749999738, 76.93750000204839523 ) ) ;
#20373=CARTESIAN_POINT ( 'NONE',  ( 10.18810118750000093, -4.220049686691933921, 85.18750000204838102 ) ) ;
#20376=AXIS2_PLACEMENT_3D ( 'NONE', #7733, #19405, #48449 ) ;
#20380=CARTESIAN_POINT ( 'NONE',  ( 7.204075437095966983, 7.204075437095967871, 92.59375000204838102 ) ) ;
#20382=VERTEX_POINT ( 'NONE', #61342 ) ;
#20390=CARTESIAN_POINT ( 'NONE',  ( -7.204075437095965206, -7.204075437095968759, 95.21875000204838102 ) ) ;
#20406=CARTESIAN_POINT ( 'NONE',  ( -7.204075437095965206, -7.204075437095968759, 100.8437500020483668 ) ) ;
#20419=SHAPE_REPRESENTATION ( 'square bolt', ( #57354 ), #67028 ) ;
#20425=CARTESIAN_POINT ( 'NONE',  ( 11.00000000000000000, 4.556349186104045934, 111.3437499999999858 ) ) ;
#20429=CARTESIAN_POINT ( 'NONE',  ( -11.00000000000000000, 0.000000000000000000, 101.5000000000000000 ) ) ;
#20433=ORIENTED_EDGE ( 'NONE', *, *, #7424, .T. ) ;
#20434=EDGE_CURVE ( 'NONE', #47217, #50184, #40142, .T. ) ;
#20438=CARTESIAN_POINT ( 'NONE',  ( 7.778174593052021635, 7.778174593052023411, 99.62500000409677625 ) ) ;
#20458=CARTESIAN_POINT ( 'NONE',  ( 10.18810118750000093, -4.220049686691933921, 106.1875000020483810 ) ) ;
#20464=CARTESIAN_POINT ( 'NONE',  ( -4.220049686691935698, 10.18810118749999916, 67.75000000204836681 ) ) ;
#20467=DIRECTION ( 'NONE',  ( -0.000000000000000000, -0.000000000000000000, -1.000000000000000000 ) ) ;
#20476=CARTESIAN_POINT ( 'NONE',  ( -4.220049686691937474, -10.18810118749999738, 113.3125000020483668 ) ) ;
#20481=ORIENTED_EDGE ( 'NONE', *, *, #44070, .F. ) ;
#20492=( BOUNDED_CURVE ( )  B_SPLINE_CURVE ( 2, ( #73986, #62657, #10991, #34024, #1170, #35132, #51716, #35494, #29825 ),
 .UNSPECIFIED., .F., .F. ) 
 B_SPLINE_CURVE_WITH_KNOTS ( ( 3, 2, 2, 2, 3 ),
 ( 0.6176470588235293269, 0.6213235294117646079, 0.6249999999999998890, 0.6286764705882351700, 0.6323529411764704511 ),
 .UNSPECIFIED. ) 
 CURVE ( )  GEOMETRIC_REPRESENTATION_ITEM ( )  RATIONAL_B_SPLINE_CURVE ( ( 1.000000000000002220, 0.9238795325112844070, 1.000000000000000000, 0.9238795325112867385, 1.000000000000000000, 0.9238795325112867385, 1.000000000000000000, 0.9238795325112890700, 0.9999999999999976685 ) ) 
 REPRESENTATION_ITEM ( '' )  );
#20503=CARTESIAN_POINT ( 'NONE',  ( -10.99999999999996625, 4.556349186104079685, 113.5937500040967620 ) ) ;
#20505=ORIENTED_EDGE ( 'NONE', *, *, #44581, .T. ) ;
#20512=FACE_OUTER_BOUND ( 'NONE', #16516, .T. ) ;
#20538=CARTESIAN_POINT ( 'NONE',  ( 11.00000000000000000, 1.347111479062088405E-15, 118.0000000000000000 ) ) ;
#20550=CARTESIAN_POINT ( 'NONE',  ( -7.204075437095965206, -7.204075437095968759, 94.84375000204838102 ) ) ;
#20564=CARTESIAN_POINT ( 'NONE',  ( -4.220049686691935698, 10.18810118749999916, 87.25000000204838102 ) ) ;
#20571=CARTESIAN_POINT ( 'NONE',  ( -4.556349186104048599, -10.99999999999999822, 85.46875000409677625 ) ) ;
#20579=CARTESIAN_POINT ( 'NONE',  ( 4.220049686691934809, 10.18810118749999916, 85.18750000204838102 ) ) ;
#20584=ORIENTED_EDGE ( 'NONE', *, *, #8899, .T. ) ;
#20591=CARTESIAN_POINT ( 'NONE',  ( 11.00000000000000355, -4.556349186104044158, 76.65625000000000000 ) ) ;
#20609=CARTESIAN_POINT ( 'NONE',  ( 11.00000000000005151, 4.556349186103993532, 114.3437500000000142 ) ) ;
#20613=CARTESIAN_POINT ( 'NONE',  ( 2.020667218593132706E-15, -11.00000000000000000, 73.37500000000000000 ) ) ;
#20622=( BOUNDED_CURVE ( )  B_SPLINE_CURVE ( 2, ( #63749, #69416, #22634, #16224, #16595, #45287, #34738, #63372, #46401 ),
 .UNSPECIFIED., .F., .F. ) 
 B_SPLINE_CURVE_WITH_KNOTS ( ( 3, 2, 2, 2, 3 ),
 ( 0.7352941176470587648, 0.7389705882352940458, 0.7426470588235293269, 0.7463235294117646079, 0.7499999999999998890 ),
 .UNSPECIFIED. ) 
 CURVE ( )  GEOMETRIC_REPRESENTATION_ITEM ( )  RATIONAL_B_SPLINE_CURVE ( ( 1.000000000000002220, 0.9238795325112844070, 1.000000000000000000, 0.9238795325112867385, 1.000000000000000000, 0.9238795325112867385, 1.000000000000000000, 0.9238795325112890700, 0.9999999999999976685 ) ) 
 REPRESENTATION_ITEM ( '' )  );
#20625=CARTESIAN_POINT ( 'NONE',  ( 7.778174593052023411, -7.778174593052021635, 115.7500000040967905 ) ) ;
#20632=FACE_OUTER_BOUND ( 'NONE', #66710, .T. ) ;
#20643=CARTESIAN_POINT ( 'NONE',  ( 10.18810118750000093, -4.220049686691933921, 86.68750000204836681 ) ) ;
#20644=CARTESIAN_POINT ( 'NONE',  ( 10.18810118749999916, 4.220049686691935698, 110.5000000020483810 ) ) ;
#20657=CARTESIAN_POINT ( 'NONE',  ( 10.18810118749999916, 1.247682550866122264E-15, 109.2812500020483668 ) ) ;
#20684=CARTESIAN_POINT ( 'NONE',  ( -4.556349186104045934, 11.00000000000000000, 72.71875000000000000 ) ) ;
#20691=EDGE_CURVE ( 'NONE', #53484, #13320, #72557, .T. ) ;
#20692=CARTESIAN_POINT ( 'NONE',  ( 4.556349186104045934, 11.00000000000000000, 83.03124999999998579 ) ) ;
#20695=ORIENTED_EDGE ( 'NONE', *, *, #32311, .F. ) ;
#20697=CARTESIAN_POINT ( 'NONE',  ( -10.18810118749999916, 0.000000000000000000, 79.65625000204836681 ) ) ;
#20700=CARTESIAN_POINT ( 'NONE',  ( -7.778174593052023411, 7.778174593052023411, 89.31249999999998579 ) ) ;
#20704=CARTESIAN_POINT ( 'NONE',  ( -10.99999999999989164, -4.556349186104158733, 83.59375000000000000 ) ) ;
#20717=CARTESIAN_POINT ( 'NONE',  ( 11.00000000000000000, 1.347111479062088405E-15, 99.43750000409677625 ) ) ;
#20723=CARTESIAN_POINT ( 'NONE',  ( -10.99999999999996092, 4.556349186104085902, 112.0937500040967620 ) ) ;
#20726=CARTESIAN_POINT ( 'NONE',  ( -11.00000000000000533, -11.00000000000000355, 20.00000000000000000 ) ) ;
#20728=CARTESIAN_POINT ( 'NONE',  ( -11.00000000000000000, 4.556349186104045934, 79.09375000409676204 ) ) ;
#20740=ORIENTED_EDGE ( 'NONE', *, *, #68045, .T. ) ;
#20743=( BOUNDED_CURVE ( )  B_SPLINE_CURVE ( 2, ( #47568, #23083, #18173, #24191, #6852, #11768, #40811, #11400, #6491 ),
 .UNSPECIFIED., .F., .F. ) 
 B_SPLINE_CURVE_WITH_KNOTS ( ( 3, 2, 2, 2, 3 ),
 ( 0.3088235294117646079, 0.3124999999999998890, 0.3161764705882351700, 0.3198529411764704511, 0.3235294117647057877 ),
 .UNSPECIFIED. ) 
 CURVE ( )  GEOMETRIC_REPRESENTATION_ITEM ( )  RATIONAL_B_SPLINE_CURVE ( ( 1.000000000000002220, 0.9238795325112844070, 1.000000000000000000, 0.9238795325112867385, 1.000000000000000000, 0.9238795325112867385, 1.000000000000000000, 0.9238795325112890700, 0.9999999999999976685 ) ) 
 REPRESENTATION_ITEM ( '' )  );
#20746=DIRECTION ( 'NONE',  ( -0.000000000000000000, -0.000000000000000000, -1.000000000000000000 ) ) ;
#20747=CARTESIAN_POINT ( 'NONE',  ( 1.871523826299183495E-15, -10.18810118749999916, 77.03125000204836681 ) ) ;
#20756=CARTESIAN_POINT ( 'NONE',  ( 4.220049686691941027, -10.18810118749999738, 88.00000000204836681 ) ) ;
#20757=EDGE_LOOP ( 'NONE', ( #42295, #30030, #30272, #23002 ) ) ;
#20758=DIRECTION ( 'NONE',  ( -1.000000000000000000, 0.000000000000000000, 0.000000000000000000 ) ) ;
#20761=CARTESIAN_POINT ( 'NONE',  ( -10.18810118749999916, 0.000000000000000000, 94.65625000204836681 ) ) ;
#20768=CARTESIAN_POINT ( 'NONE',  ( 4.220049686691934809, 10.18810118749999916, 93.06250000204839523 ) ) ;
#20786=CARTESIAN_POINT ( 'NONE',  ( -4.220049686691937474, -10.18810118749999738, 100.9375000020483810 ) ) ;
#20820=CARTESIAN_POINT ( 'NONE',  ( 4.556349186104045934, 11.00000000000000000, 96.71875000409677625 ) ) ;
#20841=CARTESIAN_POINT ( 'NONE',  ( -10.99999999999978861, 4.556349186104256432, 69.90625000000000000 ) ) ;
#20842=CARTESIAN_POINT ( 'NONE',  ( 4.220049686691941027, -10.18810118749999738, 101.5000000020483810 ) ) ;
#20849=CARTESIAN_POINT ( 'NONE',  ( -10.18810118749999916, 0.000000000000000000, 68.03125000204838102 ) ) ;
#20852=CARTESIAN_POINT ( 'NONE',  ( 10.18810118749999916, 4.220049686691935698, 110.5000000020483810 ) ) ;
#20854=ORIENTED_EDGE ( 'NONE', *, *, #3468, .T. ) ;
#20860=( BOUNDED_CURVE ( )  B_SPLINE_CURVE ( 2, ( #73622, #21927, #33652, #38926, #10626, #56657, #21560, #5710, #61927 ),
 .UNSPECIFIED., .F., .F. ) 
 B_SPLINE_CURVE_WITH_KNOTS ( ( 3, 2, 2, 2, 3 ),
 ( 0.5735294117647057321, 0.5772058823529410132, 0.5808823529411764053, 0.5845588235294116863, 0.5882352941176469674 ),
 .UNSPECIFIED. ) 
 CURVE ( )  GEOMETRIC_REPRESENTATION_ITEM ( )  RATIONAL_B_SPLINE_CURVE ( ( 1.000000000000002220, 0.9238795325112844070, 1.000000000000000000, 0.9238795325112867385, 1.000000000000000000, 0.9238795325112867385, 1.000000000000000000, 0.9238795325112890700, 0.9999999999999976685 ) ) 
 REPRESENTATION_ITEM ( '' )  );
#20861=CARTESIAN_POINT ( 'NONE',  ( 10.18810118749999916, 4.220049686691935698, 109.3750000020483810 ) ) ;
#20865=ORIENTED_EDGE ( 'NONE', *, *, #11782, .F. ) ;
#20876=CARTESIAN_POINT ( 'NONE',  ( -10.18810118749999916, 4.220049686691934809, 117.0625000020483668 ) ) ;
#20885=DIRECTION ( 'NONE',  ( -0.000000000000000000, 0.000000000000000000, -1.000000000000000000 ) ) ;
#20889=CARTESIAN_POINT ( 'NONE',  ( -11.00000000000000000, 0.000000000000000000, 88.18750000409677625 ) ) ;
#20893=CARTESIAN_POINT ( 'NONE',  ( -7.778174593052023411, 7.778174593052023411, 107.5000000040967763 ) ) ;
#20904=VECTOR ( 'NONE', #7552, 1000.000000000000000 ) ;
#20926=CARTESIAN_POINT ( 'NONE',  ( 7.204075437095968759, -7.204075437095966983, 90.71875000204838102 ) ) ;
#20940=CARTESIAN_POINT ( 'NONE',  ( -7.204075437095965206, -7.204075437095968759, 81.71875000204836681 ) ) ;
#20942=VERTEX_POINT ( 'NONE', #20126 ) ;
#20953=CARTESIAN_POINT ( 'NONE',  ( -7.204075437095965206, -7.204075437095968759, 81.34375000204838102 ) ) ;
#20980=CARTESIAN_POINT ( 'NONE',  ( 2.020667218593132706E-15, -11.00000000000000000, 92.87499999999998579 ) ) ;
#20988=CARTESIAN_POINT ( 'NONE',  ( 4.556349186104045934, 11.00000000000000000, 69.53124999999998579 ) ) ;
#20997=CARTESIAN_POINT ( 'NONE',  ( 7.778174593052021635, 7.778174593052023411, 108.6250000040967763 ) ) ;
#21008=EDGE_CURVE ( 'NONE', #36810, #46282, #73849, .T. ) ;
#21017=CARTESIAN_POINT ( 'NONE',  ( -7.204075437095965206, -7.204075437095968759, 114.3437500020483810 ) ) ;
#21021=CARTESIAN_POINT ( 'NONE',  ( 11.00000000000010836, -4.556349186103939353, 106.6562500000000000 ) ) ;
#21031=CARTESIAN_POINT ( 'NONE',  ( 7.204075437095968759, -7.204075437095966983, 101.5937500020483668 ) ) ;
#21037=CARTESIAN_POINT ( 'NONE',  ( -11.00000000000000000, 0.000000000000000000, 71.49999999999998579 ) ) ;
#21053=EDGE_LOOP ( 'NONE', ( #25574, #37214, #25366, #3164 ) ) ;
#21058=CARTESIAN_POINT ( 'NONE',  ( -11.00000000000000000, 0.000000000000000000, 70.18750000409676204 ) ) ;
#21074=CARTESIAN_POINT ( 'NONE',  ( 4.220049686691941027, -10.18810118749999738, 83.12500000204836681 ) ) ;
#21077=CARTESIAN_POINT ( 'NONE',  ( 7.778174593052021635, 7.778174593052023411, 88.93749999999998579 ) ) ;
#21102=CARTESIAN_POINT ( 'NONE',  ( 7.778174593052021635, 7.778174593052023411, 111.6250000040967763 ) ) ;
#21107=CARTESIAN_POINT ( 'NONE',  ( -7.778174593052020747, -7.778174593052023411, 79.37500000409677625 ) ) ;
#21123=CARTESIAN_POINT ( 'NONE',  ( -4.220049686691937474, -10.18810118749999738, 75.43750000204836681 ) ) ;
#21125=DIRECTION ( 'NONE',  ( -1.000000000000000000, 0.000000000000000000, 0.000000000000000000 ) ) ;
#21130=CARTESIAN_POINT ( 'NONE',  ( -10.18810118749999916, 0.000000000000000000, 84.53125000204836681 ) ) ;
#21135=CARTESIAN_POINT ( 'NONE',  ( 10.18810118749999916, 4.220049686691935698, 97.00000000204836681 ) ) ;
#21137=ORIENTED_EDGE ( 'NONE', *, *, #60821, .F. ) ;
#21143=CARTESIAN_POINT ( 'NONE',  ( 10.18810118749999916, 4.220049686691935698, 91.37500000204838102 ) ) ;
#21146=EDGE_CURVE ( 'NONE', #1123, #39166, #66127, .T. ) ;
#21157=VERTEX_POINT ( 'NONE', #28406 ) ;
#21160=CARTESIAN_POINT ( 'NONE',  ( -10.18810118749999916, 0.000000000000000000, 100.6562500020483810 ) ) ;
#21163=CARTESIAN_POINT ( 'NONE',  ( -4.556349186104047710, -10.99999999999999822, 109.2812499999999858 ) ) ;
#21193=CARTESIAN_POINT ( 'NONE',  ( 7.778174593052023411, -7.778174593052021635, 97.75000000409677625 ) ) ;
#21196=DIRECTION ( 'NONE',  ( -1.000000000000000000, -1.577021341797097560E-16, -0.000000000000000000 ) ) ;
#21214=CARTESIAN_POINT ( 'NONE',  ( -7.204075437095965206, -7.204075437095968759, 104.2187500020483810 ) ) ;
#21221=B_SPLINE_CURVE_WITH_KNOTS ( 'NONE', 3,
 ( #34225, #40985, #63993, #12308, #58352, #52674, #1010, #23990, #46999, #70031, #18340, #41354, #7022, #30031, #53046, #1379, #40235, #57227, #5539, #28541, #60172, #19805, #64731, #18711, #59447, #36801, #8492, #47731 ),
 .UNSPECIFIED., .F., .F.,
 ( 4, 2, 2, 2, 2, 2, 2, 2, 2, 2, 2, 2, 2, 4 ),
 ( 0.000000000000000000, 0.001421530729010940649, 0.002843061458021881299, 0.005686122916043762597, 0.008529184374065643462, 0.009950715103076584328, 0.01137224583208752346, 0.01279377656109846259, 0.01421530729010940346, 0.01563683801912034085, 0.01705836874813127652, 0.01990143020615315478, 0.02132296093516409738, 0.02274449166417503651 ),
 .UNSPECIFIED. ) ;
#21226=CARTESIAN_POINT ( 'NONE',  ( 10.18810118749999916, 4.220049686691935698, 113.5000000020483810 ) ) ;
#21235=CARTESIAN_POINT ( 'NONE',  ( -10.18810118749999916, 4.220049686691934809, 112.9375000020483810 ) ) ;
#21242=EDGE_CURVE ( 'NONE', #68202, #21157, #14104, .T. ) ;
#21244=CARTESIAN_POINT ( 'NONE',  ( 10.18810118749999916, 4.220049686691935698, 68.87500000204838102 ) ) ;
#21250=ORIENTED_EDGE ( 'NONE', *, *, #38242, .F. ) ;
#21251=CARTESIAN_POINT ( 'NONE',  ( 7.204075437095966983, 7.204075437095967871, 116.5937500020483810 ) ) ;
#21263=CARTESIAN_POINT ( 'NONE',  ( -10.99999999999999822, -4.556349186104053040, 77.59374999999998579 ) ) ;
#21264=CARTESIAN_POINT ( 'NONE',  ( -15.99999999999999645, -16.00000000000000355, 20.00000000000000000 ) ) ;
#21278=CARTESIAN_POINT ( 'NONE',  ( -6.735557395310442023E-16, 11.00000000000000000, 77.31250000409677625 ) ) ;
#21281=CARTESIAN_POINT ( 'NONE',  ( 11.00000000000000000, 1.347111479062088405E-15, 79.74999999999998579 ) ) ;
#21296=CARTESIAN_POINT ( 'NONE',  ( -4.556349186104045934, 11.00000000000000000, 95.21874999999998579 ) ) ;
#21301=CARTESIAN_POINT ( 'NONE',  ( 10.18810118749999916, 4.220049686691935698, 88.00000000204836681 ) ) ;
#21302=CARTESIAN_POINT ( 'NONE',  ( 11.00000000000000000, 1.347111479062088405E-15, 93.24999999999998579 ) ) ;
#21308=ORIENTED_EDGE ( 'NONE', *, *, #69399, .T. ) ;
#21315=CARTESIAN_POINT ( 'NONE',  ( -4.220049686691937474, -10.18810118749999738, 84.81250000204838102 ) ) ;
#21331=CARTESIAN_POINT ( 'NONE',  ( -4.220049686691937474, -10.18810118749999738, 79.93750000204839523 ) ) ;
#21335=EDGE_LOOP ( 'NONE', ( #64573, #54062, #60860, #4540 ) ) ;
#21361=CARTESIAN_POINT ( 'NONE',  ( -10.99999999999999822, -4.556349186104052151, 71.59374999999998579 ) ) ;
#21364=CARTESIAN_POINT ( 'NONE',  ( -11.00000000000000000, 0.000000000000000000, 110.6875000040967763 ) ) ;
#21383=CARTESIAN_POINT ( 'NONE',  ( 11.00000000000000000, 1.347111479062088405E-15, 69.43750000409676204 ) ) ;
#21389=CARTESIAN_POINT ( 'NONE',  ( 7.204075437095966983, 7.204075437095967871, 109.0937500020483810 ) ) ;
#21403=CARTESIAN_POINT ( 'NONE',  ( 10.18810118749999916, 1.247682550866122264E-15, 101.7812500020483810 ) ) ;
#21413=EDGE_LOOP ( 'NONE', ( #22445, #10927, #29720, #28568 ) ) ;
#21426=CARTESIAN_POINT ( 'NONE',  ( -7.204075437095967871, 7.204075437095967871, 82.84375000204838102 ) ) ;
#21444=CARTESIAN_POINT ( 'NONE',  ( -7.204075437095967871, 7.204075437095967871, 73.46875000204838102 ) ) ;
#21447=CARTESIAN_POINT ( 'NONE',  ( 4.556349186104045934, 11.00000000000000000, 87.53125000000000000 ) ) ;
#21452=FACE_OUTER_BOUND ( 'NONE', #29854, .T. ) ;
#21463=LINE ( 'NONE', #26362, #44440 ) ;
#21476=VECTOR ( 'NONE', #3993, 1000.000000000000000 ) ;
#21477=CARTESIAN_POINT ( 'NONE',  ( -11.00000000000000000, 4.556349186104045934, 74.59375000409676204 ) ) ;
#21496=CARTESIAN_POINT ( 'NONE',  ( 10.18810118750000093, -4.220049686691933921, 78.81250000204838102 ) ) ;
#21504=CARTESIAN_POINT ( 'NONE',  ( -4.220049686691935698, 10.18810118749999916, 76.75000000204838102 ) ) ;
#21508=CARTESIAN_POINT ( 'NONE',  ( 10.99999999999989342, 4.556349186104152515, 105.3437499999999858 ) ) ;
#21517=CARTESIAN_POINT ( 'NONE',  ( 10.18810118750000093, -4.220049686691933921, 92.68750000204838102 ) ) ;
#21533=CARTESIAN_POINT ( 'NONE',  ( 10.18810118749999916, 1.247682550866122264E-15, 92.40625000204836681 ) ) ;
#21536=CARTESIAN_POINT ( 'NONE',  ( 7.778174593052023411, -7.778174593052021635, 105.0624999999999858 ) ) ;
#21560=CARTESIAN_POINT ( 'NONE',  ( -7.778174593052020747, -7.778174593052023411, 88.18749999999998579 ) ) ;
#21565=CARTESIAN_POINT ( 'NONE',  ( -7.778174593052020747, -7.778174593052023411, 100.3750000040967763 ) ) ;
#21586=CARTESIAN_POINT ( 'NONE',  ( 7.204075437095966983, 7.204075437095967871, 106.4687500020483810 ) ) ;
#21595=CARTESIAN_POINT ( 'NONE',  ( -4.220049686691937474, -10.18810118749999738, 112.9375000020483810 ) ) ;
#21603=CARTESIAN_POINT ( 'NONE',  ( -10.18810118749999916, 0.000000000000000000, 111.5312500020483668 ) ) ;
#21612=CARTESIAN_POINT ( 'NONE',  ( 7.204075437095968759, -7.204075437095966983, 71.59375000204836681 ) ) ;
#21620=( BOUNDED_CURVE ( )  B_SPLINE_CURVE ( 2, ( #37619, #38363, #56096, #9315, #3655, #9696, #32717, #44392, #20240 ),
 .UNSPECIFIED., .F., .F. ) 
 B_SPLINE_CURVE_WITH_KNOTS ( ( 3, 2, 2, 2, 3 ),
 ( 0.04411764705882355309, 0.04779411764705884802, 0.05147058823529414295, 0.05514705882352943789, 0.05882352941176473976 ),
 .UNSPECIFIED. ) 
 CURVE ( )  GEOMETRIC_REPRESENTATION_ITEM ( )  RATIONAL_B_SPLINE_CURVE ( ( 0.9999999999999995559, 0.9238795325112871826, 1.000000000000000000, 0.9238795325112867385, 1.000000000000000000, 0.9238795325112867385, 1.000000000000000000, 0.9238795325112860723, 1.000000000000000666 ) ) 
 REPRESENTATION_ITEM ( '' )  );
#21622=CARTESIAN_POINT ( 'NONE',  ( 10.18810118749999916, 4.220049686691935698, 113.5000000020483810 ) ) ;
#21630=EDGE_CURVE ( 'NONE', #45401, #7250, #70967, .T. ) ;
#21635=CARTESIAN_POINT ( 'NONE',  ( 4.556349186104052151, -10.99999999999999822, 91.46874999999998579 ) ) ;
#21644=CARTESIAN_POINT ( 'NONE',  ( 11.00000000000021494, -4.556349186103832771, 82.84375000409677625 ) ) ;
#21670=CARTESIAN_POINT ( 'NONE',  ( -4.220049686691935698, 10.18810118749999916, 89.87500000204836681 ) ) ;
#21671=DIRECTION ( 'NONE',  ( -1.000000000000000000, 0.000000000000000000, 0.000000000000000000 ) ) ;
#21682=CARTESIAN_POINT ( 'NONE',  ( -7.204075437095965206, -7.204075437095968759, 80.21875000204836681 ) ) ;
#21689=CARTESIAN_POINT ( 'NONE',  ( 11.00000000000000000, 1.347111479062088405E-15, 85.93750000409677625 ) ) ;
#21696=CARTESIAN_POINT ( 'NONE',  ( -4.220049686691937474, -10.18810118749999738, 76.93750000204839523 ) ) ;
#21725=CARTESIAN_POINT ( 'NONE',  ( -4.556349186104048599, -10.99999999999999822, 115.4687500040967763 ) ) ;
#21729=CARTESIAN_POINT ( 'NONE',  ( 2.020667218593132706E-15, -11.00000000000000000, 70.37500000000000000 ) ) ;
#21757=CARTESIAN_POINT ( 'NONE',  ( -4.220049686691935698, 10.18810118749999916, 104.8750000020483668 ) ) ;
#21772=CARTESIAN_POINT ( 'NONE',  ( -4.220049686691935698, 10.18810118749999916, 103.7500000020483668 ) ) ;
#21789=CARTESIAN_POINT ( 'NONE',  ( -6.238412754330611322E-16, 10.18810118749999916, 81.15625000204838102 ) ) ;
#21797=LINE ( 'NONE', #67469, #14939 ) ;
#21808=CARTESIAN_POINT ( 'NONE',  ( -4.220049686691937474, -10.18810118749999738, 75.43750000204836681 ) ) ;
#21811=CARTESIAN_POINT ( 'NONE',  ( -11.00000000000000000, 0.000000000000000000, 88.00000000000000000 ) ) ;
#21825=CARTESIAN_POINT ( 'NONE',  ( -7.778174593052020747, -7.778174593052023411, 98.87500000409676204 ) ) ;
#21841=CARTESIAN_POINT ( 'NONE',  ( -4.556349186104047710, -10.99999999999999822, 71.96875000409677625 ) ) ;
#21861=CARTESIAN_POINT ( 'NONE',  ( -10.18810118749999738, -4.220049686691941915, 70.75000000204836681 ) ) ;
#21864=DIRECTION ( 'NONE',  ( -1.000000000000000000, 0.000000000000000000, 0.000000000000000000 ) ) ;
#21872=CARTESIAN_POINT ( 'NONE',  ( 4.220049686691934809, 10.18810118749999916, 81.06250000204836681 ) ) ;
#21874=ADVANCED_FACE ( 'NONE', ( #34375 ), #34747, .T. ) ;
#21884=CARTESIAN_POINT ( 'NONE',  ( 10.18810118749999916, 1.247682550866122264E-15, 91.28125000204836681 ) ) ;
#21890=VERTEX_POINT ( 'NONE', #29062 ) ;
#21893=CARTESIAN_POINT ( 'NONE',  ( 4.556349186104052151, -10.99999999999999822, 96.15625000409677625 ) ) ;
#21900=CARTESIAN_POINT ( 'NONE',  ( -6.238412754330611322E-16, 10.18810118749999916, 94.28125000204836681 ) ) ;
#21903=CARTESIAN_POINT ( 'NONE',  ( 7.778174593052023411, -7.778174593052021635, 108.0624999999999858 ) ) ;
#21911=EDGE_CURVE ( 'NONE', #32460, #70626, #26690, .T. ) ;
#21927=CARTESIAN_POINT ( 'NONE',  ( 11.00000000000010836, -4.556349186103939353, 88.65624999999998579 ) ) ;
#21933=CARTESIAN_POINT ( 'NONE',  ( 11.00000000000000355, -4.556349186104045046, 90.34375000409677625 ) ) ;
#21946=CARTESIAN_POINT ( 'NONE',  ( -11.00000000000000000, 0.000000000000000000, 103.1875000040967763 ) ) ;
#21956=CARTESIAN_POINT ( 'NONE',  ( 4.220049686691934809, 10.18810118749999916, 97.56250000204836681 ) ) ;
#21967=CARTESIAN_POINT ( 'NONE',  ( -7.204075437095965206, -7.204075437095968759, 111.3437500020483810 ) ) ;
#21974=CARTESIAN_POINT ( 'NONE',  ( 11.00000000000000000, 1.347111479062088405E-15, 93.43750000409677625 ) ) ;
#21975=CARTESIAN_POINT ( 'NONE',  ( -4.220049686691937474, -10.18810118749999738, 110.3125000020483810 ) ) ;
#21984=EDGE_CURVE ( 'NONE', #46282, #5598, #2525, .T. ) ;
#21995=CARTESIAN_POINT ( 'NONE',  ( -10.18810118749999738, -4.220049686691941915, 109.7500000020483810 ) ) ;
#21996=CARTESIAN_POINT ( 'NONE',  ( -11.00000000000000000, 4.556349186104045934, 97.09375000409680467 ) ) ;
#22008=CARTESIAN_POINT ( 'NONE',  ( -11.00000000000010303, -4.556349186103947346, 94.09375000000000000 ) ) ;
#22013=CARTESIAN_POINT ( 'NONE',  ( 2.020667218593132706E-15, -11.00000000000000000, 110.8749999999999858 ) ) ;
#22034=VERTEX_POINT ( 'NONE', #33084 ) ;
#22040=CARTESIAN_POINT ( 'NONE',  ( 1.871523826299183495E-15, -10.18810118749999916, 90.53125000204836681 ) ) ;
#22044=CARTESIAN_POINT ( 'NONE',  ( -10.18810118749999916, 0.000000000000000000, 117.5312500020483810 ) ) ;
#22052=CARTESIAN_POINT ( 'NONE',  ( 7.204075437095966983, 7.204075437095967871, 83.96875000204836681 ) ) ;
#22065=CARTESIAN_POINT ( 'NONE',  ( -10.18810118749999916, 4.220049686691934809, 76.56250000204836681 ) ) ;
#22102=CARTESIAN_POINT ( 'NONE',  ( -11.00000000000000000, 4.556349186104045934, 71.40624999999997158 ) ) ;
#22128=CARTESIAN_POINT ( 'NONE',  ( -10.18810118749999916, 4.220049686691934809, 108.0625000020483810 ) ) ;
#22131=CARTESIAN_POINT ( 'NONE',  ( -11.00000000000000000, 0.000000000000000000, 106.0000000000000000 ) ) ;
#22136=ORIENTED_EDGE ( 'NONE', *, *, #7336, .T. ) ;
#22142=CARTESIAN_POINT ( 'NONE',  ( 10.18810118749999916, 1.247682550866122264E-15, 100.2812500020483810 ) ) ;
#22146=DIRECTION ( 'NONE',  ( -0.000000000000000000, -0.000000000000000000, -1.000000000000000000 ) ) ;
#22164=AXIS2_PLACEMENT_3D ( 'NONE', #7698, #23931, #46940 ) ;
#22165=CARTESIAN_POINT ( 'NONE',  ( -7.204075437095967871, 7.204075437095967871, 79.84375000204838102 ) ) ;
#22178=PRODUCT_CONTEXT ( 'NONE', #58288, 'mechanical' ) ;
#22184=CARTESIAN_POINT ( 'NONE',  ( -4.220049686691937474, -10.18810118749999738, 73.93750000204838102 ) ) ;
#22187=CARTESIAN_POINT ( 'NONE',  ( -11.00000000000000000, 4.556349186104045934, 86.40624999999998579 ) ) ;
#22200=CARTESIAN_POINT ( 'NONE',  ( 2.020667218593132706E-15, -11.00000000000000000, 99.06250000409677625 ) ) ;
#22209=ORIENTED_EDGE ( 'NONE', *, *, #22786, .T. ) ;
#22213=CARTESIAN_POINT ( 'NONE',  ( -10.99999999999999822, -4.556349186104052151, 74.78125000409679046 ) ) ;
#22227=CARTESIAN_POINT ( 'NONE',  ( -4.220049686691935698, 10.18810118749999916, 117.2500000020483952 ) ) ;
#22231=CARTESIAN_POINT ( 'NONE',  ( -7.204075437095967871, 7.204075437095967871, 70.46875000204836681 ) ) ;
#22238=CARTESIAN_POINT ( 'NONE',  ( 10.18810118749999916, 1.247682550866122264E-15, 77.78125000204836681 ) ) ;
#22262=SHAPE_REPRESENTATION_RELATIONSHIP ( 'NONE' , 'NONE' ,  #20419, #22811 ) ;
#22270=CARTESIAN_POINT ( 'NONE',  ( 7.204075437095968759, -7.204075437095966983, 95.21875000204838102 ) ) ;
#22273=CARTESIAN_POINT ( 'NONE',  ( 2.020667218593132706E-15, -11.00000000000000000, 107.8750000000000000 ) ) ;
#22293=CYLINDRICAL_SURFACE ( 'NONE', #56393, 11.00000000000000000 ) ;
#22297=ORIENTED_EDGE ( 'NONE', *, *, #61774, .F. ) ;
#22300=CARTESIAN_POINT ( 'NONE',  ( 2.020667218593132706E-15, -11.00000000000000000, 94.56250000409677625 ) ) ;
#22321=CARTESIAN_POINT ( 'NONE',  ( 7.204075437095968759, -7.204075437095966983, 95.59375000204838102 ) ) ;
#22329=CARTESIAN_POINT ( 'NONE',  ( -10.18810118749999916, 0.000000000000000000, 105.1562500020483810 ) ) ;
#22337=CARTESIAN_POINT ( 'NONE',  ( 10.18810118750000093, -4.220049686691933921, 107.6875000020483810 ) ) ;
#22341=LINE ( 'NONE', #39344, #68650 ) ;
#22354=CARTESIAN_POINT ( 'NONE',  ( -7.204075437095967871, 7.204075437095967871, 109.4687500020483810 ) ) ;
#22355=CARTESIAN_POINT ( 'NONE',  ( 11.00000000000000000, 1.347111479062088405E-15, 96.43750000409677625 ) ) ;
#22363=DIRECTION ( 'NONE',  ( -0.000000000000000000, -0.000000000000000000, -1.000000000000000000 ) ) ;
#22379=DIRECTION ( 'NONE',  ( -0.000000000000000000, -0.000000000000000000, -1.000000000000000000 ) ) ;
#22383=CARTESIAN_POINT ( 'NONE',  ( 2.020667218593132706E-15, -11.00000000000000000, 111.0625000040967763 ) ) ;
#22389=( BOUNDED_CURVE ( )  B_SPLINE_CURVE ( 2, ( #6392, #41083, #12765, #371, #46365, #35797, #11663, #16943, #6754 ),
 .UNSPECIFIED., .F., .F. ) 
 B_SPLINE_CURVE_WITH_KNOTS ( ( 3, 2, 2, 2, 3 ),
 ( 0.1764705882352942401, 0.1801470588235295212, 0.1838235294117648300, 0.1875000000000001388, 0.1911764705882354198 ),
 .UNSPECIFIED. ) 
 CURVE ( )  GEOMETRIC_REPRESENTATION_ITEM ( )  RATIONAL_B_SPLINE_CURVE ( ( 0.9999999999999976685, 0.9238795325112890700, 1.000000000000000000, 0.9238795325112867385, 1.000000000000000000, 0.9238795325112867385, 1.000000000000000000, 0.9238795325112838519, 1.000000000000002887 ) ) 
 REPRESENTATION_ITEM ( '' )  );
#22405=CARTESIAN_POINT ( 'NONE',  ( 10.18810118750000093, -4.220049686691933921, 90.81250000204838102 ) ) ;
#22419=CARTESIAN_POINT ( 'NONE',  ( 10.18810118750000093, -4.220049686691933033, 80.68750000204836681 ) ) ;
#22433=CARTESIAN_POINT ( 'NONE',  ( -4.220049686691935698, 10.18810118749999916, 74.87500000204836681 ) ) ;
#22445=ORIENTED_EDGE ( 'NONE', *, *, #69873, .F. ) ;
#22483=CARTESIAN_POINT ( 'NONE',  ( 16.00000000000000711, -16.00000000000000000, 20.00000000000000000 ) ) ;
#22495=CARTESIAN_POINT ( 'NONE',  ( 7.204075437095968759, -7.204075437095966983, 110.2187500020483810 ) ) ;
#22499=CARTESIAN_POINT ( 'NONE',  ( 2.020667218593132706E-15, -11.00000000000000000, 97.37499999999998579 ) ) ;
#22512=CARTESIAN_POINT ( 'NONE',  ( 10.18810118750000093, -4.220049686691933033, 98.68750000204838102 ) ) ;
#22516=ORIENTED_EDGE ( 'NONE', *, *, #21911, .F. ) ;
#22526=CARTESIAN_POINT ( 'NONE',  ( -6.238412754330611322E-16, 10.18810118749999916, 95.78125000204836681 ) ) ;
#22537=CARTESIAN_POINT ( 'NONE',  ( -6.238412754330611322E-16, 10.18810118749999916, 82.65625000204838102 ) ) ;
#22557=CARTESIAN_POINT ( 'NONE',  ( 7.204075437095966983, 7.204075437095967871, 76.09375000204838102 ) ) ;
#22560=CARTESIAN_POINT ( 'NONE',  ( -7.778174593052023411, 7.778174593052023411, 80.31249999999998579 ) ) ;
#22588=CARTESIAN_POINT ( 'NONE',  ( 11.00000000000000000, 1.347111479062088405E-15, 76.93750000409677625 ) ) ;
#22601=CARTESIAN_POINT ( 'NONE',  ( 1.871523826299183495E-15, -10.18810118749999916, 116.4062500020483810 ) ) ;
#22605=CARTESIAN_POINT ( 'NONE',  ( -7.204075437095967871, 7.204075437095967871, 71.96875000204836681 ) ) ;
#22617=AXIS2_PLACEMENT_3D ( 'NONE', #61187, #71740, #20055 ) ;
#22634=CARTESIAN_POINT ( 'NONE',  ( -7.778174593052023411, 7.778174593052023411, 79.00000000409676204 ) ) ;
#22641=CARTESIAN_POINT ( 'NONE',  ( -10.18810118749999738, -4.220049686691941915, 94.75000000204838102 ) ) ;
#22644=CARTESIAN_POINT ( 'NONE',  ( 4.556349186104051263, -10.99999999999999822, 100.4687500000000000 ) ) ;
#22647=CARTESIAN_POINT ( 'NONE',  ( 11.00000000000003908, 4.556349186104006854, 113.0312500040967905 ) ) ;
#22676=CARTESIAN_POINT ( 'NONE',  ( -11.00000000000000000, 0.000000000000000000, 89.68750000409677625 ) ) ;
#22690=ORIENTED_EDGE ( 'NONE', *, *, #81, .F. ) ;
#22700=CARTESIAN_POINT ( 'NONE',  ( -10.18810118749999916, 0.000000000000000000, 95.03125000204836681 ) ) ;
#22708=CARTESIAN_POINT ( 'NONE',  ( 7.204075437095966983, 7.204075437095967871, 107.5937500020483810 ) ) ;
#22717=CARTESIAN_POINT ( 'NONE',  ( -4.220049686691937474, -10.18810118749999738, 102.8125000020483952 ) ) ;
#22733=CARTESIAN_POINT ( 'NONE',  ( -4.220049686691935698, 10.18810118749999916, 109.3750000020483810 ) ) ;
#22742=CARTESIAN_POINT ( 'NONE',  ( -11.00000000000000000, 0.000000000000000000, 77.49999999999998579 ) ) ;
#22758=EDGE_CURVE ( 'NONE', #69783, #26210, #14474, .T. ) ;
#22760=CARTESIAN_POINT ( 'NONE',  ( -10.99999999999999822, -4.556349186104052151, 109.2812500040967620 ) ) ;
#22775=CARTESIAN_POINT ( 'NONE',  ( -4.556349186104045934, 11.00000000000000000, 116.2187500000000000 ) ) ;
#22781=CARTESIAN_POINT ( 'NONE',  ( -4.220049686691937474, -10.18810118749999738, 84.43750000204838102 ) ) ;
#22786=EDGE_CURVE ( 'NONE', #68143, #34951, #44287, .T. ) ;
#22787=CARTESIAN_POINT ( 'NONE',  ( 4.220049686691941027, -10.18810118749999738, 116.5000000020483810 ) ) ;
#22788=VERTEX_POINT ( 'NONE', #38638 ) ;
#22790=CARTESIAN_POINT ( 'NONE',  ( 4.556349186104045934, 11.00000000000000000, 108.7187500040967763 ) ) ;
#22795=CARTESIAN_POINT ( 'NONE',  ( 7.204075437095966983, 7.204075437095967871, 74.96875000204836681 ) ) ;
#22808=CARTESIAN_POINT ( 'NONE',  ( -4.220049686691935698, 10.18810118749999916, 77.87500000204838102 ) ) ;
#22811=ADVANCED_BREP_SHAPE_REPRESENTATION ( '', ( #17043, #57354 ), #67028 ) ;
#22822=CARTESIAN_POINT ( 'NONE',  ( -7.778174593052020747, -7.778174593052023411, 74.87500000409677625 ) ) ;
#22824=VERTEX_POINT ( 'NONE', #25424 ) ;
#22846=DIRECTION ( 'NONE',  ( 0.000000000000000000, 1.000000000000000000, 0.000000000000000000 ) ) ;
#22847=CARTESIAN_POINT ( 'NONE',  ( 7.778174593052023411, -7.778174593052021635, 90.06249999999998579 ) ) ;
#22860=ADVANCED_FACE ( 'NONE', ( #14848 ), #49186, .T. ) ;
#22881=CARTESIAN_POINT ( 'NONE',  ( 10.18810118749999916, 1.247682550866122264E-15, 107.4062500020483668 ) ) ;
#22892=EDGE_CURVE ( 'NONE', #18846, #11062, #60886, .T. ) ;
#22898=CARTESIAN_POINT ( 'NONE',  ( 4.220049686691934809, 10.18810118749999916, 96.06250000204836681 ) ) ;
#22911=CARTESIAN_POINT ( 'NONE',  ( -10.18810118749999738, -4.220049686691941915, 96.25000000204838102 ) ) ;
#22921=CARTESIAN_POINT ( 'NONE',  ( 7.204075437095968759, -7.204075437095966983, 82.09375000204838102 ) ) ;
#22928=CARTESIAN_POINT ( 'NONE',  ( -7.778174593052020747, -7.778174593052023411, 92.87500000409677625 ) ) ;
#22932=EDGE_CURVE ( 'NONE', #34951, #56815, #58447, .T. ) ;
#22944=CARTESIAN_POINT ( 'NONE',  ( -7.204075437095967871, 7.204075437095967871, 74.96875000204836681 ) ) ;
#22947=CARTESIAN_POINT ( 'NONE',  ( 2.020667218593132706E-15, -11.00000000000000000, 80.87499999999998579 ) ) ;
#22969=DIRECTION ( 'NONE',  ( -0.000000000000000000, -0.000000000000000000, -1.000000000000000000 ) ) ;
#22970=( BOUNDED_CURVE ( )  B_SPLINE_CURVE ( 2, ( #49219, #26578, #62401, #21296, #56025, #67707, #44320, #26957, #72230 ),
 .UNSPECIFIED., .F., .F. ) 
 B_SPLINE_CURVE_WITH_KNOTS ( ( 3, 2, 2, 2, 3 ),
 ( 0.4411764705882353366, 0.4448529411764706176, 0.4485294117647059542, 0.4522058823529412352, 0.4558823529411765163 ),
 .UNSPECIFIED. ) 
 CURVE ( )  GEOMETRIC_REPRESENTATION_ITEM ( )  RATIONAL_B_SPLINE_CURVE ( ( 0.9999999999999988898, 0.9238795325112878487, 1.000000000000000000, 0.9238795325112867385, 1.000000000000000000, 0.9238795325112867385, 1.000000000000000000, 0.9238795325112856283, 1.000000000000001110 ) ) 
 REPRESENTATION_ITEM ( '' )  );
#22976=CARTESIAN_POINT ( 'NONE',  ( 11.00000000000000000, 4.556349186104045934, 72.53125000409676204 ) ) ;
#22989=CARTESIAN_POINT ( 'NONE',  ( 4.220049686691941027, -10.18810118749999738, 116.5000000020483810 ) ) ;
#22993=CARTESIAN_POINT ( 'NONE',  ( 7.204075437095968759, -7.204075437095966983, 71.21875000204836681 ) ) ;
#23002=ORIENTED_EDGE ( 'NONE', *, *, #51992, .F. ) ;
#23028=CARTESIAN_POINT ( 'NONE',  ( -4.220049686691935698, 10.18810118749999916, 94.37500000204839523 ) ) ;
#23030=CARTESIAN_POINT ( 'NONE',  ( 7.778174593052023411, -7.778174593052021635, 99.06250000000000000 ) ) ;
#23057=CARTESIAN_POINT ( 'NONE',  ( -4.556349186104047710, -10.99999999999999822, 92.96875000409676204 ) ) ;
#23080=CARTESIAN_POINT ( 'NONE',  ( 10.18810118749999916, 1.247682550866122264E-15, 100.2812500020483810 ) ) ;
#23083=CARTESIAN_POINT ( 'NONE',  ( 11.00000000000010836, -4.556349186103939353, 100.8437500040967763 ) ) ;
#23087=CARTESIAN_POINT ( 'NONE',  ( 7.204075437095968759, -7.204075437095966983, 105.7187500020483810 ) ) ;
#23096=CARTESIAN_POINT ( 'NONE',  ( -7.204075437095965206, -7.204075437095968759, 105.7187500020483810 ) ) ;
#23098=CARTESIAN_POINT ( 'NONE',  ( 11.00000000000010658, 4.556349186103942017, 75.34374999999998579 ) ) ;
#23102=EDGE_CURVE ( 'NONE', #70626, #34562, #63269, .T. ) ;
#23111=CARTESIAN_POINT ( 'NONE',  ( 7.204075437095966983, 7.204075437095967871, 112.0937500020483810 ) ) ;
#23129=CARTESIAN_POINT ( 'NONE',  ( -7.778174593052023411, 7.778174593052023411, 73.00000000409677625 ) ) ;
#23130=CARTESIAN_POINT ( 'NONE',  ( -7.778174593052023411, 7.778174593052023411, 117.8125000000000000 ) ) ;
#23141=CARTESIAN_POINT ( 'NONE',  ( 11.00000000000000000, 4.556349186104045934, 108.5312500040967905 ) ) ;
#23145=CYLINDRICAL_SURFACE ( 'NONE', #5302, 11.00000000000000000 ) ;
#23156=CARTESIAN_POINT ( 'NONE',  ( -6.735557395310442023E-16, 11.00000000000000000, 116.1249999999999858 ) ) ;
#23162=CARTESIAN_POINT ( 'NONE',  ( -4.220049686691937474, -10.18810118749999738, 81.43750000204836681 ) ) ;
#23166=CARTESIAN_POINT ( 'NONE',  ( -4.220049686691937474, -10.18810118749999738, 116.3125000020483668 ) ) ;
#23174=CARTESIAN_POINT ( 'NONE',  ( -4.220049686691935698, 10.18810118749999916, 75.25000000204836681 ) ) ;
#23191=CARTESIAN_POINT ( 'NONE',  ( 7.204075437095966983, 7.204075437095967871, 71.59375000204836681 ) ) ;
#23232=ORIENTED_EDGE ( 'NONE', *, *, #40236, .T. ) ;
#23255=CARTESIAN_POINT ( 'NONE',  ( 4.220049686691934809, 10.18810118749999916, 101.6875000020483810 ) ) ;
#23271=CARTESIAN_POINT ( 'NONE',  ( 4.220049686691941027, -10.18810118749999738, 92.50000000204838102 ) ) ;
#23275=DIRECTION ( 'NONE',  ( -0.000000000000000000, -0.000000000000000000, -1.000000000000000000 ) ) ;
#23283=CARTESIAN_POINT ( 'NONE',  ( -4.220049686691935698, 10.18810118749999916, 88.37500000204839523 ) ) ;
#23293=CARTESIAN_POINT ( 'NONE',  ( -10.18810118749999738, -4.220049686691941915, 77.12500000204838102 ) ) ;
#23303=CARTESIAN_POINT ( 'NONE',  ( 7.778174593052023411, -7.778174593052021635, 88.75000000409677625 ) ) ;
#23312=CARTESIAN_POINT ( 'NONE',  ( -7.204075437095965206, -7.204075437095968759, 69.34375000204836681 ) ) ;
#23315=CARTESIAN_POINT ( 'NONE',  ( -4.556349186104045934, 11.00000000000000000, 84.71874999999998579 ) ) ;
#23339=CARTESIAN_POINT ( 'NONE',  ( -11.00000000000010303, -4.556349186103947346, 74.59374999999997158 ) ) ;
#23341=CARTESIAN_POINT ( 'NONE',  ( -11.00000000000000000, 0.000000000000000000, 116.4999999999999858 ) ) ;
#23343=CARTESIAN_POINT ( 'NONE',  ( 11.00000000000000000, 1.347111479062088405E-15, 67.93750000409676204 ) ) ;
#23354=CARTESIAN_POINT ( 'NONE',  ( 10.18810118749999916, 4.220049686691935698, 115.3750000020483810 ) ) ;
#23358=CARTESIAN_POINT ( 'NONE',  ( -7.204075437095965206, -7.204075437095968759, 72.34375000204836681 ) ) ;
#23387=DIRECTION ( 'NONE',  ( 0.000000000000000000, 0.000000000000000000, 1.000000000000000000 ) ) ;
#23394=CARTESIAN_POINT ( 'NONE',  ( -10.18810118749999738, -4.220049686691941915, 88.75000000204836681 ) ) ;
#23397=CARTESIAN_POINT ( 'NONE',  ( 7.778174593052021635, 7.778174593052023411, 102.4374999999999858 ) ) ;
#23427=CARTESIAN_POINT ( 'NONE',  ( 11.00000000000000000, 1.347111479062088405E-15, 91.93750000409677625 ) ) ;
#23429=CARTESIAN_POINT ( 'NONE',  ( 2.020667218593132706E-15, -11.00000000000000000, 111.0625000040967763 ) ) ;
#23430=LINE ( 'NONE', #36243, #72009 ) ;
#23448=FACE_OUTER_BOUND ( 'NONE', #37029, .T. ) ;
#23451=CARTESIAN_POINT ( 'NONE',  ( -10.18810118749999916, 0.000000000000000000, 99.53125000204838102 ) ) ;
#23458=CARTESIAN_POINT ( 'NONE',  ( -6.238412754330611322E-16, 10.18810118749999916, 109.2812500020483668 ) ) ;
#23465=CARTESIAN_POINT ( 'NONE',  ( 7.778174593052023411, -7.778174593052021635, 76.75000000409676204 ) ) ;
#23468=CARTESIAN_POINT ( 'NONE',  ( -6.238412754330611322E-16, 10.18810118749999916, 102.1562500020483810 ) ) ;
#23474=CARTESIAN_POINT ( 'NONE',  ( 11.00000000000000355, -4.556349186104044158, 81.15625000000000000 ) ) ;
#23482=CARTESIAN_POINT ( 'NONE',  ( 10.18810118749999916, 4.220049686691935698, 101.5000000020483668 ) ) ;
#23492=( BOUNDED_CURVE ( )  B_SPLINE_CURVE ( 2, ( #69295, #52690, #40624, #68919, #63624, #58000, #40250, #656, #41369 ),
 .UNSPECIFIED., .F., .F. ) 
 B_SPLINE_CURVE_WITH_KNOTS ( ( 3, 2, 2, 2, 3 ),
 ( 0.3235294117647057877, 0.3272058823529410687, 0.3308823529411763498, 0.3345588235294116308, 0.3382352941176469674 ),
 .UNSPECIFIED. ) 
 CURVE ( )  GEOMETRIC_REPRESENTATION_ITEM ( )  RATIONAL_B_SPLINE_CURVE ( ( 1.000000000000002220, 0.9238795325112844070, 1.000000000000000000, 0.9238795325112867385, 1.000000000000000000, 0.9238795325112867385, 1.000000000000000000, 0.9238795325112890700, 0.9999999999999976685 ) ) 
 REPRESENTATION_ITEM ( '' )  );
#23500=CARTESIAN_POINT ( 'NONE',  ( 7.778174593052021635, 7.778174593052023411, 117.4375000000000000 ) ) ;
#23510=CARTESIAN_POINT ( 'NONE',  ( -7.778174593052020747, -7.778174593052023411, 107.8750000040967763 ) ) ;
#23515=CARTESIAN_POINT ( 'NONE',  ( -11.00000000000000000, 0.000000000000000000, 107.6875000040967763 ) ) ;
#23535=CARTESIAN_POINT ( 'NONE',  ( -7.204075437095965206, -7.204075437095968759, 85.84375000204836681 ) ) ;
#23539=CARTESIAN_POINT ( 'NONE',  ( 1.871523826299183495E-15, -10.18810118749999916, 113.4062500020483810 ) ) ;
#23546=CARTESIAN_POINT ( 'NONE',  ( 7.204075437095966983, 7.204075437095967871, 77.96875000204836681 ) ) ;
#23559=CARTESIAN_POINT ( 'NONE',  ( 7.204075437095966983, 7.204075437095967871, 70.09375000204836681 ) ) ;
#23571=CARTESIAN_POINT ( 'NONE',  ( -7.778174593052023411, 7.778174593052023411, 94.00000000409677625 ) ) ;
#23589=CARTESIAN_POINT ( 'NONE',  ( -11.00000000000000000, 0.000000000000000000, 104.6875000040967763 ) ) ;
#23598=CARTESIAN_POINT ( 'NONE',  ( 11.00000000000000000, 1.347111479062088405E-15, 106.7500000000000000 ) ) ;
#23608=EDGE_CURVE ( 'NONE', #8912, #30991, #38815, .T. ) ;
#23628=CARTESIAN_POINT ( 'NONE',  ( -4.220049686691937474, -10.18810118749999738, 100.9375000020483810 ) ) ;
#23632=CARTESIAN_POINT ( 'NONE',  ( 10.99999999999999467, 11.00000000000000355, 41.99999999999999289 ) ) ;
#23639=ADVANCED_FACE ( 'NONE', ( #32343 ), #11709, .T. ) ;
#23646=CARTESIAN_POINT ( 'NONE',  ( -4.220049686691935698, 10.18810118749999916, 94.75000000204838102 ) ) ;
#23648=ORIENTED_EDGE ( 'NONE', *, *, #32311, .T. ) ;
#23652=CARTESIAN_POINT ( 'NONE',  ( 7.204075437095966983, 7.204075437095967871, 80.96875000204836681 ) ) ;
#23661=CARTESIAN_POINT ( 'NONE',  ( -10.18810118749999916, 4.220049686691934809, 88.56250000204836681 ) ) ;
#23669=CARTESIAN_POINT ( 'NONE',  ( -4.220049686691937474, -10.18810118749999738, 74.31250000204836681 ) ) ;
#23684=CARTESIAN_POINT ( 'NONE',  ( 1.871523826299183495E-15, -10.18810118749999916, 68.03125000204838102 ) ) ;
#23687=CARTESIAN_POINT ( 'NONE',  ( 11.00000000000000000, 1.347111479062088405E-15, 85.75000000000000000 ) ) ;
#23711=CARTESIAN_POINT ( 'NONE',  ( 10.99999999999989697, -4.556349186104149851, 75.15624999999998579 ) ) ;
#23712=CARTESIAN_POINT ( 'NONE',  ( -7.778174593052020747, -7.778174593052023411, 116.6875000000000000 ) ) ;
#23714=CARTESIAN_POINT ( 'NONE',  ( -11.00000000000000000, 0.000000000000000000, 68.68750000409676204 ) ) ;
#23727=CARTESIAN_POINT ( 'NONE',  ( -6.238412754330611322E-16, 10.18810118749999916, 115.6562500020483810 ) ) ;
#23761=CARTESIAN_POINT ( 'NONE',  ( 11.00000000000005329, -4.556349186103991755, 99.15624999999998579 ) ) ;
#23762=ORIENTED_EDGE ( 'NONE', *, *, #63309, .T. ) ;
#23767=CARTESIAN_POINT ( 'NONE',  ( -7.204075437095967871, 7.204075437095967871, 83.96875000204836681 ) ) ;
#23770=CARTESIAN_POINT ( 'NONE',  ( 7.778174593052021635, 7.778174593052023411, 103.9374999999999858 ) ) ;
#23803=CARTESIAN_POINT ( 'NONE',  ( 7.778174593052023411, -7.778174593052021635, 84.25000000409677625 ) ) ;
#23811=CIRCLE ( 'NONE', #22617, 11.00000000000000000 ) ;
#23826=CARTESIAN_POINT ( 'NONE',  ( -10.18810118749999916, 0.000000000000000000, 90.53125000204836681 ) ) ;
#23827=ORIENTED_EDGE ( 'NONE', *, *, #73564, .F. ) ;
#23828=EDGE_CURVE ( 'NONE', #46063, #8912, #26232, .T. ) ;
#23833=VERTEX_POINT ( 'NONE', #47628 ) ;
#23834=CARTESIAN_POINT ( 'NONE',  ( 10.18810118749999916, 1.247682550866122264E-15, 107.4062500020483668 ) ) ;
#23843=CARTESIAN_POINT ( 'NONE',  ( -7.204075437095965206, -7.204075437095968759, 104.2187500020483810 ) ) ;
#23854=CARTESIAN_POINT ( 'NONE',  ( -11.00000000000010658, 4.556349186103942017, 84.90624999999998579 ) ) ;
#23856=ORIENTED_EDGE ( 'NONE', *, *, #34457, .T. ) ;
#23858=CARTESIAN_POINT ( 'NONE',  ( 4.220049686691934809, 10.18810118749999916, 104.6875000020483810 ) ) ;
#23869=DIRECTION ( 'NONE',  ( -1.000000000000000000, -1.577021341797097560E-16, -0.000000000000000000 ) ) ;
#23876=CARTESIAN_POINT ( 'NONE',  ( -4.220049686691937474, -10.18810118749999738, 71.31250000204836681 ) ) ;
#23888=CARTESIAN_POINT ( 'NONE',  ( 7.778174593052021635, 7.778174593052023411, 104.1250000040967763 ) ) ;
#23890=CARTESIAN_POINT ( 'NONE',  ( 11.00000000000000000, 1.347111479062088405E-15, 70.74999999999998579 ) ) ;
#23904=CARTESIAN_POINT ( 'NONE',  ( 0.000000000000000000, 0.000000000000000000, 118.0000000000000000 ) ) ;
#23906=CARTESIAN_POINT ( 'NONE',  ( 1.871523826299183495E-15, -10.18810118749999916, 81.53125000204838102 ) ) ;
#23910=CARTESIAN_POINT ( 'NONE',  ( -10.18810118749999738, -4.220049686691941915, 111.6250000020483810 ) ) ;
#23918=CARTESIAN_POINT ( 'NONE',  ( -10.18810118749999916, 4.220049686691934809, 78.43750000204838102 ) ) ;
#23929=CARTESIAN_POINT ( 'NONE',  ( 4.220049686691941027, -10.18810118749999738, 72.62500000204836681 ) ) ;
#23931=DIRECTION ( 'NONE',  ( -0.000000000000000000, -0.000000000000000000, -1.000000000000000000 ) ) ;
#23939=EDGE_CURVE ( 'NONE', #72729, #36393, #59944, .T. ) ;
#23955=ORIENTED_EDGE ( 'NONE', *, *, #16197, .F. ) ;
#23990=CARTESIAN_POINT ( 'NONE',  ( -8.825921739425714563, 6.257269313017580714, 117.7228986236605692 ) ) ;
#23991=CARTESIAN_POINT ( 'NONE',  ( 1.871523826299183495E-15, -10.18810118749999916, 101.0312500020483810 ) ) ;
#24008=CARTESIAN_POINT ( 'NONE',  ( -10.18810118749999738, -4.220049686691941915, 95.12500000204838102 ) ) ;
#24014=CARTESIAN_POINT ( 'NONE',  ( -4.220049686691937474, -10.18810118749999738, 80.31250000204836681 ) ) ;
#24018=ORIENTED_EDGE ( 'NONE', *, *, #1749, .T. ) ;
#24021=CARTESIAN_POINT ( 'NONE',  ( -10.18810118749999738, -4.220049686691941915, 88.75000000204836681 ) ) ;
#24030=CARTESIAN_POINT ( 'NONE',  ( -4.220049686691935698, 10.18810118749999916, 73.75000000204836681 ) ) ;
#24033=CARTESIAN_POINT ( 'NONE',  ( 11.00000000000000000, 1.347111479062088405E-15, 112.7499999999999858 ) ) ;
#24036=CARTESIAN_POINT ( 'NONE',  ( 7.778174593052023411, -7.778174593052021635, 93.25000000409677625 ) ) ;
#24042=ORIENTED_EDGE ( 'NONE', *, *, #44390, .F. ) ;
#24046=( BOUNDED_CURVE ( )  B_SPLINE_CURVE ( 2, ( #45770, #53298, #59693, #31008, #47983, #54033, #66080, #48725, #71732 ),
 .UNSPECIFIED., .F., .F. ) 
 B_SPLINE_CURVE_WITH_KNOTS ( ( 3, 2, 2, 2, 3 ),
 ( 0.4852941176470588758, 0.4889705882352941568, 0.4926470588235294379, 0.4963235294117647189, 0.5000000000000000000 ),
 .UNSPECIFIED. ) 
 CURVE ( )  GEOMETRIC_REPRESENTATION_ITEM ( )  RATIONAL_B_SPLINE_CURVE ( ( 0.9999999999999988898, 0.9238795325112878487, 1.000000000000000000, 0.9238795325112867385, 1.000000000000000000, 0.9238795325112867385, 1.000000000000000000, 0.9238795325112867385, 1.000000000000000000 ) ) 
 REPRESENTATION_ITEM ( '' )  );
#24049=DIRECTION ( 'NONE',  ( -0.000000000000000000, 0.000000000000000000, 1.000000000000000000 ) ) ;
#24050=CARTESIAN_POINT ( 'NONE',  ( 2.020667218593132706E-15, -11.00000000000000000, 82.37499999999998579 ) ) ;
#24070=CARTESIAN_POINT ( 'NONE',  ( 0.000000000000000000, 0.000000000000000000, 118.0000000000000000 ) ) ;
#24076=CARTESIAN_POINT ( 'NONE',  ( -10.99999999999999822, -4.556349186104052151, 68.78125000409679046 ) ) ;
#24088=CARTESIAN_POINT ( 'NONE',  ( 7.204075437095966983, 7.204075437095967871, 113.9687500020483810 ) ) ;
#24128=CARTESIAN_POINT ( 'NONE',  ( -4.220049686691937474, -10.18810118749999738, 85.93750000204839523 ) ) ;
#24130=CARTESIAN_POINT ( 'NONE',  ( 11.00000000000000000, 1.347111479062088405E-15, 99.24999999999998579 ) ) ;
#24136=EDGE_CURVE ( 'NONE', #49272, #33217, #31075, .T. ) ;
#24154=CARTESIAN_POINT ( 'NONE',  ( 0.000000000000000000, 0.000000000000000000, 38.34805510287551300 ) ) ;
#24156=DIRECTION ( 'NONE',  ( -0.000000000000000000, -0.000000000000000000, -1.000000000000000000 ) ) ;
#24157=VERTEX_POINT ( 'NONE', #66097 ) ;
#24162=CARTESIAN_POINT ( 'NONE',  ( -6.735557395310442023E-16, 11.00000000000000000, 86.31250000409676204 ) ) ;
#24176=ORIENTED_EDGE ( 'NONE', *, *, #58294, .T. ) ;
#24187=CARTESIAN_POINT ( 'NONE',  ( 1.871523826299183495E-15, -10.18810118749999916, 92.40625000204836681 ) ) ;
#24189=AXIS2_PLACEMENT_3D ( 'NONE', #34667, #11629, #7088 ) ;
#24191=CARTESIAN_POINT ( 'NONE',  ( 4.556349186104052151, -10.99999999999999822, 100.6562500040967905 ) ) ;
#24193=CARTESIAN_POINT ( 'NONE',  ( 4.220049686691941027, -10.18810118749999738, 99.62500000204838102 ) ) ;
#24201=CARTESIAN_POINT ( 'NONE',  ( -10.18810118749999738, -4.220049686691941915, 101.1250000020483810 ) ) ;
#24207=CARTESIAN_POINT ( 'NONE',  ( 2.020667218593132706E-15, -11.00000000000000000, 80.87499999999998579 ) ) ;
#24212=EDGE_CURVE ( 'NONE', #17249, #43963, #49874, .T. ) ;
#24217=CARTESIAN_POINT ( 'NONE',  ( 10.18810118749999916, 4.220049686691935698, 106.0000000020483668 ) ) ;
#24228=CARTESIAN_POINT ( 'NONE',  ( 2.020667218593132706E-15, -11.00000000000000000, 109.3750000000000000 ) ) ;
#24236=CARTESIAN_POINT ( 'NONE',  ( -10.18810118749999738, -4.220049686691941915, 71.12500000204836681 ) ) ;
#24242=CARTESIAN_POINT ( 'NONE',  ( 11.00000000000005329, -4.556349186103991755, 97.84375000409679046 ) ) ;
#24249=CARTESIAN_POINT ( 'NONE',  ( -10.99999999999999822, -4.556349186104052151, 101.7812500040967620 ) ) ;
#24253=CARTESIAN_POINT ( 'NONE',  ( -4.556349186104045934, 11.00000000000000000, 71.40625000409676204 ) ) ;
#24254=CARTESIAN_POINT ( 'NONE',  ( -11.00000000000007816, -4.556349186103974880, 107.7812500040967905 ) ) ;
#24265=( BOUNDED_CURVE ( )  B_SPLINE_CURVE ( 2, ( #27262, #15566, #61605, #50280, #73300, #38968, #33325, #74033, #27639 ),
 .UNSPECIFIED., .F., .F. ) 
 B_SPLINE_CURVE_WITH_KNOTS ( ( 3, 2, 2, 2, 3 ),
 ( 0.2499999999999998612, 0.2536764705882351145, 0.2573529411764703956, 0.2610294117647057321, 0.2647058823529410132 ),
 .UNSPECIFIED. ) 
 CURVE ( )  GEOMETRIC_REPRESENTATION_ITEM ( )  RATIONAL_B_SPLINE_CURVE ( ( 1.000000000000002887, 0.9238795325112838519, 1.000000000000000000, 0.9238795325112867385, 1.000000000000000000, 0.9238795325112867385, 1.000000000000000000, 0.9238795325112901802, 0.9999999999999965583 ) ) 
 REPRESENTATION_ITEM ( '' )  );
#24270=CARTESIAN_POINT ( 'NONE',  ( 4.220049686691934809, 10.18810118749999916, 83.68750000204836681 ) ) ;
#24275=CARTESIAN_POINT ( 'NONE',  ( 4.220049686691934809, 10.18810118749999916, 109.5625000020483810 ) ) ;
#24276=ORIENTED_EDGE ( 'NONE', *, *, #68278, .T. ) ;
#24283=CARTESIAN_POINT ( 'NONE',  ( -6.238412754330611322E-16, 10.18810118749999916, 75.15625000204836681 ) ) ;
#24297=CARTESIAN_POINT ( 'NONE',  ( 10.18810118750000093, -4.220049686691933921, 69.81250000204835260 ) ) ;
#24364=CARTESIAN_POINT ( 'NONE',  ( 10.18810118749999916, 4.220049686691935698, 103.0000000020483668 ) ) ;
#24382=CARTESIAN_POINT ( 'NONE',  ( -10.18810118749999738, -4.220049686691941915, 96.62500000204838102 ) ) ;
#24387=CARTESIAN_POINT ( 'NONE',  ( 4.556349186104045934, 11.00000000000000000, 102.5312500000000000 ) ) ;
#24388=CARTESIAN_POINT ( 'NONE',  ( -7.204075437095967871, 7.204075437095967871, 75.34375000204838102 ) ) ;
#24396=CARTESIAN_POINT ( 'NONE',  ( 4.220049686691934809, 10.18810118749999916, 86.68750000204836681 ) ) ;
#24406=CARTESIAN_POINT ( 'NONE',  ( 4.220049686691941027, -10.18810118749999738, 74.50000000204838102 ) ) ;
#24411=CARTESIAN_POINT ( 'NONE',  ( 2.020667218593132706E-15, -11.00000000000000000, 93.06250000409677625 ) ) ;
#24422=CARTESIAN_POINT ( 'NONE',  ( -7.204075437095967871, 7.204075437095967871, 70.46875000204836681 ) ) ;
#24425=CARTESIAN_POINT ( 'NONE',  ( -7.778174593052023411, 7.778174593052023411, 77.31249999999997158 ) ) ;
#24447=ORIENTED_EDGE ( 'NONE', *, *, #25834, .T. ) ;
#24451=CARTESIAN_POINT ( 'NONE',  ( -7.778174593052020747, -7.778174593052023411, 68.87500000409677625 ) ) ;
#24464=CARTESIAN_POINT ( 'NONE',  ( -6.238412754330611322E-16, 10.18810118749999916, 114.1562500020483810 ) ) ;
#24482=ORIENTED_EDGE ( 'NONE', *, *, #26692, .T. ) ;
#24483=EDGE_CURVE ( 'NONE', #42214, #73730, #23430, .T. ) ;
#24491=CARTESIAN_POINT ( 'NONE',  ( -11.00000000000000000, 0.000000000000000000, 80.68750000409677625 ) ) ;
#24493=CYLINDRICAL_SURFACE ( 'NONE', #45117, 11.00000000000000000 ) ;
#24503=CARTESIAN_POINT ( 'NONE',  ( 4.220049686691934809, 10.18810118749999916, 85.18750000204838102 ) ) ;
#24506=CARTESIAN_POINT ( 'NONE',  ( 11.00000000000000355, -4.556349186104045046, 94.65625000000001421 ) ) ;
#24512=CARTESIAN_POINT ( 'NONE',  ( 11.00000000000000000, 4.556349186104045934, 78.34374999999998579 ) ) ;
#24533=CARTESIAN_POINT ( 'NONE',  ( 2.020667218593132706E-15, -11.00000000000000000, 88.56250000409676204 ) ) ;
#24549=VERTEX_POINT ( 'NONE', #1184 ) ;
#24555=EDGE_CURVE ( 'NONE', #5227, #49057, #44542, .T. ) ;
#24557=CARTESIAN_POINT ( 'NONE',  ( -7.204075437095967871, 7.204075437095967871, 90.34375000204838102 ) ) ;
#24558=ORIENTED_EDGE ( 'NONE', *, *, #68963, .T. ) ;
#24564=CARTESIAN_POINT ( 'NONE',  ( 4.220049686691941027, -10.18810118749999738, 104.1250000020483810 ) ) ;
#24566=ORIENTED_EDGE ( 'NONE', *, *, #41762, .T. ) ;
#24574=CARTESIAN_POINT ( 'NONE',  ( -6.238412754330611322E-16, 10.18810118749999916, 97.65625000204838102 ) ) ;
#24581=( BOUNDED_CURVE ( )  B_SPLINE_CURVE ( 2, ( #73969, #11343, #28687, #34379, #57379, #35843, #65978, #7169, #59950 ),
 .UNSPECIFIED., .F., .F. ) 
 B_SPLINE_CURVE_WITH_KNOTS ( ( 3, 2, 2, 2, 3 ),
 ( 0.6029411764705880916, 0.6066176470588233727, 0.6102941176470587648, 0.6139705882352940458, 0.6176470588235293269 ),
 .UNSPECIFIED. ) 
 CURVE ( )  GEOMETRIC_REPRESENTATION_ITEM ( )  RATIONAL_B_SPLINE_CURVE ( ( 1.000000000000002220, 0.9238795325112844070, 1.000000000000000000, 0.9238795325112867385, 1.000000000000000000, 0.9238795325112867385, 1.000000000000000000, 0.9238795325112890700, 0.9999999999999976685 ) ) 
 REPRESENTATION_ITEM ( '' )  );
#24585=LINE ( 'NONE', #59671, #51308 ) ;
#24589=CARTESIAN_POINT ( 'NONE',  ( -10.18810118749999916, 0.000000000000000000, 102.1562500020483810 ) ) ;
#24603=CARTESIAN_POINT ( 'NONE',  ( 11.00000000000000000, 1.347111479062088405E-15, 118.0000000000000000 ) ) ;
#24604=CARTESIAN_POINT ( 'NONE',  ( 7.778174593052023411, -7.778174593052021635, 112.5625000000000000 ) ) ;
#24616=CARTESIAN_POINT ( 'NONE',  ( -4.556349186104047710, -10.99999999999999822, 106.4687500040967763 ) ) ;
#24637=FACE_OUTER_BOUND ( 'NONE', #3780, .T. ) ;
#24638=CARTESIAN_POINT ( 'NONE',  ( 1.871523826299183495E-15, -10.18810118749999916, 110.4062500020483668 ) ) ;
#24639=ORIENTED_EDGE ( 'NONE', *, *, #40780, .T. ) ;
#24645=DIRECTION ( 'NONE',  ( -1.000000000000000000, 0.000000000000000000, 0.000000000000000000 ) ) ;
#24646=CARTESIAN_POINT ( 'NONE',  ( -10.18810118749999916, 0.000000000000000000, 74.03125000204838102 ) ) ;
#24657=CARTESIAN_POINT ( 'NONE',  ( -7.204075437095967871, 7.204075437095967871, 117.3437500020483810 ) ) ;
#24711=CARTESIAN_POINT ( 'NONE',  ( 11.00000000000010836, -4.556349186103939353, 85.65625000000000000 ) ) ;
#24723=CARTESIAN_POINT ( 'NONE',  ( -7.204075437095967871, 7.204075437095967871, 103.4687500020483668 ) ) ;
#24724=LINE ( 'NONE', #19073, #32104 ) ;
#24739=CARTESIAN_POINT ( 'NONE',  ( -4.220049686691935698, 10.18810118749999916, 90.25000000204838102 ) ) ;
#24745=CARTESIAN_POINT ( 'NONE',  ( 7.204075437095966983, 7.204075437095967871, 71.96875000204836681 ) ) ;
#24752=CARTESIAN_POINT ( 'NONE',  ( -4.220049686691935698, 10.18810118749999916, 91.37500000204838102 ) ) ;
#24764=CARTESIAN_POINT ( 'NONE',  ( 4.220049686691934809, 10.18810118749999916, 75.06250000204836681 ) ) ;
#24773=VERTEX_POINT ( 'NONE', #49787 ) ;
#24781=CARTESIAN_POINT ( 'NONE',  ( 11.00000000000000355, -4.556349186104045046, 76.65625000000000000 ) ) ;
#24784=CARTESIAN_POINT ( 'NONE',  ( -4.556349186104048599, -10.99999999999999822, 113.7812500000000142 ) ) ;
#24794=AXIS2_PLACEMENT_3D ( 'NONE', #46520, #11453, #34111 ) ;
#24810=CARTESIAN_POINT ( 'NONE',  ( -4.220049686691935698, 10.18810118749999916, 88.75000000204836681 ) ) ;
#24811=CARTESIAN_POINT ( 'NONE',  ( 7.778174593052021635, 7.778174593052023411, 68.12500000409677625 ) ) ;
#24822=LINE ( 'NONE', #65562, #18337 ) ;
#24824=CARTESIAN_POINT ( 'NONE',  ( -4.220049686691935698, 10.18810118749999916, 115.7500000020483810 ) ) ;
#24828=CARTESIAN_POINT ( 'NONE',  ( 4.220049686691941027, -10.18810118749999738, 68.12500000204838102 ) ) ;
#24859=CARTESIAN_POINT ( 'NONE',  ( -4.220049686691937474, -10.18810118749999738, 88.93750000204839523 ) ) ;
#24861=CARTESIAN_POINT ( 'NONE',  ( -4.556349186104045934, 11.00000000000000000, 96.71874999999998579 ) ) ;
#24891=CARTESIAN_POINT ( 'NONE',  ( -11.00000000000000000, 0.000000000000000000, 88.18750000409677625 ) ) ;
#24895=CARTESIAN_POINT ( 'NONE',  ( 11.00000000000000000, 1.347111479062088405E-15, 100.7499999999999858 ) ) ;
#24914=CARTESIAN_POINT ( 'NONE',  ( 7.778174593052021635, 7.778174593052023411, 90.62500000409677625 ) ) ;
#24916=CARTESIAN_POINT ( 'NONE',  ( -10.18810118749999916, 4.220049686691934809, 91.93750000204836681 ) ) ;
#24922=CARTESIAN_POINT ( 'NONE',  ( 4.220049686691934809, 10.18810118749999916, 103.1875000020483810 ) ) ;
#24931=CARTESIAN_POINT ( 'NONE',  ( 10.18810118749999916, 4.220049686691935698, 100.3750000020484094 ) ) ;
#24932=EDGE_CURVE ( 'NONE', #72729, #26793, #3393, .T. ) ;
#24933=DIRECTION ( 'NONE',  ( 2.168404344971008868E-16, -1.000000000000000000, 0.000000000000000000 ) ) ;
#24949=CARTESIAN_POINT ( 'NONE',  ( -10.18810118749999916, 4.220049686691934809, 106.5625000020483810 ) ) ;
#24968=CARTESIAN_POINT ( 'NONE',  ( -4.556349186104047710, -10.99999999999999822, 112.2812499999999858 ) ) ;
#24972=CARTESIAN_POINT ( 'NONE',  ( -4.556349186104048599, -10.99999999999999822, 101.7812499999999858 ) ) ;
#24979=CARTESIAN_POINT ( 'NONE',  ( -7.778174593052023411, 7.778174593052023411, 104.5000000040967763 ) ) ;
#24984=CARTESIAN_POINT ( 'NONE',  ( 11.00000000000000000, 1.347111479062088405E-15, 70.93750000409676204 ) ) ;
#24996=CYLINDRICAL_SURFACE ( 'NONE', #27886, 11.00000000000000000 ) ;
#24998=DIRECTION ( 'NONE',  ( -0.000000000000000000, -0.000000000000000000, -1.000000000000000000 ) ) ;
#25001=CARTESIAN_POINT ( 'NONE',  ( -7.204075437095965206, -7.204075437095968759, 108.7187500020483810 ) ) ;
#25004=CARTESIAN_POINT ( 'NONE',  ( -11.00000000000000000, 0.000000000000000000, 118.0000000000000000 ) ) ;
#25008=CARTESIAN_POINT ( 'NONE',  ( 7.204075437095966983, 7.204075437095967871, 70.46875000204836681 ) ) ;
#25021=CARTESIAN_POINT ( 'NONE',  ( -4.220049686691937474, -10.18810118749999738, 67.93750000204838102 ) ) ;
#25076=CARTESIAN_POINT ( 'NONE',  ( -4.556349186104048599, -10.99999999999999822, 85.28124999999998579 ) ) ;
#25078=CARTESIAN_POINT ( 'NONE',  ( -7.778174593052023411, 7.778174593052023411, 101.5000000040967763 ) ) ;
#25089=CARTESIAN_POINT ( 'NONE',  ( 1.871523826299183495E-15, -10.18810118749999916, 93.53125000204836681 ) ) ;
#25101=CARTESIAN_POINT ( 'NONE',  ( -7.778174593052023411, 7.778174593052023411, 83.50000000409677625 ) ) ;
#25105=CARTESIAN_POINT ( 'NONE',  ( -7.204075437095967871, 7.204075437095967871, 91.84375000204838102 ) ) ;
#25110=CARTESIAN_POINT ( 'NONE',  ( 10.99999999999994849, 4.556349186104097448, 102.3437499999999858 ) ) ;
#25111=CARTESIAN_POINT ( 'NONE',  ( 10.18810118750000093, -4.220049686691933921, 73.18750000204838102 ) ) ;
#25117=CARTESIAN_POINT ( 'NONE',  ( 10.18810118749999916, 4.220049686691935698, 83.50000000204840944 ) ) ;
#25128=CARTESIAN_POINT ( 'NONE',  ( -10.18810118749999738, -4.220049686691941915, 68.12500000204838102 ) ) ;
#25153=CARTESIAN_POINT ( 'NONE',  ( 11.00000000000000355, -4.556349186104045046, 75.15624999999998579 ) ) ;
#25163=CARTESIAN_POINT ( 'NONE',  ( -4.556349186104047710, -10.99999999999999822, 115.4687500040967763 ) ) ;
#25171=EDGE_LOOP ( 'NONE', ( #35659, #37884, #34925, #45920 ) ) ;
#25175=VERTEX_POINT ( 'NONE', #52319 ) ;
#25180=CARTESIAN_POINT ( 'NONE',  ( 7.204075437095966983, 7.204075437095967871, 86.96875000204836681 ) ) ;
#25182=CARTESIAN_POINT ( 'NONE',  ( 7.204075437095968759, -7.204075437095966983, 113.2187500020483810 ) ) ;
#25194=CARTESIAN_POINT ( 'NONE',  ( 7.204075437095966983, 7.204075437095967871, 106.4687500020483810 ) ) ;
#25230=VERTEX_POINT ( 'NONE', #62507 ) ;
#25231=CARTESIAN_POINT ( 'NONE',  ( 7.204075437095968759, -7.204075437095966983, 83.21875000204836681 ) ) ;
#25233=CARTESIAN_POINT ( 'NONE',  ( 11.00000000000000000, 4.556349186104045934, 93.34374999999998579 ) ) ;
#25238=CARTESIAN_POINT ( 'NONE',  ( -4.556349186104045934, 11.00000000000000000, 105.9062500040967763 ) ) ;
#25249=DIRECTION ( 'NONE',  ( -1.000000000000000000, 0.000000000000000000, 0.000000000000000000 ) ) ;
#25260=CARTESIAN_POINT ( 'NONE',  ( 10.99999999999986855, 4.556349186104178273, 104.0312500040967905 ) ) ;
#25263=CARTESIAN_POINT ( 'NONE',  ( 11.00000000000000000, 4.556349186104045934, 89.03125000409677625 ) ) ;
#25281=CARTESIAN_POINT ( 'NONE',  ( 7.778174593052021635, 7.778174593052023411, 92.12500000409677625 ) ) ;
#25288=CARTESIAN_POINT ( 'NONE',  ( -10.18810118749999916, 4.220049686691934809, 88.93750000204839523 ) ) ;
#25294=CARTESIAN_POINT ( 'NONE',  ( 10.18810118749999916, 4.220049686691935698, 101.5000000020483810 ) ) ;
#25297=ORIENTED_EDGE ( 'NONE', *, *, #68991, .T. ) ;
#25303=CARTESIAN_POINT ( 'NONE',  ( 10.18810118749999916, 1.247682550866122264E-15, 97.28125000204838102 ) ) ;
#25315=CARTESIAN_POINT ( 'NONE',  ( -6.735557395310442023E-16, 11.00000000000000000, 84.62499999999997158 ) ) ;
#25319=CARTESIAN_POINT ( 'NONE',  ( -10.18810118749999738, -4.220049686691941915, 97.75000000204838102 ) ) ;
#25331=DIRECTION ( 'NONE',  ( 1.000000000000000000, 0.000000000000000000, 0.000000000000000000 ) ) ;
#25338=CARTESIAN_POINT ( 'NONE',  ( -11.00000000000000000, 0.000000000000000000, 110.4999999999999858 ) ) ;
#25346=CARTESIAN_POINT ( 'NONE',  ( 11.00000000000000000, 1.347111479062088405E-15, 118.0000000000000000 ) ) ;
#25347=FACE_OUTER_BOUND ( 'NONE', #51893, .T. ) ;
#25351=CARTESIAN_POINT ( 'NONE',  ( 7.778174593052023411, -7.778174593052021635, 102.2500000040967763 ) ) ;
#25357=CARTESIAN_POINT ( 'NONE',  ( -4.556349186104045934, 11.00000000000000000, 87.71874999999998579 ) ) ;
#25366=ORIENTED_EDGE ( 'NONE', *, *, #48717, .F. ) ;
#25374=CARTESIAN_POINT ( 'NONE',  ( -10.18810118749999916, 0.000000000000000000, 108.5312500020483810 ) ) ;
#25378=FACE_OUTER_BOUND ( 'NONE', #37357, .T. ) ;
#25382=CARTESIAN_POINT ( 'NONE',  ( -10.18810118749999738, -4.220049686691941915, 72.62500000204836681 ) ) ;
#25389=ORIENTED_EDGE ( 'NONE', *, *, #31352, .T. ) ;
#25397=CARTESIAN_POINT ( 'NONE',  ( 10.18810118749999916, 1.247682550866122264E-15, 115.2812500020483810 ) ) ;
#25424=CARTESIAN_POINT ( 'NONE',  ( -11.00000000000000000, 0.000000000000000000, 74.68750000409676204 ) ) ;
#25433=CARTESIAN_POINT ( 'NONE',  ( 7.778174593052021635, 7.778174593052023411, 75.62500000409677625 ) ) ;
#25437=ORIENTED_EDGE ( 'NONE', *, *, #40888, .F. ) ;
#25439=AXIS2_PLACEMENT_3D ( 'NONE', #548, #36711, #70665 ) ;
#25442=CARTESIAN_POINT ( 'NONE',  ( -11.00000000000000000, 0.000000000000000000, 78.99999999999998579 ) ) ;
#25456=CARTESIAN_POINT ( 'NONE',  ( -11.00000000000021139, 4.556349186103834548, 82.09375000409677625 ) ) ;
#25461=CARTESIAN_POINT ( 'NONE',  ( 10.18810118749999916, 1.247682550866122264E-15, 93.90625000204836681 ) ) ;
#25475=CARTESIAN_POINT ( 'NONE',  ( 7.204075437095968759, -7.204075437095966983, 88.09375000204836681 ) ) ;
#25481=CARTESIAN_POINT ( 'NONE',  ( 4.220049686691934809, 10.18810118749999916, 76.56250000204836681 ) ) ;
#25491=CARTESIAN_POINT ( 'NONE',  ( -7.204075437095967871, 7.204075437095967871, 83.96875000204836681 ) ) ;
#25502=CARTESIAN_POINT ( 'NONE',  ( 1.871523826299183495E-15, -10.18810118749999916, 69.90625000204836681 ) ) ;
#25517=CARTESIAN_POINT ( 'NONE',  ( -11.00000000000000000, 0.000000000000000000, 118.0000000000000000 ) ) ;
#25524=CARTESIAN_POINT ( 'NONE',  ( 4.556349186104045934, 11.00000000000000000, 78.53124999999998579 ) ) ;
#25549=CARTESIAN_POINT ( 'NONE',  ( 7.204075437095968759, -7.204075437095966983, 86.59375000204836681 ) ) ;
#25550=CARTESIAN_POINT ( 'NONE',  ( -7.204075437095967871, 7.204075437095967871, 110.9687500020483810 ) ) ;
#25563=CARTESIAN_POINT ( 'NONE',  ( 4.220049686691941027, -10.18810118749999738, 109.0000000020483810 ) ) ;
#25573=EDGE_CURVE ( 'NONE', #32089, #62341, #33990, .T. ) ;
#25574=ORIENTED_EDGE ( 'NONE', *, *, #12435, .T. ) ;
#25603=ORIENTED_EDGE ( 'NONE', *, *, #35947, .F. ) ;
#25604=CARTESIAN_POINT ( 'NONE',  ( -7.204075437095967871, 7.204075437095967871, 77.96875000204836681 ) ) ;
#25607=CARTESIAN_POINT ( 'NONE',  ( -6.735557395310442023E-16, 11.00000000000000000, 96.62499999999998579 ) ) ;
#25612=CARTESIAN_POINT ( 'NONE',  ( 10.99999999999989342, 4.556349186104152515, 88.84374999999998579 ) ) ;
#25634=CARTESIAN_POINT ( 'NONE',  ( 11.00000000000000000, 4.556349186104045934, 83.03125000409677625 ) ) ;
#25651=CARTESIAN_POINT ( 'NONE',  ( 4.220049686691941027, -10.18810118749999738, 80.12500000204835260 ) ) ;
#25659=CARTESIAN_POINT ( 'NONE',  ( 10.18810118749999916, 1.247682550866122264E-15, 86.78125000204836681 ) ) ;
#25661=FACE_OUTER_BOUND ( 'NONE', #31527, .T. ) ;
#25664=CARTESIAN_POINT ( 'NONE',  ( -7.204075437095965206, -7.204075437095968759, 103.8437500020483810 ) ) ;
#25672=CARTESIAN_POINT ( 'NONE',  ( -4.220049686691935698, 10.18810118749999916, 96.25000000204838102 ) ) ;
#25688=CARTESIAN_POINT ( 'NONE',  ( -7.204075437095967871, 7.204075437095967871, 98.96875000204838102 ) ) ;
#25706=CARTESIAN_POINT ( 'NONE',  ( -11.00000000000000000, 0.000000000000000000, 113.4999999999999858 ) ) ;
#25715=ORIENTED_EDGE ( 'NONE', *, *, #26692, .F. ) ;
#25718=CARTESIAN_POINT ( 'NONE',  ( -10.99999999999999822, -4.556349186104052151, 100.2812500040967620 ) ) ;
#25722=CARTESIAN_POINT ( 'NONE',  ( 4.556349186104052151, -10.99999999999999822, 107.9687500000000000 ) ) ;
#25723=CARTESIAN_POINT ( 'NONE',  ( -6.735557395310442023E-16, 11.00000000000000000, 87.62499999999998579 ) ) ;
#25724=EDGE_CURVE ( 'NONE', #37130, #31137, #38304, .T. ) ;
#25729=DIRECTION ( 'NONE',  ( -1.000000000000000000, 0.000000000000000000, 0.000000000000000000 ) ) ;
#25734=EDGE_CURVE ( 'NONE', #56815, #47217, #54243, .T. ) ;
#25742=CYLINDRICAL_SURFACE ( 'NONE', #37411, 11.00000000000000000 ) ;
#25743=CARTESIAN_POINT ( 'NONE',  ( 7.204075437095966983, 7.204075437095967871, 104.9687500020483810 ) ) ;
#25750=CARTESIAN_POINT ( 'NONE',  ( -4.220049686691937474, -10.18810118749999738, 72.81250000204838102 ) ) ;
#25762=CARTESIAN_POINT ( 'NONE',  ( -4.220049686691937474, -10.18810118749999738, 114.8125000020483668 ) ) ;
#25778=CARTESIAN_POINT ( 'NONE',  ( 7.204075437095966983, 7.204075437095967871, 115.0937500020483810 ) ) ;
#25798=( BOUNDED_SURFACE ( )  B_SPLINE_SURFACE ( 1, 2, ( 
 ( #19141, #42883, #65158, #13469, #60620, #42524, #2913, #66651, #36508, #7830, #20625, #30834, #59883, #25163, #65903, #48179, #8944, #37247, #71187, #14958, #31956, #19506, #65538, #60243, #8569, #31584, #26274, #54606, #25901, #48918, #71931, #54981, #72312, #63132, #74451, #33742, #68420, #63505, #39385, #57501, #49681, #5804, #56745, #34116, #69170, #69545, #17102, #57116, #51440, #45782, #35229, #44022, #11827, #63879, #67032, #12191, #46153, #5064, #28060, #39748, #22383, #62749, #51071, #28801, #5428, #34865, #26658, #74083, #40500, #52200, #45404, #17855, #62382, #72695, #16721, #51819, #10710, #11090, #28432, #22760, #68793, #57870, #163, #15331, #40125, #58247, #20997, #23141, #11459, #34494, #17479, #6178, #29185, #531, #23510, #46526, #40874, #54046, #53311, #18231, #1269, #64626, #29921, #7283, #58604, #71371, #1635, #13287, #1989, #24616, #58976, #37061, #59706, #901, #47261, #12922, #47996, #48367, #19325, #53676, #19696, #35956, #30291, #8015, #18966, #52562, #71010, #36327, #70646, #42338, #24979, #69921, #42708, #18602, #23888, #47624, #41246, #65355, #41969, #64254, #2357, #13655, #12563, #35590, #70288, #65719, #14023, #36695, #64979, #59341, #7653, #30659, #6910, #31022, #25351, #6547, #52939, #41612, #29553, #24249, #46897, #8382, #15156, #66094, #66468, #26856, #27222, #49493, #14777, #9136, #3479, #67603, #2730, #44218, #21565, #25718, #44591, #3861, #14404, #60435, #72124, #54795, #20438, #37436, #38188, #37817, #67231, #60061, #8765, #72886, #9889, #31775, #50239, #71745, #31397, #26092, #61192, #43078, #3106, #60812, #49112, #43454, #21193, #9522, #48739, #32153, #15900, #54424, #55548, #55174, #20060, #26469, #66853, #20820, #72512, #32537, #15527, #49870, #32918, #43838, #38568, #61568, #55924, #4234, #73260, #16264, #29096, #11004, #45693, #34406, #34037, #16636, #69459, #17392, #33285, #4979, #22300, #5715, #6091, #51730, #11372, #52116, #45324, #62669, #40417, #51354, #10260, #28715, #68708, #28347, #79, #57408, #27597, #23057, #33657, #17019, #34780, #4602, #50608, #11742, #56284, #46066, #448, #73628, #23427, #69086, #67969, #39304, #50985, #56663, #73998, #62302, #40043, #68341, #63414, #38931, #10630, #57784, #46441, #27980, #61933, #21933, #44963, #39670, #63047, #57034, #5346, #74365, #22676, #46806, #30571, #41887, #58159, #18145, #2269, #25263, #13201, #41160, #52479, #48282, #24533, #53222, #17767, #70564, #24891, #64898, #65263, #64538, #29469, #12474, #1181, #64170, #18515, #69830, #7931, #12835, #47541, #36239, #35872, #70206, #40783, #70928, #12107, #58518, #24162, #59255, #59616, #53593, #7567, #30935, #47174, #41522, #19240, #30201, #63789, #1904, #18880, #7198, #47909, #42250, #6466, #13568, #35505, #36606, #53956, #815, #23803, #35145, #6824, #29837, #52849, #58889, #1554, #43746, #20346, #59979, #44130, #66760, #54334, #25634, #37346, #32822, #38472, #26766, #9047, #55081, #14686, #72030, #48649, #38099, #32061, #43363, #2645, #60344, #32444, #8295, #26374, #19608, #49398, #71657, #3015, #61097, #61475, #60725, #25997, #66379, #37727, #4148, #66006, #19978, #3390, #71288, #31306, #8672, #72418, #55832, #72798, #42986, #21107, #42621, #55453, #20728, #65636, #49022, #14311, #36973, #31687, #67140, #15064, #13932, #54707, #9426, #3764, #49784, #15435, #27138, #9799, #10539, #34316, #57320, #74278, #33945, #33571, #40324, #22588, #57696, #56200, #4513, #27883, #6004, #4887, #50894, #56574, #45982, #68622, #16547, #16170, #73909, #11654, #45608, #10168, #28631, #39585, #39213, #73533, #34688, #50153, #22213, #73170, #21477, #5631, #45240, #56944, #28261, #44498, #33204, #68252, #67511, #16931, #39955, #33395, #5260, #51645, #51268, #63328, #15809, #38845, #62960, #62580, #61848, #50518, #22976, #10912, #44873, #11286, #27508, #68998, #21841, #67879, #17305, #62213, #65175, #30120, #59174, #36154, #361, #36525, #53137, #7484, #58435, #30489, #47085, #7114, #35428, #29748, #42162, #29005, #13486, #1100, #1824, #12393, #53506, #40697, #59535, #52762, #17680, #6745, #52023, #35059, #6383, #24451, #24076, #23714, #64816, #70123, #58072, #69370, #732, #24811, #18429, #23343, #46353, #41444, #63701, #64456, #12026, #29389, #47826, #64083, #13118, #70847, #1470, #12756, #35788, #19160 ),
 ( #47460, #52396, #46718, #58802, #18058, #69744, #41073, #70483, #18802, #41806, #44041, #14977, #54623, #14604, #60641, #2186, #65553, #65921, #30854, #3306, #26292, #32357, #66297, #66671, #8962, #72713, #15350, #53875, #37643, #20259, #21017, #8214, #38013, #48936, #2561, #43282, #38385, #31602, #67050, #7847, #61012, #55371, #25182, #31975, #9337, #3677, #48195, #71204, #54999, #26676, #37267, #49700, #25918, #49313, #14225, #8587, #19523, #42540, #13847, #2932, #36890, #60260, #59900, #31226, #54250, #71948, #25550, #72329, #48564, #71573, #19895, #20644, #43659, #42901, #22495, #16090, #15723, #56115, #67425, #68163, #61389, #73081, #73451, #16462, #45893, #62866, #21389, #11199, #9715, #45517, #10823, #55745, #39125, #4424, #16837, #27796, #27419, #22128, #68907, #10452, #51550, #17218, #39864, #34226, #22881, #62494, #57228, #68533, #32736, #4062, #33858, #5540, #62129, #28542, #4803, #39499, #67799, #33483, #74568, #27055, #50067, #56485, #44412, #44786, #38766, #61765, #10083, #50809, #33121, #73820, #50436, #21757, #45153, #56857, #5174, #28170, #51182, #74190, #69284, #34972, #46264, #47001, #40237, #51935, #52308, #70032, #24723, #41720, #273, #64732, #63239, #24364, #64365, #34599, #69655, #57988, #5916, #11940, #13031, #63994, #57606, #28919, #40987, #11565, #17968, #23255, #47732, #18712, #644, #47371, #70397, #12667, #23991, #23628, #30401, #35698, #70756, #36068, #12309, #63613, #1380, #35341, #58353, #46635, #59085, #58714, #6658, #6292, #29661, #1742, #7025, #17593, #7394, #52677, #29298, #1011, #40611, #18341, #41355, #30032, #53048, #53419, #65829, #25828, #71856, #13397, #2095, #2471, #42076, #14510, #37549, #43563, #2838, #3215, #20171, #9244, #26583, #65086, #48847, #31511, #32266, #19435, #43189, #54532, #55284, #42446, #49224, #60173, #13758, #66205, #49607, #42812, #3588, #19072, #72234, #66580, #36435, #60548, #20550, #26203, #59448, #7762, #8872, #14884, #48478, #37923, #37171, #31885, #25461, #19806, #30765, #53786, #25089, #14136, #60923, #71480, #48104, #71114, #65464, #8494, #36802, #54906, #59812, #8126, #31129, #54161, #4338, #67337, #33766, #27329, #26961, #15634, #3974, #4712, #72622, #9628, #9997, #27706, #57137, #74106, #32648, #22405, #20926, #56767, #22040, #66958, #50345, #38674, #38295, #44324, #45427, #21670, #15262, #61303, #73367, #43948, #44695, #55658, #5453, #51093, #33027, #5087, #28080, #45067, #56391, #56029, #62771, #68080, #28455, #68440, #67711, #21301, #16744, #16009, #39039, #62041, #39769, #16369, #10365, #61676, #33391, #34138, #39406, #49977, #11115, #50716, #73732, #62405, #72994, #10732, #34886, #51461, #12942, #58625, #23535, #58266, #29574, #45803, #34517, #57891, #74474, #46916, #69941, #1291, #35248, #35610, #52586, #41633, #59995, #22781, #923, #6198, #52220, #64644, #68813, #35979, #46547, #24270, #29207, #6932, #63155, #8312, #552, #40151, #69566, #17126, #57522, #28823, #18249, #17877, #46175, #12581, #40894, #5827, #69192, #51840, #6567, #11482, #186, #63526, #23906, #23162, #52957, #17504, #47281, #40521, #29942, #41265, #11849, #63900, #12210, #64274, #70307, #18622, #55100, #25651, #48666, #32079, #54349, #60744, #71674, #38861, #9815, #66398, #15454, #38489, #55469, #15081, #14706, #21496, #3782, #61865, #4166, #9067, #54727, #67159, #3407, #26391, #37744, #27153, #49800, #72438, #72047, #49416, #67527, #26783, #66023, #32839, #20747, #20364, #3033, #15826, #31323, #43763, #2659, #19995, #61492, #66777, #38116, #9445, #43003, #14331, #61115, #37363, #72816, #21123, #55849, #32462, #50170, #44145, #44515, #60363, #8689, #73188, #31704, #26017, #49040, #43381, #51286, #4909, #45626, #17695, #33966, #377, #40713, #40342, #34703, #46372, #11303, #63344, #17321, #56216, #10188, #34336, #11669, #39602, #57712, #28280, #23358, #16565, #56963, #6018, #22605, #4530, #5, #16949, #74297, #45999, #28647, #73552, #22993, #27903, #39973, #29022, #50537, #21861, #52041, #69387, #22231, #27525, #5278, #44892, #57337, #68640, #67897, #33219, #5647, #16189, #39230, #50912, #62230, #10557, #33588, #62980, #51662, #69017, #10929, #56593, #73926, #45257, #68269, #62599, #29764, #24828, #748, #18818, #12041, #41821, #69760, #70139, #30504, #30872, #53153, #18446, #12771 ) ),
 .UNSPECIFIED., .F., .F., .F. ) 
 B_SPLINE_SURFACE_WITH_KNOTS ( ( 2, 2 ),
 ( 3, 2, 2, 2, 2, 2, 2, 2, 2, 2, 2, 2, 2, 2, 2, 2, 2, 2, 2, 2, 2, 2, 2, 2, 2, 2, 2, 2, 2, 2, 2, 2, 2, 2, 2, 2, 2, 2, 2, 2, 2, 2, 2, 2, 2, 2, 2, 2, 2, 2, 2, 2, 2, 2, 2, 2, 2, 2, 2, 2, 2, 2, 2, 2, 2, 2, 2, 2, 2, 2, 2, 2, 2, 2, 2, 2, 2, 2, 2, 2, 2, 2, 2, 2, 2, 2, 2, 2, 2, 2, 2, 2, 2, 2, 2, 2, 2, 2, 2, 2, 2, 2, 2, 2, 2, 2, 2, 2, 2, 2, 2, 2, 2, 2, 2, 2, 2, 2, 2, 2, 2, 2, 2, 2, 2, 2, 2, 2, 2, 2, 2, 2, 2, 2, 2, 2, 2, 2, 2, 2, 2, 2, 2, 2, 2, 2, 2, 2, 2, 2, 2, 2, 2, 2, 2, 2, 2, 2, 2, 2, 2, 2, 2, 2, 2, 2, 2, 2, 2, 2, 2, 2, 2, 2, 2, 2, 2, 2, 2, 2, 2, 2, 2, 2, 2, 2, 2, 2, 2, 2, 2, 2, 2, 2, 2, 2, 2, 2, 2, 2, 2, 2, 2, 2, 2, 2, 2, 2, 2, 2, 2, 2, 2, 2, 2, 2, 2, 2, 2, 2, 2, 2, 2, 2, 2, 2, 2, 2, 2, 2, 2, 2, 2, 2, 2, 2, 2, 2, 2, 2, 2, 2, 2, 2, 2, 2, 2, 2, 2, 2, 2, 2, 2, 2, 2, 2, 2, 2, 2, 2, 2, 2, 2, 2, 2, 2, 2, 3 ),
 ( 0.000000000000000000, 1.000000000000000000 ),
 ( 0.000000000000000000, 0.003676470588235294067, 0.007352941176470588133, 0.01102941176470588307, 0.01470588235294117627, 0.01838235294117647120, 0.02205882352941176613, 0.02573529411764705760, 0.02941176470588235253, 0.03308823529411764747, 0.03676470588235294240, 0.04044117647058823733, 0.04411764705882353227, 0.04779411764705882026, 0.05147058823529411520, 0.05514705882352941013, 0.05882352941176470507, 0.06250000000000000000, 0.06617647058823529493, 0.06985294117647058987, 0.07352941176470588480, 0.07720588235294117974, 0.08088235294117647467, 0.08455882352941176960, 0.08823529411764706454, 0.09191176470588235947, 0.09558823529411764053, 0.09926470588235293546, 0.1029411764705882304, 0.1066176470588235253, 0.1102941176470588203, 0.1139705882352941152, 0.1176470588235294101, 0.1213235294117647051, 0.1250000000000000000, 0.1286764705882352811, 0.1323529411764705899, 0.1360294117647058709, 0.1397058823529411797, 0.1433823529411764608, 0.1470588235294117696, 0.1507352941176470507, 0.1544117647058823595, 0.1580882352941176405, 0.1617647058823529493, 0.1654411764705882304, 0.1691176470588235392, 0.1727941176470588203, 0.1764705882352941291, 0.1801470588235294101, 0.1838235294117647189, 0.1875000000000000000, 0.1911764705882352811, 0.1948529411764705899, 0.1985294117647058709, 0.2022058823529411797, 0.2058823529411764608, 0.2095588235294117696, 0.2132352941176470507, 0.2169117647058823595, 0.2205882352941176405, 0.2242647058823529493, 0.2279411764705882304, 0.2316176470588235392, 0.2352941176470588203, 0.2389705882352941291, 0.2426470588235294101, 0.2463235294117647189, 0.2500000000000000000, 0.2536764705882352811, 0.2573529411764705621, 0.2610294117647058987, 0.2647058823529411797, 0.2683823529411764608, 0.2720588235294117418, 0.2757352941176470784, 0.2794117647058823595, 0.2830882352941176405, 0.2867647058823529216, 0.2904411764705882582, 0.2941176470588235392, 0.2977941176470588203, 0.3014705882352941013, 0.3051470588235294379, 0.3088235294117647189, 0.3125000000000000000, 0.3161764705882352811, 0.3198529411764705621, 0.3235294117647058987, 0.3272058823529411797, 0.3308823529411764608, 0.3345588235294117418, 0.3382352941176470784, 0.3419117647058823595, 0.3455882352941176405, 0.3492647058823529216, 0.3529411764705882582, 0.3566176470588235392, 0.3602941176470588203, 0.3639705882352941013, 0.3676470588235294379, 0.3713235294117647189, 0.3750000000000000000, 0.3786764705882352811, 0.3823529411764705621, 0.3860294117647058987, 0.3897058823529411797, 0.3933823529411764608, 0.3970588235294117418, 0.4007352941176470784, 0.4044117647058823595, 0.4080882352941176405, 0.4117647058823529216, 0.4154411764705882582, 0.4191176470588235392, 0.4227941176470588203, 0.4264705882352941013, 0.4301470588235294379, 0.4338235294117647189, 0.4375000000000000000, 0.4411764705882352811, 0.4448529411764705621, 0.4485294117647058987, 0.4522058823529411797, 0.4558823529411764608, 0.4595588235294117418, 0.4632352941176470784, 0.4669117647058823595, 0.4705882352941176405, 0.4742647058823529216, 0.4779411764705882582, 0.4816176470588235392, 0.4852941176470588203, 0.4889705882352941013, 0.4926470588235294379, 0.4963235294117647189, 0.5000000000000000000, 0.5036764705882352811, 0.5073529411764705621, 0.5110294117647058432, 0.5147058823529411242, 0.5183823529411765163, 0.5220588235294117974, 0.5257352941176470784, 0.5294117647058823595, 0.5330882352941176405, 0.5367647058823529216, 0.5404411764705882026, 0.5441176470588234837, 0.5477941176470588758, 0.5514705882352941568, 0.5551470588235294379, 0.5588235294117647189, 0.5625000000000000000, 0.5661764705882352811, 0.5698529411764705621, 0.5735294117647058432, 0.5772058823529411242, 0.5808823529411765163, 0.5845588235294117974, 0.5882352941176470784, 0.5919117647058823595, 0.5955882352941176405, 0.5992647058823529216, 0.6029411764705882026, 0.6066176470588234837, 0.6102941176470588758, 0.6139705882352941568, 0.6176470588235294379, 0.6213235294117647189, 0.6250000000000000000, 0.6286764705882352811, 0.6323529411764705621, 0.6360294117647058432, 0.6397058823529411242, 0.6433823529411765163, 0.6470588235294117974, 0.6507352941176470784, 0.6544117647058823595, 0.6580882352941176405, 0.6617647058823529216, 0.6654411764705882026, 0.6691176470588234837, 0.6727941176470588758, 0.6764705882352941568, 0.6801470588235294379, 0.6838235294117647189, 0.6875000000000000000, 0.6911764705882352811, 0.6948529411764705621, 0.6985294117647058432, 0.7022058823529411242, 0.7058823529411765163, 0.7095588235294117974, 0.7132352941176470784, 0.7169117647058823595, 0.7205882352941176405, 0.7242647058823529216, 0.7279411764705882026, 0.7316176470588234837, 0.7352941176470588758, 0.7389705882352941568, 0.7426470588235294379, 0.7463235294117647189, 0.7500000000000000000, 0.7536764705882352811, 0.7573529411764705621, 0.7610294117647058432, 0.7647058823529411242, 0.7683823529411765163, 0.7720588235294117974, 0.7757352941176470784, 0.7794117647058823595, 0.7830882352941176405, 0.7867647058823529216, 0.7904411764705882026, 0.7941176470588234837, 0.7977941176470588758, 0.8014705882352941568, 0.8051470588235294379, 0.8088235294117647189, 0.8125000000000000000, 0.8161764705882352811, 0.8198529411764705621, 0.8235294117647058432, 0.8272058823529411242, 0.8308823529411765163, 0.8345588235294117974, 0.8382352941176470784, 0.8419117647058823595, 0.8455882352941176405, 0.8492647058823529216, 0.8529411764705882026, 0.8566176470588234837, 0.8602941176470588758, 0.8639705882352941568, 0.8676470588235294379, 0.8713235294117647189, 0.8750000000000000000, 0.8786764705882352811, 0.8823529411764705621, 0.8860294117647058432, 0.8897058823529411242, 0.8933823529411765163, 0.8970588235294117974, 0.9007352941176470784, 0.9044117647058823595, 0.9080882352941176405, 0.9117647058823529216, 0.9154411764705882026, 0.9191176470588234837, 0.9227941176470588758, 0.9264705882352941568, 0.9301470588235294379, 0.9338235294117647189, 0.9375000000000000000, 0.9411764705882352811, 0.9448529411764705621, 0.9485294117647058432, 0.9522058823529411242, 0.9558823529411765163, 0.9595588235294117974, 0.9632352941176470784, 0.9669117647058823595, 0.9705882352941176405, 0.9742647058823529216, 0.9779411764705882026, 0.9803851222046974234 ),
 .UNSPECIFIED. ) 
 GEOMETRIC_REPRESENTATION_ITEM ( )  RATIONAL_B_SPLINE_SURFACE ( (
 ( 1.000000000000000000, 0.9238795325112867385, 1.000000000000000000, 0.9238795325112867385, 1.000000000000000000, 0.9238795325112867385, 1.000000000000000000, 0.9238795325112867385, 1.000000000000000000, 0.9238795325112867385, 1.000000000000000000, 0.9238795325112867385, 1.000000000000000000, 0.9238795325112867385, 1.000000000000000000, 0.9238795325112867385, 1.000000000000000000, 0.9238795325112867385, 1.000000000000000000, 0.9238795325112867385, 1.000000000000000000, 0.9238795325112867385, 1.000000000000000000, 0.9238795325112867385, 1.000000000000000000, 0.9238795325112867385, 1.000000000000000000, 0.9238795325112867385, 1.000000000000000000, 0.9238795325112867385, 1.000000000000000000, 0.9238795325112867385, 1.000000000000000000, 0.9238795325112867385, 1.000000000000000000, 0.9238795325112867385, 1.000000000000000000, 0.9238795325112867385, 1.000000000000000000, 0.9238795325112867385, 1.000000000000000000, 0.9238795325112867385, 1.000000000000000000, 0.9238795325112867385, 1.000000000000000000, 0.9238795325112867385, 1.000000000000000000, 0.9238795325112867385, 1.000000000000000000, 0.9238795325112867385, 1.000000000000000000, 0.9238795325112867385, 1.000000000000000000, 0.9238795325112867385, 1.000000000000000000, 0.9238795325112867385, 1.000000000000000000, 0.9238795325112867385, 1.000000000000000000, 0.9238795325112867385, 1.000000000000000000, 0.9238795325112867385, 1.000000000000000000, 0.9238795325112867385, 1.000000000000000000, 0.9238795325112867385, 1.000000000000000000, 0.9238795325112867385, 1.000000000000000000, 0.9238795325112867385, 1.000000000000000000, 0.9238795325112867385, 1.000000000000000000, 0.9238795325112867385, 1.000000000000000000, 0.9238795325112867385, 1.000000000000000000, 0.9238795325112867385, 1.000000000000000000, 0.9238795325112867385, 1.000000000000000000, 0.9238795325112867385, 1.000000000000000000, 0.9238795325112867385, 1.000000000000000000, 0.9238795325112867385, 1.000000000000000000, 0.9238795325112867385, 1.000000000000000000, 0.9238795325112867385, 1.000000000000000000, 0.9238795325112867385, 1.000000000000000000, 0.9238795325112867385, 1.000000000000000000, 0.9238795325112867385, 1.000000000000000000, 0.9238795325112867385, 1.000000000000000000, 0.9238795325112867385, 1.000000000000000000, 0.9238795325112867385, 1.000000000000000000, 0.9238795325112867385, 1.000000000000000000, 0.9238795325112867385, 1.000000000000000000, 0.9238795325112867385, 1.000000000000000000, 0.9238795325112867385, 1.000000000000000000, 0.9238795325112867385, 1.000000000000000000, 0.9238795325112867385, 1.000000000000000000, 0.9238795325112867385, 1.000000000000000000, 0.9238795325112867385, 1.000000000000000000, 0.9238795325112867385, 1.000000000000000000, 0.9238795325112867385, 1.000000000000000000, 0.9238795325112867385, 1.000000000000000000, 0.9238795325112867385, 1.000000000000000000, 0.9238795325112867385, 1.000000000000000000, 0.9238795325112867385, 1.000000000000000000, 0.9238795325112867385, 1.000000000000000000, 0.9238795325112867385, 1.000000000000000000, 0.9238795325112867385, 1.000000000000000000, 0.9238795325112867385, 1.000000000000000000, 0.9238795325112867385, 1.000000000000000000, 0.9238795325112867385, 1.000000000000000000, 0.9238795325112867385, 1.000000000000000000, 0.9238795325112867385, 1.000000000000000000, 0.9238795325112867385, 1.000000000000000000, 0.9238795325112867385, 1.000000000000000000, 0.9238795325112867385, 1.000000000000000000, 0.9238795325112867385, 1.000000000000000000, 0.9238795325112867385, 1.000000000000000000, 0.9238795325112867385, 1.000000000000000000, 0.9238795325112867385, 1.000000000000000000, 0.9238795325112867385, 1.000000000000000000, 0.9238795325112867385, 1.000000000000000000, 0.9238795325112867385, 1.000000000000000000, 0.9238795325112867385, 1.000000000000000000, 0.9238795325112867385, 1.000000000000000000, 0.9238795325112867385, 1.000000000000000000, 0.9238795325112867385, 1.000000000000000000, 0.9238795325112867385, 1.000000000000000000, 0.9238795325112867385, 1.000000000000000000, 0.9238795325112867385, 1.000000000000000000, 0.9238795325112867385, 1.000000000000000000, 0.9238795325112867385, 1.000000000000000000, 0.9238795325112867385, 1.000000000000000000, 0.9238795325112867385, 1.000000000000000000, 0.9238795325112867385, 1.000000000000000000, 0.9238795325112867385, 1.000000000000000000, 0.9238795325112867385, 1.000000000000000000, 0.9238795325112867385, 1.000000000000000000, 0.9238795325112867385, 1.000000000000000000, 0.9238795325112867385, 1.000000000000000000, 0.9238795325112867385, 1.000000000000000000, 0.9238795325112867385, 1.000000000000000000, 0.9238795325112867385, 1.000000000000000000, 0.9238795325112867385, 1.000000000000000000, 0.9238795325112867385, 1.000000000000000000, 0.9238795325112867385, 1.000000000000000000, 0.9238795325112867385, 1.000000000000000000, 0.9238795325112867385, 1.000000000000000000, 0.9238795325112867385, 1.000000000000000000, 0.9238795325112867385, 1.000000000000000000, 0.9238795325112867385, 1.000000000000000000, 0.9238795325112867385, 1.000000000000000000, 0.9238795325112867385, 1.000000000000000000, 0.9238795325112867385, 1.000000000000000000, 0.9238795325112867385, 1.000000000000000000, 0.9238795325112867385, 1.000000000000000000, 0.9238795325112867385, 1.000000000000000000, 0.9238795325112867385, 1.000000000000000000, 0.9238795325112867385, 1.000000000000000000, 0.9238795325112867385, 1.000000000000000000, 0.9238795325112867385, 1.000000000000000000, 0.9238795325112867385, 1.000000000000000000, 0.9238795325112867385, 1.000000000000000000, 0.9238795325112867385, 1.000000000000000000, 0.9238795325112867385, 1.000000000000000000, 0.9238795325112867385, 1.000000000000000000, 0.9238795325112867385, 1.000000000000000000, 0.9238795325112867385, 1.000000000000000000, 0.9238795325112867385, 1.000000000000000000, 0.9238795325112867385, 1.000000000000000000, 0.9238795325112867385, 1.000000000000000000, 0.9238795325112867385, 1.000000000000000000, 0.9238795325112867385, 1.000000000000000000, 0.9238795325112867385, 1.000000000000000000, 0.9238795325112867385, 1.000000000000000000, 0.9238795325112867385, 1.000000000000000000, 0.9238795325112867385, 1.000000000000000000, 0.9238795325112867385, 1.000000000000000000, 0.9238795325112867385, 1.000000000000000000, 0.9238795325112867385, 1.000000000000000000, 0.9238795325112867385, 1.000000000000000000, 0.9238795325112867385, 1.000000000000000000, 0.9238795325112867385, 1.000000000000000000, 0.9238795325112867385, 1.000000000000000000, 0.9238795325112867385, 1.000000000000000000, 0.9238795325112867385, 1.000000000000000000, 0.9238795325112867385, 1.000000000000000000, 0.9238795325112867385, 1.000000000000000000, 0.9238795325112867385, 1.000000000000000000, 0.9238795325112867385, 1.000000000000000000, 0.9238795325112867385, 1.000000000000000000, 0.9238795325112867385, 1.000000000000000000, 0.9238795325112867385, 1.000000000000000000, 0.9238795325112867385, 1.000000000000000000, 0.9238795325112867385, 1.000000000000000000, 0.9238795325112867385, 1.000000000000000000, 0.9238795325112867385, 1.000000000000000000, 0.9238795325112867385, 1.000000000000000000, 0.9238795325112867385, 1.000000000000000000, 0.9238795325112867385, 1.000000000000000000, 0.9238795325112867385, 1.000000000000000000, 0.9238795325112867385, 1.000000000000000000, 0.9238795325112867385, 1.000000000000000000, 0.9238795325112867385, 1.000000000000000000, 0.9238795325112867385, 1.000000000000000000, 0.9238795325112867385, 1.000000000000000000, 0.9238795325112867385, 1.000000000000000000, 0.9238795325112867385, 1.000000000000000000, 0.9238795325112867385, 1.000000000000000000, 0.9238795325112867385, 1.000000000000000000, 0.9238795325112867385, 1.000000000000000000, 0.9238795325112867385, 1.000000000000000000, 0.9238795325112867385, 1.000000000000000000, 0.9238795325112867385, 1.000000000000000000, 0.9238795325112867385, 1.000000000000000000, 0.9238795325112867385, 1.000000000000000000, 0.9238795325112867385, 1.000000000000000000, 0.9238795325112867385, 1.000000000000000000, 0.9238795325112867385, 1.000000000000000000, 0.9238795325112867385, 1.000000000000000000, 0.9238795325112867385, 1.000000000000000000, 0.9238795325112867385, 1.000000000000000000, 0.9238795325112867385, 1.000000000000000000, 0.9238795325112867385, 1.000000000000000000, 0.9238795325112867385, 1.000000000000000000, 0.9238795325112867385, 1.000000000000000000, 0.9238795325112867385, 1.000000000000000000, 0.9238795325112867385, 1.000000000000000000, 0.9238795325112867385, 1.000000000000000000, 0.9238795325112867385, 1.000000000000000000, 0.9238795325112867385, 1.000000000000000000, 0.9238795325112867385, 1.000000000000000000, 0.9238795325112867385, 1.000000000000000000, 0.9238795325112867385, 1.000000000000000000, 0.9238795325112867385, 1.000000000000000000, 0.9238795325112867385, 1.000000000000000000, 0.9238795325112867385, 1.000000000000000000, 0.9238795325112867385, 1.000000000000000000, 0.9238795325112867385, 1.000000000000000000, 0.9238795325112867385, 1.000000000000000000, 0.9238795325112867385, 1.000000000000000000, 0.9238795325112867385, 1.000000000000000000, 0.9238795325112867385, 1.000000000000000000, 0.9238795325112867385, 1.000000000000000000, 0.9238795325112867385, 1.000000000000000000, 0.9238795325112867385, 1.000000000000000000, 0.9238795325112867385, 1.000000000000000000, 0.9238795325112867385, 1.000000000000000000, 0.9238795325112867385, 1.000000000000000000, 0.9238795325112867385, 1.000000000000000000, 0.9238795325112867385, 1.000000000000000000, 0.9238795325112867385, 1.000000000000000000, 0.9238795325112867385, 1.000000000000000000, 0.9238795325112867385, 1.000000000000000000, 0.9238795325112867385, 1.000000000000000000, 0.9238795325112867385, 1.000000000000000000, 0.9238795325112867385, 1.000000000000000000, 0.9238795325112867385, 1.000000000000000000, 0.9238795325112867385, 1.000000000000000000, 0.9238795325112867385, 1.000000000000000000, 0.9238795325112867385, 1.000000000000000000, 0.9238795325112867385, 1.000000000000000000, 0.9238795325112867385, 1.000000000000000000, 0.9238795325112867385, 1.000000000000000000, 0.9238795325112867385, 1.000000000000000000, 0.9238795325112867385, 1.000000000000000000, 0.9238795325112867385, 1.000000000000000000, 0.9238795325112867385, 1.000000000000000000, 0.9238795325112867385, 1.000000000000000000, 0.9238795325112867385, 1.000000000000000000, 0.9238795325112867385, 1.000000000000000000, 0.9238795325112867385, 1.000000000000000000, 0.9238795325112867385, 1.000000000000000000, 0.9238795325112867385, 1.000000000000000000, 0.9238795325112867385, 1.000000000000000000, 0.9238795325112867385, 1.000000000000000000, 0.9238795325112867385, 1.000000000000000000, 0.9238795325112867385, 1.000000000000000000, 0.9238795325112867385, 1.000000000000000000, 0.9238795325112867385, 1.000000000000000000, 0.9238795325112867385, 1.000000000000000000, 0.9238795325112867385, 1.000000000000000000, 0.9238795325112867385, 1.000000000000000000, 0.9238795325112867385, 1.000000000000000000, 0.9238795325112867385, 1.000000000000000000, 0.9238795325112867385, 1.000000000000000000, 0.9238795325112867385, 1.000000000000000000, 0.9238795325112867385, 1.000000000000000000, 0.9238795325112867385, 1.000000000000000000, 0.9238795325112867385, 1.000000000000000000, 0.9238795325112867385, 1.000000000000000000, 0.9238795325112867385, 1.000000000000000000, 0.9238795325112867385, 1.000000000000000000, 0.9238795325112867385, 1.000000000000000000, 0.9238795325112867385, 1.000000000000000000, 0.9238795325112867385, 1.000000000000000000, 0.9238795325112867385, 1.000000000000000000, 0.9238795325112867385, 1.000000000000000000, 0.9238795325112867385, 1.000000000000000000, 0.9238795325112867385, 1.000000000000000000, 0.9238795325112867385, 1.000000000000000000, 0.9238795325112867385, 1.000000000000000000, 0.9238795325112867385, 1.000000000000000000, 0.9238795325112867385, 1.000000000000000000, 0.9238795325112867385, 1.000000000000000000, 0.9238795325112867385, 1.000000000000000000, 0.9493986726310960078, 0.9660721378631347278),
 ( 1.000000000000000000, 0.9238795325112867385, 1.000000000000000000, 0.9238795325112867385, 1.000000000000000000, 0.9238795325112867385, 1.000000000000000000, 0.9238795325112867385, 1.000000000000000000, 0.9238795325112867385, 1.000000000000000000, 0.9238795325112867385, 1.000000000000000000, 0.9238795325112867385, 1.000000000000000000, 0.9238795325112867385, 1.000000000000000000, 0.9238795325112867385, 1.000000000000000000, 0.9238795325112867385, 1.000000000000000000, 0.9238795325112867385, 1.000000000000000000, 0.9238795325112867385, 1.000000000000000000, 0.9238795325112867385, 1.000000000000000000, 0.9238795325112867385, 1.000000000000000000, 0.9238795325112867385, 1.000000000000000000, 0.9238795325112867385, 1.000000000000000000, 0.9238795325112867385, 1.000000000000000000, 0.9238795325112867385, 1.000000000000000000, 0.9238795325112867385, 1.000000000000000000, 0.9238795325112867385, 1.000000000000000000, 0.9238795325112867385, 1.000000000000000000, 0.9238795325112867385, 1.000000000000000000, 0.9238795325112867385, 1.000000000000000000, 0.9238795325112867385, 1.000000000000000000, 0.9238795325112867385, 1.000000000000000000, 0.9238795325112867385, 1.000000000000000000, 0.9238795325112867385, 1.000000000000000000, 0.9238795325112867385, 1.000000000000000000, 0.9238795325112867385, 1.000000000000000000, 0.9238795325112867385, 1.000000000000000000, 0.9238795325112867385, 1.000000000000000000, 0.9238795325112867385, 1.000000000000000000, 0.9238795325112867385, 1.000000000000000000, 0.9238795325112867385, 1.000000000000000000, 0.9238795325112867385, 1.000000000000000000, 0.9238795325112867385, 1.000000000000000000, 0.9238795325112867385, 1.000000000000000000, 0.9238795325112867385, 1.000000000000000000, 0.9238795325112867385, 1.000000000000000000, 0.9238795325112867385, 1.000000000000000000, 0.9238795325112867385, 1.000000000000000000, 0.9238795325112867385, 1.000000000000000000, 0.9238795325112867385, 1.000000000000000000, 0.9238795325112867385, 1.000000000000000000, 0.9238795325112867385, 1.000000000000000000, 0.9238795325112867385, 1.000000000000000000, 0.9238795325112867385, 1.000000000000000000, 0.9238795325112867385, 1.000000000000000000, 0.9238795325112867385, 1.000000000000000000, 0.9238795325112867385, 1.000000000000000000, 0.9238795325112867385, 1.000000000000000000, 0.9238795325112867385, 1.000000000000000000, 0.9238795325112867385, 1.000000000000000000, 0.9238795325112867385, 1.000000000000000000, 0.9238795325112867385, 1.000000000000000000, 0.9238795325112867385, 1.000000000000000000, 0.9238795325112867385, 1.000000000000000000, 0.9238795325112867385, 1.000000000000000000, 0.9238795325112867385, 1.000000000000000000, 0.9238795325112867385, 1.000000000000000000, 0.9238795325112867385, 1.000000000000000000, 0.9238795325112867385, 1.000000000000000000, 0.9238795325112867385, 1.000000000000000000, 0.9238795325112867385, 1.000000000000000000, 0.9238795325112867385, 1.000000000000000000, 0.9238795325112867385, 1.000000000000000000, 0.9238795325112867385, 1.000000000000000000, 0.9238795325112867385, 1.000000000000000000, 0.9238795325112867385, 1.000000000000000000, 0.9238795325112867385, 1.000000000000000000, 0.9238795325112867385, 1.000000000000000000, 0.9238795325112867385, 1.000000000000000000, 0.9238795325112867385, 1.000000000000000000, 0.9238795325112867385, 1.000000000000000000, 0.9238795325112867385, 1.000000000000000000, 0.9238795325112867385, 1.000000000000000000, 0.9238795325112867385, 1.000000000000000000, 0.9238795325112867385, 1.000000000000000000, 0.9238795325112867385, 1.000000000000000000, 0.9238795325112867385, 1.000000000000000000, 0.9238795325112867385, 1.000000000000000000, 0.9238795325112867385, 1.000000000000000000, 0.9238795325112867385, 1.000000000000000000, 0.9238795325112867385, 1.000000000000000000, 0.9238795325112867385, 1.000000000000000000, 0.9238795325112867385, 1.000000000000000000, 0.9238795325112867385, 1.000000000000000000, 0.9238795325112867385, 1.000000000000000000, 0.9238795325112867385, 1.000000000000000000, 0.9238795325112867385, 1.000000000000000000, 0.9238795325112867385, 1.000000000000000000, 0.9238795325112867385, 1.000000000000000000, 0.9238795325112867385, 1.000000000000000000, 0.9238795325112867385, 1.000000000000000000, 0.9238795325112867385, 1.000000000000000000, 0.9238795325112867385, 1.000000000000000000, 0.9238795325112867385, 1.000000000000000000, 0.9238795325112867385, 1.000000000000000000, 0.9238795325112867385, 1.000000000000000000, 0.9238795325112867385, 1.000000000000000000, 0.9238795325112867385, 1.000000000000000000, 0.9238795325112867385, 1.000000000000000000, 0.9238795325112867385, 1.000000000000000000, 0.9238795325112867385, 1.000000000000000000, 0.9238795325112867385, 1.000000000000000000, 0.9238795325112867385, 1.000000000000000000, 0.9238795325112867385, 1.000000000000000000, 0.9238795325112867385, 1.000000000000000000, 0.9238795325112867385, 1.000000000000000000, 0.9238795325112867385, 1.000000000000000000, 0.9238795325112867385, 1.000000000000000000, 0.9238795325112867385, 1.000000000000000000, 0.9238795325112867385, 1.000000000000000000, 0.9238795325112867385, 1.000000000000000000, 0.9238795325112867385, 1.000000000000000000, 0.9238795325112867385, 1.000000000000000000, 0.9238795325112867385, 1.000000000000000000, 0.9238795325112867385, 1.000000000000000000, 0.9238795325112867385, 1.000000000000000000, 0.9238795325112867385, 1.000000000000000000, 0.9238795325112867385, 1.000000000000000000, 0.9238795325112867385, 1.000000000000000000, 0.9238795325112867385, 1.000000000000000000, 0.9238795325112867385, 1.000000000000000000, 0.9238795325112867385, 1.000000000000000000, 0.9238795325112867385, 1.000000000000000000, 0.9238795325112867385, 1.000000000000000000, 0.9238795325112867385, 1.000000000000000000, 0.9238795325112867385, 1.000000000000000000, 0.9238795325112867385, 1.000000000000000000, 0.9238795325112867385, 1.000000000000000000, 0.9238795325112867385, 1.000000000000000000, 0.9238795325112867385, 1.000000000000000000, 0.9238795325112867385, 1.000000000000000000, 0.9238795325112867385, 1.000000000000000000, 0.9238795325112867385, 1.000000000000000000, 0.9238795325112867385, 1.000000000000000000, 0.9238795325112867385, 1.000000000000000000, 0.9238795325112867385, 1.000000000000000000, 0.9238795325112867385, 1.000000000000000000, 0.9238795325112867385, 1.000000000000000000, 0.9238795325112867385, 1.000000000000000000, 0.9238795325112867385, 1.000000000000000000, 0.9238795325112867385, 1.000000000000000000, 0.9238795325112867385, 1.000000000000000000, 0.9238795325112867385, 1.000000000000000000, 0.9238795325112867385, 1.000000000000000000, 0.9238795325112867385, 1.000000000000000000, 0.9238795325112867385, 1.000000000000000000, 0.9238795325112867385, 1.000000000000000000, 0.9238795325112867385, 1.000000000000000000, 0.9238795325112867385, 1.000000000000000000, 0.9238795325112867385, 1.000000000000000000, 0.9238795325112867385, 1.000000000000000000, 0.9238795325112867385, 1.000000000000000000, 0.9238795325112867385, 1.000000000000000000, 0.9238795325112867385, 1.000000000000000000, 0.9238795325112867385, 1.000000000000000000, 0.9238795325112867385, 1.000000000000000000, 0.9238795325112867385, 1.000000000000000000, 0.9238795325112867385, 1.000000000000000000, 0.9238795325112867385, 1.000000000000000000, 0.9238795325112867385, 1.000000000000000000, 0.9238795325112867385, 1.000000000000000000, 0.9238795325112867385, 1.000000000000000000, 0.9238795325112867385, 1.000000000000000000, 0.9238795325112867385, 1.000000000000000000, 0.9238795325112867385, 1.000000000000000000, 0.9238795325112867385, 1.000000000000000000, 0.9238795325112867385, 1.000000000000000000, 0.9238795325112867385, 1.000000000000000000, 0.9238795325112867385, 1.000000000000000000, 0.9238795325112867385, 1.000000000000000000, 0.9238795325112867385, 1.000000000000000000, 0.9238795325112867385, 1.000000000000000000, 0.9238795325112867385, 1.000000000000000000, 0.9238795325112867385, 1.000000000000000000, 0.9238795325112867385, 1.000000000000000000, 0.9238795325112867385, 1.000000000000000000, 0.9238795325112867385, 1.000000000000000000, 0.9238795325112867385, 1.000000000000000000, 0.9238795325112867385, 1.000000000000000000, 0.9238795325112867385, 1.000000000000000000, 0.9238795325112867385, 1.000000000000000000, 0.9238795325112867385, 1.000000000000000000, 0.9238795325112867385, 1.000000000000000000, 0.9238795325112867385, 1.000000000000000000, 0.9238795325112867385, 1.000000000000000000, 0.9238795325112867385, 1.000000000000000000, 0.9238795325112867385, 1.000000000000000000, 0.9238795325112867385, 1.000000000000000000, 0.9238795325112867385, 1.000000000000000000, 0.9238795325112867385, 1.000000000000000000, 0.9238795325112867385, 1.000000000000000000, 0.9238795325112867385, 1.000000000000000000, 0.9238795325112867385, 1.000000000000000000, 0.9238795325112867385, 1.000000000000000000, 0.9238795325112867385, 1.000000000000000000, 0.9238795325112867385, 1.000000000000000000, 0.9238795325112867385, 1.000000000000000000, 0.9238795325112867385, 1.000000000000000000, 0.9238795325112867385, 1.000000000000000000, 0.9238795325112867385, 1.000000000000000000, 0.9238795325112867385, 1.000000000000000000, 0.9238795325112867385, 1.000000000000000000, 0.9238795325112867385, 1.000000000000000000, 0.9238795325112867385, 1.000000000000000000, 0.9238795325112867385, 1.000000000000000000, 0.9238795325112867385, 1.000000000000000000, 0.9238795325112867385, 1.000000000000000000, 0.9238795325112867385, 1.000000000000000000, 0.9238795325112867385, 1.000000000000000000, 0.9238795325112867385, 1.000000000000000000, 0.9238795325112867385, 1.000000000000000000, 0.9238795325112867385, 1.000000000000000000, 0.9238795325112867385, 1.000000000000000000, 0.9238795325112867385, 1.000000000000000000, 0.9238795325112867385, 1.000000000000000000, 0.9238795325112867385, 1.000000000000000000, 0.9238795325112867385, 1.000000000000000000, 0.9238795325112867385, 1.000000000000000000, 0.9238795325112867385, 1.000000000000000000, 0.9238795325112867385, 1.000000000000000000, 0.9238795325112867385, 1.000000000000000000, 0.9238795325112867385, 1.000000000000000000, 0.9238795325112867385, 1.000000000000000000, 0.9238795325112867385, 1.000000000000000000, 0.9238795325112867385, 1.000000000000000000, 0.9238795325112867385, 1.000000000000000000, 0.9238795325112867385, 1.000000000000000000, 0.9238795325112867385, 1.000000000000000000, 0.9238795325112867385, 1.000000000000000000, 0.9238795325112867385, 1.000000000000000000, 0.9238795325112867385, 1.000000000000000000, 0.9238795325112867385, 1.000000000000000000, 0.9238795325112867385, 1.000000000000000000, 0.9238795325112867385, 1.000000000000000000, 0.9238795325112867385, 1.000000000000000000, 0.9238795325112867385, 1.000000000000000000, 0.9238795325112867385, 1.000000000000000000, 0.9238795325112867385, 1.000000000000000000, 0.9238795325112867385, 1.000000000000000000, 0.9238795325112867385, 1.000000000000000000, 0.9238795325112867385, 1.000000000000000000, 0.9238795325112867385, 1.000000000000000000, 0.9238795325112867385, 1.000000000000000000, 0.9238795325112867385, 1.000000000000000000, 0.9238795325112867385, 1.000000000000000000, 0.9238795325112867385, 1.000000000000000000, 0.9238795325112867385, 1.000000000000000000, 0.9238795325112867385, 1.000000000000000000, 0.9238795325112867385, 1.000000000000000000, 0.9238795325112867385, 1.000000000000000000, 0.9238795325112867385, 1.000000000000000000, 0.9238795325112867385, 1.000000000000000000, 0.9238795325112867385, 1.000000000000000000, 0.9238795325112867385, 1.000000000000000000, 0.9238795325112867385, 1.000000000000000000, 0.9238795325112867385, 1.000000000000000000, 0.9238795325112867385, 1.000000000000000000, 0.9238795325112867385, 1.000000000000000000, 0.9238795325112867385, 1.000000000000000000, 0.9238795325112867385, 1.000000000000000000, 0.9238795325112867385, 1.000000000000000000, 0.9238795325112867385, 1.000000000000000000, 0.9238795325112867385, 1.000000000000000000, 0.9493986726310960078, 0.9660721378631347278) ) ) 
 REPRESENTATION_ITEM ( '' )  SURFACE ( )  );
#25799=DIRECTION ( 'NONE',  ( -0.000000000000000000, -0.000000000000000000, -1.000000000000000000 ) ) ;
#25808=EDGE_CURVE ( 'NONE', #47864, #30692, #33774, .T. ) ;
#25810=CARTESIAN_POINT ( 'NONE',  ( -7.778174593052023411, 7.778174593052023411, 77.50000000409676204 ) ) ;
#25811=DIRECTION ( 'NONE',  ( -0.000000000000000000, 0.000000000000000000, 1.000000000000000000 ) ) ;
#25827=DIRECTION ( 'NONE',  ( -1.000000000000000000, 0.000000000000000000, 0.000000000000000000 ) ) ;
#25828=CARTESIAN_POINT ( 'NONE',  ( 4.220049686691941027, -10.18810118749999738, 98.12500000204836681 ) ) ;
#25834=EDGE_CURVE ( 'NONE', #18351, #11931, #49365, .T. ) ;
#25837=CARTESIAN_POINT ( 'NONE',  ( -7.778174593052023411, 7.778174593052023411, 77.31249999999997158 ) ) ;
#25842=CARTESIAN_POINT ( 'NONE',  ( -10.18810118749999916, 0.000000000000000000, 92.03125000204836681 ) ) ;
#25855=CARTESIAN_POINT ( 'NONE',  ( 10.18810118749999916, 4.220049686691935698, 82.00000000204836681 ) ) ;
#25868=CARTESIAN_POINT ( 'NONE',  ( -11.00000000000000000, 0.000000000000000000, 75.99999999999998579 ) ) ;
#25888=CARTESIAN_POINT ( 'NONE',  ( 11.00000000000000000, 1.347111479062088405E-15, 79.74999999999998579 ) ) ;
#25899=EDGE_CURVE ( 'NONE', #40560, #8028, #42364, .T. ) ;
#25901=CARTESIAN_POINT ( 'NONE',  ( 2.020667218593132706E-15, -11.00000000000000000, 114.0625000040967763 ) ) ;
#25917=CARTESIAN_POINT ( 'NONE',  ( -10.18810118749999916, 4.220049686691934809, 85.93750000204839523 ) ) ;
#25918=CARTESIAN_POINT ( 'NONE',  ( -6.238412754330611322E-16, 10.18810118749999916, 112.2812500020483810 ) ) ;
#25929=AXIS2_PLACEMENT_3D ( 'NONE', #71698, #3428, #37388 ) ;
#25933=CARTESIAN_POINT ( 'NONE',  ( -10.18810118749999916, 0.000000000000000000, 110.0312500020483668 ) ) ;
#25957=CARTESIAN_POINT ( 'NONE',  ( -10.99999999999989342, 4.556349186104152515, 72.90624999999995737 ) ) ;
#25967=CARTESIAN_POINT ( 'NONE',  ( -10.18810118749999738, -4.220049686691941915, 81.25000000204838102 ) ) ;
#25969=CARTESIAN_POINT ( 'NONE',  ( 4.556349186104051263, -10.99999999999999822, 95.96875000000000000 ) ) ;
#25997=CARTESIAN_POINT ( 'NONE',  ( -11.00000000000000000, 0.000000000000000000, 80.68750000409677625 ) ) ;
#26003=EDGE_CURVE ( 'NONE', #72648, #39873, #29950, .T. ) ;
#26014=CARTESIAN_POINT ( 'NONE',  ( 11.00000000000000000, 1.347111479062088405E-15, 94.74999999999998579 ) ) ;
#26017=CARTESIAN_POINT ( 'NONE',  ( 10.18810118749999916, 4.220049686691935698, 74.50000000204838102 ) ) ;
#26026=CARTESIAN_POINT ( 'NONE',  ( -4.220049686691935698, 10.18810118749999916, 82.75000000204838102 ) ) ;
#26033=CARTESIAN_POINT ( 'NONE',  ( -7.204075437095965206, -7.204075437095968759, 94.84375000204838102 ) ) ;
#26040=CARTESIAN_POINT ( 'NONE',  ( 4.220049686691941027, -10.18810118749999738, 98.50000000204838102 ) ) ;
#26041=AXIS2_PLACEMENT_3D ( 'NONE', #12286, #28894, #6637 ) ;
#26058=CARTESIAN_POINT ( 'NONE',  ( 4.220049686691941027, -10.18810118749999738, 101.1250000020483810 ) ) ;
#26071=EDGE_CURVE ( 'NONE', #48097, #31332, #35255, .T. ) ;
#26078=CARTESIAN_POINT ( 'NONE',  ( -7.778174593052020747, -7.778174593052023411, 110.6875000000000000 ) ) ;
#26092=CARTESIAN_POINT ( 'NONE',  ( -4.556349186104045934, 11.00000000000000000, 98.40625000409677625 ) ) ;
#26115=CARTESIAN_POINT ( 'NONE',  ( 4.220049686691941027, -10.18810118749999738, 104.5000000020483668 ) ) ;
#26122=CARTESIAN_POINT ( 'NONE',  ( 10.18810118750000093, -4.220049686691933033, 73.18750000204838102 ) ) ;
#26125=CARTESIAN_POINT ( 'NONE',  ( 0.000000000000000000, 0.000000000000000000, 118.0000000000000000 ) ) ;
#26137=CARTESIAN_POINT ( 'NONE',  ( 4.220049686691941027, -10.18810118749999738, 113.5000000020483810 ) ) ;
#26154=CARTESIAN_POINT ( 'NONE',  ( -10.18810118749999916, 4.220049686691934809, 115.5625000020483810 ) ) ;
#26168=CARTESIAN_POINT ( 'NONE',  ( -7.778174593052020747, -7.778174593052023411, 94.18750000000000000 ) ) ;
#26170=CYLINDRICAL_SURFACE ( 'NONE', #34292, 11.00000000000000000 ) ;
#26177=CARTESIAN_POINT ( 'NONE',  ( 5.499989586027935751, 9.526285454130809072, 66.68677389048282578 ) ) ;
#26185=CYLINDRICAL_SURFACE ( 'NONE', #31171, 11.00000000000000000 ) ;
#26186=CARTESIAN_POINT ( 'NONE',  ( 0.000000000000000000, 0.000000000000000000, 41.99999999999999289 ) ) ;
#26196=ORIENTED_EDGE ( 'NONE', *, *, #38242, .T. ) ;
#26198=CARTESIAN_POINT ( 'NONE',  ( -11.00000000000000000, 0.000000000000000000, 81.99999999999998579 ) ) ;
#26202=FACE_OUTER_BOUND ( 'NONE', #31302, .T. ) ;
#26203=CARTESIAN_POINT ( 'NONE',  ( -10.18810118749999738, -4.220049686691941915, 94.75000000204838102 ) ) ;
#26204=CARTESIAN_POINT ( 'NONE',  ( -4.556349186104045934, 11.00000000000000000, 93.71874999999998579 ) ) ;
#26210=VERTEX_POINT ( 'NONE', #57720 ) ;
#26216=CARTESIAN_POINT ( 'NONE',  ( -4.220049686691937474, -10.18810118749999738, 89.31250000204838102 ) ) ;
#26222=CARTESIAN_POINT ( 'NONE',  ( 2.020667218593132706E-15, -11.00000000000000000, 85.56250000409676204 ) ) ;
#26230=CARTESIAN_POINT ( 'NONE',  ( -4.220049686691937474, -10.18810118749999738, 84.43750000204838102 ) ) ;
#26232=( BOUNDED_CURVE ( )  B_SPLINE_CURVE ( 2, ( #903, #54050, #1638, #64982, #35959, #58979, #36330, #1992, #23890 ),
 .UNSPECIFIED., .F., .F. ) 
 B_SPLINE_CURVE_WITH_KNOTS ( ( 3, 2, 2, 2, 3 ),
 ( 0.9117647058823530326, 0.9154411764705883137, 0.9191176470588235947, 0.9227941176470588758, 0.9264705882352941568 ),
 .UNSPECIFIED. ) 
 CURVE ( )  GEOMETRIC_REPRESENTATION_ITEM ( )  RATIONAL_B_SPLINE_CURVE ( ( 0.9999999999999976685, 0.9238795325112890700, 1.000000000000000000, 0.9238795325112867385, 1.000000000000000000, 0.9238795325112867385, 1.000000000000000000, 0.9238795325112867385, 1.000000000000000000 ) ) 
 REPRESENTATION_ITEM ( '' )  );
#26238=VECTOR ( 'NONE', #47289, 1000.000000000000000 ) ;
#26245=CARTESIAN_POINT ( 'NONE',  ( -4.556349186104048599, -10.99999999999999822, 76.28125000000000000 ) ) ;
#26260=CARTESIAN_POINT ( 'NONE',  ( 11.00000000000000000, 1.347111479062088405E-15, 115.9375000040967763 ) ) ;
#26265=CARTESIAN_POINT ( 'NONE',  ( -4.556349186104045934, 11.00000000000000000, 74.21875000000001421 ) ) ;
#26268=CARTESIAN_POINT ( 'NONE',  ( 4.556349186104045934, 11.00000000000000000, 110.2187500040967763 ) ) ;
#26274=CARTESIAN_POINT ( 'NONE',  ( 7.778174593052023411, -7.778174593052021635, 114.2500000040967763 ) ) ;
#26291=CARTESIAN_POINT ( 'NONE',  ( -10.18810118749999738, -4.220049686691941915, 84.62500000204838102 ) ) ;
#26292=CARTESIAN_POINT ( 'NONE',  ( -6.238412754330611322E-16, 10.18810118749999916, 115.2812500020483810 ) ) ;
#26306=CARTESIAN_POINT ( 'NONE',  ( -7.204075437095967871, 7.204075437095967871, 109.8437500020483810 ) ) ;
#26317=CARTESIAN_POINT ( 'NONE',  ( 11.00000000000000355, -4.556349186104044158, 72.34375000409677625 ) ) ;
#26328=EDGE_LOOP ( 'NONE', ( #72745, #47139, #23232, #54647 ) ) ;
#26332=CARTESIAN_POINT ( 'NONE',  ( -10.99999999999999822, -4.556349186104053040, 77.78125000409680467 ) ) ;
#26346=CARTESIAN_POINT ( 'NONE',  ( -4.220049686691937474, -10.18810118749999738, 78.43750000204838102 ) ) ;
#26349=CARTESIAN_POINT ( 'NONE',  ( -11.00000000000000000, 0.000000000000000000, 91.00000000000000000 ) ) ;
#26354=CARTESIAN_POINT ( 'NONE',  ( -11.00000000000010658, 4.556349186103942017, 89.40624999999998579 ) ) ;
#26362=CARTESIAN_POINT ( 'NONE',  ( -11.00000000000000000, 0.000000000000000000, 118.0000000000000000 ) ) ;
#26364=DIRECTION ( 'NONE',  ( -0.000000000000000000, -0.000000000000000000, -1.000000000000000000 ) ) ;
#26374=CARTESIAN_POINT ( 'NONE',  ( 11.00000000000000000, 1.347111479062088405E-15, 81.43750000409677625 ) ) ;
#26391=CARTESIAN_POINT ( 'NONE',  ( -10.18810118749999916, 4.220049686691934809, 78.06250000204838102 ) ) ;
#26400=CARTESIAN_POINT ( 'NONE',  ( 4.220049686691934809, 10.18810118749999916, 87.06250000204838102 ) ) ;
#26403=DIRECTION ( 'NONE',  ( -0.000000000000000000, -0.000000000000000000, -1.000000000000000000 ) ) ;
#26406=CARTESIAN_POINT ( 'NONE',  ( -7.204075437095965206, -7.204075437095968759, 93.34375000204838102 ) ) ;
#26415=CARTESIAN_POINT ( 'NONE',  ( -10.18810118749999916, 0.000000000000000000, 90.53125000204836681 ) ) ;
#26431=ORIENTED_EDGE ( 'NONE', *, *, #24483, .T. ) ;
#26434=CARTESIAN_POINT ( 'NONE',  ( 10.18810118749999916, 1.247682550866122264E-15, 98.40625000204838102 ) ) ;
#26451=CARTESIAN_POINT ( 'NONE',  ( -11.00000000000000000, 0.000000000000000000, 111.9999999999999858 ) ) ;
#26460=CARTESIAN_POINT ( 'NONE',  ( 11.00000000000000000, 1.347111479062088405E-15, 102.4375000040967763 ) ) ;
#26464=DIRECTION ( 'NONE',  ( -0.000000000000000000, -0.000000000000000000, -1.000000000000000000 ) ) ;
#26469=CARTESIAN_POINT ( 'NONE',  ( -4.556349186104045934, 11.00000000000000000, 96.90625000409677625 ) ) ;
#26491=CARTESIAN_POINT ( 'NONE',  ( -4.220049686691935698, 10.18810118749999916, 103.7500000020483668 ) ) ;
#26499=EDGE_CURVE ( 'NONE', #36393, #2485, #30511, .T. ) ;
#26502=CARTESIAN_POINT ( 'NONE',  ( 1.871523826299183495E-15, -10.18810118749999916, 111.5312500020483668 ) ) ;
#26510=CARTESIAN_POINT ( 'NONE',  ( 4.220049686691941027, -10.18810118749999738, 107.5000000020483668 ) ) ;
#26529=CARTESIAN_POINT ( 'NONE',  ( 4.220049686691934809, 10.18810118749999916, 115.1875000020483668 ) ) ;
#26530=CARTESIAN_POINT ( 'NONE',  ( 4.556349186104052151, -10.99999999999999822, 84.15625000409676204 ) ) ;
#26542=DIRECTION ( 'NONE',  ( -0.000000000000000000, -0.000000000000000000, -1.000000000000000000 ) ) ;
#26543=CARTESIAN_POINT ( 'NONE',  ( -11.00000000000000000, 0.000000000000000000, 118.0000000000000000 ) ) ;
#26551=DIRECTION ( 'NONE',  ( -0.000000000000000000, -0.000000000000000000, -1.000000000000000000 ) ) ;
#26553=CARTESIAN_POINT ( 'NONE',  ( 11.00000000000000000, 1.347111479062088405E-15, 82.93750000409677625 ) ) ;
#26578=CARTESIAN_POINT ( 'NONE',  ( -10.99999999999994849, 4.556349186104097448, 95.40625000000000000 ) ) ;
#26583=CARTESIAN_POINT ( 'NONE',  ( 10.18810118749999916, 1.247682550866122264E-15, 96.90625000204838102 ) ) ;
#26598=CARTESIAN_POINT ( 'NONE',  ( 4.220049686691934809, 10.18810118749999916, 85.56250000204838102 ) ) ;
#26609=ORIENTED_EDGE ( 'NONE', *, *, #2112, .T. ) ;
#26611=CARTESIAN_POINT ( 'NONE',  ( -7.204075437095967871, 7.204075437095967871, 80.96875000204836681 ) ) ;
#26617=ORIENTED_EDGE ( 'NONE', *, *, #12718, .T. ) ;
#26634=VERTEX_POINT ( 'NONE', #56511 ) ;
#26647=CARTESIAN_POINT ( 'NONE',  ( -11.00000000000000000, 0.000000000000000000, 69.99999999999998579 ) ) ;
#26658=CARTESIAN_POINT ( 'NONE',  ( -7.778174593052023411, 7.778174593052023411, 110.5000000040967763 ) ) ;
#26667=ORIENTED_EDGE ( 'NONE', *, *, #61705, .T. ) ;
#26676=CARTESIAN_POINT ( 'NONE',  ( -10.18810118749999916, 4.220049686691934809, 112.5625000020483810 ) ) ;
#26690=( BOUNDED_CURVE ( )  B_SPLINE_CURVE ( 2, ( #11706, #43, #40748, #17361, #12075, #6434, #5684, #19124, #29436 ),
 .UNSPECIFIED., .F., .F. ) 
 B_SPLINE_CURVE_WITH_KNOTS ( ( 3, 2, 2, 2, 3 ),
 ( 0.5000000000000001110, 0.5036764705882353921, 0.5073529411764706731, 0.5110294117647059542, 0.5147058823529412352 ),
 .UNSPECIFIED. ) 
 CURVE ( )  GEOMETRIC_REPRESENTATION_ITEM ( )  RATIONAL_B_SPLINE_CURVE ( ( 0.9999999999999976685, 0.9238795325112890700, 1.000000000000000000, 0.9238795325112867385, 1.000000000000000000, 0.9238795325112867385, 1.000000000000000000, 0.9238795325112844070, 1.000000000000002220 ) ) 
 REPRESENTATION_ITEM ( '' )  );
#26691=CARTESIAN_POINT ( 'NONE',  ( -6.238412754330611322E-16, 10.18810118749999916, 109.6562500020483668 ) ) ;
#26692=EDGE_CURVE ( 'NONE', #15625, #53323, #13234, .T. ) ;
#26731=CARTESIAN_POINT ( 'NONE',  ( -10.18810118749999916, 0.000000000000000000, 82.65625000204838102 ) ) ;
#26734=CARTESIAN_POINT ( 'NONE',  ( -10.99999999999999822, -4.556349186104052151, 88.09375000000000000 ) ) ;
#26760=CARTESIAN_POINT ( 'NONE',  ( -4.556349186104045934, 11.00000000000000000, 111.9062500040967763 ) ) ;
#26766=CARTESIAN_POINT ( 'NONE',  ( 4.556349186104051263, -10.99999999999999822, 82.65625000409677625 ) ) ;
#26782=CARTESIAN_POINT ( 'NONE',  ( 11.00000000000000000, 1.347111479062088405E-15, 81.24999999999998579 ) ) ;
#26783=CARTESIAN_POINT ( 'NONE',  ( 10.18810118750000093, -4.220049686691933921, 77.31250000204836681 ) ) ;
#26792=CARTESIAN_POINT ( 'NONE',  ( 4.220049686691934809, 10.18810118749999916, 85.56250000204838102 ) ) ;
#26793=VERTEX_POINT ( 'NONE', #15935 ) ;
#26798=CARTESIAN_POINT ( 'NONE',  ( 7.204075437095966983, 7.204075437095967871, 97.09375000204836681 ) ) ;
#26801=ORIENTED_EDGE ( 'NONE', *, *, #473, .T. ) ;
#26806=CARTESIAN_POINT ( 'NONE',  ( 10.18810118749999916, 4.220049686691935698, 94.37500000204839523 ) ) ;
#26823=CARTESIAN_POINT ( 'NONE',  ( -6.238412754330611322E-16, 10.18810118749999916, 100.2812500020483810 ) ) ;
#26826=CARTESIAN_POINT ( 'NONE',  ( 11.00000000000000000, 1.347111479062088405E-15, 108.2499999999999858 ) ) ;
#26851=LINE ( 'NONE', #9884, #13391 ) ;
#26856=CARTESIAN_POINT ( 'NONE',  ( 4.556349186104045934, 11.00000000000000000, 101.2187500040967905 ) ) ;
#26873=FACE_OUTER_BOUND ( 'NONE', #6301, .T. ) ;
#26878=CARTESIAN_POINT ( 'NONE',  ( -6.238412754330611322E-16, 10.18810118749999916, 103.6562500020483810 ) ) ;
#26886=CARTESIAN_POINT ( 'NONE',  ( -7.204075437095967871, 7.204075437095967871, 115.4687500020483810 ) ) ;
#26895=CARTESIAN_POINT ( 'NONE',  ( 4.220049686691934809, 10.18810118749999916, 111.0625000020483810 ) ) ;
#26904=CARTESIAN_POINT ( 'NONE',  ( -4.220049686691937474, -10.18810118749999738, 71.31250000204836681 ) ) ;
#26932=DIRECTION ( 'NONE',  ( -0.000000000000000000, -0.000000000000000000, -1.000000000000000000 ) ) ;
#26942=CARTESIAN_POINT ( 'NONE',  ( 11.00000000000000355, -4.556349186104044158, 79.65625000000000000 ) ) ;
#26952=EDGE_LOOP ( 'NONE', ( #60761, #32372, #55865, #58832, #44272, #66110, #73682, #72103, #32478, #20481, #25715, #71946, #20865, #11059, #70970, #18912, #46832, #48306, #5192, #59990, #62492, #46803, #6032, #23955, #36443, #65223, #69865, #33054, #16106, #65912, #62546, #65483, #35140, #41783, #56342, #8978, #49078, #18876, #63992, #18905, #55762, #30990, #55884, #59892, #9519, #3825, #43781, #31001, #61154, #500, #71854, #57726, #16206, #40290, #38185, #63258, #66392, #18170, #51222, #60417, #71691, #53988, #21137, #69274, #67544, #39917, #54344, #28162, #22690, #54997 ) ) ;
#26957=CARTESIAN_POINT ( 'NONE',  ( 11.00000000000005151, 4.556349186103993532, 94.84374999999997158 ) ) ;
#26961=CARTESIAN_POINT ( 'NONE',  ( -7.204075437095965206, -7.204075437095968759, 91.84375000204838102 ) ) ;
#26962=CARTESIAN_POINT ( 'NONE',  ( 11.00000000000010658, 4.556349186103942017, 93.34375000000000000 ) ) ;
#26976=CARTESIAN_POINT ( 'NONE',  ( -10.18810118749999916, 4.220049686691934809, 82.93750000204838102 ) ) ;
#26982=LINE ( 'NONE', #61695, #55521 ) ;
#26989=CARTESIAN_POINT ( 'NONE',  ( -10.18810118749999916, 4.220049686691934809, 79.56250000204836681 ) ) ;
#26994=ORIENTED_EDGE ( 'NONE', *, *, #55529, .F. ) ;
#27028=CARTESIAN_POINT ( 'NONE',  ( 11.00000000000000000, 1.347111479062088405E-15, 70.74999999999998579 ) ) ;
#27031=CARTESIAN_POINT ( 'NONE',  ( 11.00000000000007994, 4.556349186103967774, 110.0312500040967763 ) ) ;
#27055=CARTESIAN_POINT ( 'NONE',  ( 10.18810118749999916, 4.220049686691935698, 106.0000000020483668 ) ) ;
#27069=CARTESIAN_POINT ( 'NONE',  ( 1.871523826299183495E-15, -10.18810118749999916, 102.9062500020483810 ) ) ;
#27088=CARTESIAN_POINT ( 'NONE',  ( -4.220049686691935698, 10.18810118749999916, 81.25000000204836681 ) ) ;
#27101=ORIENTED_EDGE ( 'NONE', *, *, #20691, .T. ) ;
#27107=CARTESIAN_POINT ( 'NONE',  ( 10.18810118749999916, 4.220049686691935698, 71.50000000204838102 ) ) ;
#27110=CARTESIAN_POINT ( 'NONE',  ( 11.00000000000000355, -4.556349186104045046, 91.65625000000001421 ) ) ;
#27115=DIRECTION ( 'NONE',  ( -0.000000000000000000, -0.000000000000000000, -1.000000000000000000 ) ) ;
#27134=CARTESIAN_POINT ( 'NONE',  ( -10.99999999999999822, 0.000000000000000000, 112.1875000040967763 ) ) ;
#27138=CARTESIAN_POINT ( 'NONE',  ( -10.99999999999999822, -4.556349186104052151, 77.78125000409680467 ) ) ;
#27144=CARTESIAN_POINT ( 'NONE',  ( -11.00000000000000000, 0.000000000000000000, 98.68750000409677625 ) ) ;
#27150=CARTESIAN_POINT ( 'NONE',  ( -7.204075437095965206, -7.204075437095968759, 116.2187500020483810 ) ) ;
#27153=CARTESIAN_POINT ( 'NONE',  ( -4.220049686691935698, 10.18810118749999916, 77.87500000204838102 ) ) ;
#27161=CARTESIAN_POINT ( 'NONE',  ( -6.238412754330611322E-16, 10.18810118749999916, 84.15625000204838102 ) ) ;
#27163=CARTESIAN_POINT ( 'NONE',  ( 10.99999999999989697, -4.556349186104149851, 90.34375000409677625 ) ) ;
#27164=CARTESIAN_POINT ( 'NONE',  ( -6.735557395310442023E-16, 11.00000000000000000, 105.6250000000000000 ) ) ;
#27172=CARTESIAN_POINT ( 'NONE',  ( 10.18810118749999916, 1.247682550866122264E-15, 94.28125000204836681 ) ) ;
#27184=CARTESIAN_POINT ( 'NONE',  ( 7.778174593052023411, -7.778174593052021635, 96.25000000409677625 ) ) ;
#27190=CARTESIAN_POINT ( 'NONE',  ( -10.18810118749999916, 4.220049686691934809, 94.56250000204838102 ) ) ;
#27193=CARTESIAN_POINT ( 'NONE',  ( -6.735557395310442023E-16, 11.00000000000000000, 105.6250000000000000 ) ) ;
#27216=CYLINDRICAL_SURFACE ( 'NONE', #6615, 11.00000000000000000 ) ;
#27218=CARTESIAN_POINT ( 'NONE',  ( 5.499985535179889418, 9.526287792881966254, 118.0000000000000000 ) ) ;
#27222=CARTESIAN_POINT ( 'NONE',  ( 7.778174593052021635, 7.778174593052023411, 101.1250000040967763 ) ) ;
#27243=CARTESIAN_POINT ( 'NONE',  ( -7.204075437095965206, -7.204075437095968759, 102.7187500020483668 ) ) ;
#27254=ORIENTED_EDGE ( 'NONE', *, *, #68944, .T. ) ;
#27255=CARTESIAN_POINT ( 'NONE',  ( 7.204075437095968759, -7.204075437095966983, 114.7187500020483810 ) ) ;
#27262=CARTESIAN_POINT ( 'NONE',  ( 11.00000000000000000, 1.347111479062088405E-15, 103.9375000040967763 ) ) ;
#27263=CARTESIAN_POINT ( 'NONE',  ( -10.18810118749999916, 4.220049686691934809, 109.9375000020483952 ) ) ;
#27280=CARTESIAN_POINT ( 'NONE',  ( 4.220049686691934809, 10.18810118749999916, 113.6875000020483810 ) ) ;
#27295=CARTESIAN_POINT ( 'NONE',  ( -11.00000000000000000, 0.000000000000000000, 93.99999999999998579 ) ) ;
#27311=DIRECTION ( 'NONE',  ( -0.000000000000000000, -0.000000000000000000, -1.000000000000000000 ) ) ;
#27323=CARTESIAN_POINT ( 'NONE',  ( 11.00000000000000000, 1.347111479062088405E-15, 82.74999999999998579 ) ) ;
#27329=CARTESIAN_POINT ( 'NONE',  ( -4.220049686691937474, -10.18810118749999738, 91.93750000204836681 ) ) ;
#27334=CARTESIAN_POINT ( 'NONE',  ( -11.00000000000000000, 0.000000000000000000, 95.49999999999998579 ) ) ;
#27335=EDGE_LOOP ( 'NONE', ( #43114, #54473, #15291, #45624 ) ) ;
#27341=( BOUNDED_CURVE ( )  B_SPLINE_CURVE ( 1, ( #49576, #33364 ),
 .UNSPECIFIED., .F., .F. ) 
 B_SPLINE_CURVE_WITH_KNOTS ( ( 2, 2 ),
 ( 0.000000000000000000, 1.000000000000000000 ),
 .UNSPECIFIED. ) 
 CURVE ( )  GEOMETRIC_REPRESENTATION_ITEM ( )  RATIONAL_B_SPLINE_CURVE ( ( 0.9660722070829228514, 0.9660722070829228514 ) ) 
 REPRESENTATION_ITEM ( '' )  );
#27342=CARTESIAN_POINT ( 'NONE',  ( 4.220049686691941027, -10.18810118749999738, 80.50000000204839523 ) ) ;
#27349=CARTESIAN_POINT ( 'NONE',  ( -11.00000000000000000, 0.000000000000000000, 92.49999999999998579 ) ) ;
#27356=CARTESIAN_POINT ( 'NONE',  ( 10.18810118749999916, 1.247682550866122264E-15, 77.40625000204836681 ) ) ;
#27391=CARTESIAN_POINT ( 'NONE',  ( -11.00000000000000000, 4.556349186104045934, 68.40624999999998579 ) ) ;
#27419=CARTESIAN_POINT ( 'NONE',  ( -10.18810118749999916, 0.000000000000000000, 108.1562500020483668 ) ) ;
#27432=CARTESIAN_POINT ( 'NONE',  ( 4.220049686691941027, -10.18810118749999738, 101.5000000020483668 ) ) ;
#27450=( BOUNDED_CURVE ( )  B_SPLINE_CURVE ( 2, ( #61768, #7028, #5919, #276, #63242, #18344, #6295, #41358, #62869 ),
 .UNSPECIFIED., .F., .F. ) 
 B_SPLINE_CURVE_WITH_KNOTS ( ( 3, 2, 2, 2, 3 ),
 ( 0.9558823529411766273, 0.9595588235294119084, 0.9632352941176471894, 0.9669117647058825815, 0.9705882352941178626 ),
 .UNSPECIFIED. ) 
 CURVE ( )  GEOMETRIC_REPRESENTATION_ITEM ( )  RATIONAL_B_SPLINE_CURVE ( ( 0.9999999999999976685, 0.9238795325112890700, 1.000000000000000000, 0.9238795325112867385, 1.000000000000000000, 0.9238795325112867385, 1.000000000000000000, 0.9238795325112821866, 1.000000000000004663 ) ) 
 REPRESENTATION_ITEM ( '' )  );
#27454=CARTESIAN_POINT ( 'NONE',  ( -4.220049686691937474, -10.18810118749999738, 80.31250000204836681 ) ) ;
#27461=LINE ( 'NONE', #50475, #37861 ) ;
#27471=EDGE_LOOP ( 'NONE', ( #58620, #60448, #53398, #70680, #59398, #70714, #11855, #25389, #29762, #48664, #33740, #6560, #73879, #56915, #10391, #46217, #33690, #60133, #6980, #28380, #29613, #12618, #33018, #34440, #16736, #11881, #60102, #13087, #20505, #48020, #17837, #26609, #44985, #53735, #23762, #73496, #33977, #40675, #6880, #57031, #47840, #47229, #52147, #46819, #6507, #25297, #30418, #43055, #34608, #1866, #49489, #26801, #36640, #23856, #34090, #17591, #45144, #42305, #14272, #38376, #74011, #32391, #9908, #2299, #54280, #6145, #66073, #24558, #56503, #52533, #24176 ) ) ;
#27474=CARTESIAN_POINT ( 'NONE',  ( -4.220049686691935698, 10.18810118749999916, 76.37500000204838102 ) ) ;
#27477=CARTESIAN_POINT ( 'NONE',  ( -11.00000000000000000, 0.000000000000000000, 89.50000000000000000 ) ) ;
#27508=CARTESIAN_POINT ( 'NONE',  ( 4.556349186104051263, -10.99999999999999822, 72.15625000409677625 ) ) ;
#27522=CARTESIAN_POINT ( 'NONE',  ( -10.18810118749999916, 0.000000000000000000, 117.5312500020483810 ) ) ;
#27525=CARTESIAN_POINT ( 'NONE',  ( -4.220049686691935698, 10.18810118749999916, 70.37500000204838102 ) ) ;
#27531=CARTESIAN_POINT ( 'NONE',  ( 2.020667218593132706E-15, -11.00000000000000000, 79.56250000409677625 ) ) ;
#27534=CARTESIAN_POINT ( 'NONE',  ( 7.204075437095968759, -7.204075437095966983, 79.09375000204838102 ) ) ;
#27546=CARTESIAN_POINT ( 'NONE',  ( -4.220049686691935698, 10.18810118749999916, 90.25000000204838102 ) ) ;
#27549=EDGE_CURVE ( 'NONE', #41579, #42385, #20492, .T. ) ;
#27555=ORIENTED_EDGE ( 'NONE', *, *, #22758, .T. ) ;
#27561=CARTESIAN_POINT ( 'NONE',  ( -11.00000000000000533, 11.00000000000000000, 41.99999999999999289 ) ) ;
#27567=CARTESIAN_POINT ( 'NONE',  ( 7.204075437095966983, 7.204075437095967871, 94.09375000204838102 ) ) ;
#27570=CARTESIAN_POINT ( 'NONE',  ( 7.778174593052023411, -7.778174593052021635, 109.5625000000000000 ) ) ;
#27597=CARTESIAN_POINT ( 'NONE',  ( 2.020667218593132706E-15, -11.00000000000000000, 93.06250000409677625 ) ) ;
#27606=AXIS2_PLACEMENT_3D ( 'NONE', #55800, #24049, #703 ) ;
#27621=CARTESIAN_POINT ( 'NONE',  ( -4.220049686691935698, 10.18810118749999916, 97.75000000204838102 ) ) ;
#27626=CARTESIAN_POINT ( 'NONE',  ( 4.556349186104045934, 11.00000000000000000, 98.03124999999997158 ) ) ;
#27631=CARTESIAN_POINT ( 'NONE',  ( -4.220049686691937474, -10.18810118749999738, 111.4375000020483810 ) ) ;
#27639=CARTESIAN_POINT ( 'NONE',  ( -11.00000000000000000, 0.000000000000000000, 103.1875000040967763 ) ) ;
#27640=CARTESIAN_POINT ( 'NONE',  ( 4.220049686691934809, 10.18810118749999916, 112.5625000020483810 ) ) ;
#27648=DIRECTION ( 'NONE',  ( -0.000000000000000000, -0.000000000000000000, -1.000000000000000000 ) ) ;
#27656=CARTESIAN_POINT ( 'NONE',  ( 10.18810118749999916, 4.220049686691935698, 110.5000000020483810 ) ) ;
#27681=CARTESIAN_POINT ( 'NONE',  ( -10.99999999999978684, -4.556349186104264426, 82.28125000409677625 ) ) ;
#27706=CARTESIAN_POINT ( 'NONE',  ( 4.220049686691934809, 10.18810118749999916, 91.18750000204836681 ) ) ;
#27712=EDGE_LOOP ( 'NONE', ( #35560, #74414, #74635, #36185 ) ) ;
#27714=DIRECTION ( 'NONE',  ( -0.000000000000000000, -0.000000000000000000, -1.000000000000000000 ) ) ;
#27719=CARTESIAN_POINT ( 'NONE',  ( 7.204075437095968759, -7.204075437095966983, 85.09375000204836681 ) ) ;
#27733=CARTESIAN_POINT ( 'NONE',  ( -10.18810118749999916, 0.000000000000000000, 79.65625000204836681 ) ) ;
#27762=DIRECTION ( 'NONE',  ( -0.000000000000000000, -0.000000000000000000, -1.000000000000000000 ) ) ;
#27767=CARTESIAN_POINT ( 'NONE',  ( -4.556349186104047710, -10.99999999999999822, 71.78125000000000000 ) ) ;
#27772=ORIENTED_EDGE ( 'NONE', *, *, #68963, .F. ) ;
#27796=CARTESIAN_POINT ( 'NONE',  ( -10.18810118749999738, -4.220049686691941915, 108.2500000020483810 ) ) ;
#27800=CARTESIAN_POINT ( 'NONE',  ( 7.778174593052023411, -7.778174593052021635, 97.56250000000000000 ) ) ;
#27814=CARTESIAN_POINT ( 'NONE',  ( -7.204075437095967871, 7.204075437095967871, 100.8437500020483668 ) ) ;
#27837=CARTESIAN_POINT ( 'NONE',  ( 4.220049686691941027, -10.18810118749999738, 82.00000000204836681 ) ) ;
#27841=AXIS2_PLACEMENT_3D ( 'NONE', #64248, #35586, #53307 ) ;
#27855=CARTESIAN_POINT ( 'NONE',  ( 7.204075437095968759, -7.204075437095966983, 75.71875000204836681 ) ) ;
#27858=CARTESIAN_POINT ( 'NONE',  ( 7.778174593052023411, -7.778174593052021635, 87.06249999999998579 ) ) ;
#27883=CARTESIAN_POINT ( 'NONE',  ( 2.020667218593132706E-15, -11.00000000000000000, 76.56250000409677625 ) ) ;
#27886=AXIS2_PLACEMENT_3D ( 'NONE', #29571, #58995, #12578 ) ;
#27899=CARTESIAN_POINT ( 'NONE',  ( -10.18810118749999916, 4.220049686691934809, 117.4375000020483810 ) ) ;
#27901=VERTEX_POINT ( 'NONE', #44506 ) ;
#27903=CARTESIAN_POINT ( 'NONE',  ( 4.220049686691941027, -10.18810118749999738, 71.12500000204836681 ) ) ;
#27908=AXIS2_PLACEMENT_3D ( 'NONE', #1177, #41518, #49689 ) ;
#27913=CARTESIAN_POINT ( 'NONE',  ( -10.18810118749999916, 4.220049686691934809, 78.43750000204838102 ) ) ;
#27919=EDGE_CURVE ( 'NONE', #8618, #60482, #71170, .T. ) ;
#27922=ORIENTED_EDGE ( 'NONE', *, *, #67087, .F. ) ;
#27939=( LENGTH_UNIT ( ) NAMED_UNIT ( * ) SI_UNIT ( .MILLI., .METRE. ) );
#27945=CARTESIAN_POINT ( 'NONE',  ( -10.18810118749999916, 0.000000000000000000, 93.15625000204836681 ) ) ;
#27948=CARTESIAN_POINT ( 'NONE',  ( -7.778174593052023411, 7.778174593052023411, 104.3124999999999858 ) ) ;
#27955=CARTESIAN_POINT ( 'NONE',  ( -10.99999999999978684, -4.556349186104264426, 86.78125000409677625 ) ) ;
#27980=CARTESIAN_POINT ( 'NONE',  ( 11.00000000000000000, 4.556349186104045934, 90.53125000409676204 ) ) ;
#28001=CARTESIAN_POINT ( 'NONE',  ( 4.220049686691941027, -10.18810118749999738, 95.50000000204838102 ) ) ;
#28009=CARTESIAN_POINT ( 'NONE',  ( 7.204075437095968759, -7.204075437095966983, 111.7187500020483810 ) ) ;
#28016=CARTESIAN_POINT ( 'NONE',  ( 7.204075437095968759, -7.204075437095966983, 112.0937500020483810 ) ) ;
#28022=CARTESIAN_POINT ( 'NONE',  ( 11.00000000000000000, 1.347111479062088405E-15, 112.7499999999999858 ) ) ;
#28023=ORIENTED_EDGE ( 'NONE', *, *, #3084, .T. ) ;
#28034=CARTESIAN_POINT ( 'NONE',  ( -10.18810118749999916, 4.220049686691934809, 109.5625000020483810 ) ) ;
#28046=CARTESIAN_POINT ( 'NONE',  ( 11.00000000000000000, 1.347111479062088405E-15, 91.74999999999998579 ) ) ;
#28054=DIRECTION ( 'NONE',  ( -0.000000000000000000, -0.000000000000000000, -1.000000000000000000 ) ) ;
#28056=FACE_OUTER_BOUND ( 'NONE', #18798, .T. ) ;
#28060=CARTESIAN_POINT ( 'NONE',  ( 7.778174593052023411, -7.778174593052021635, 111.2500000040967763 ) ) ;
#28080=CARTESIAN_POINT ( 'NONE',  ( -7.204075437095965206, -7.204075437095968759, 88.84375000204838102 ) ) ;
#28084=CARTESIAN_POINT ( 'NONE',  ( -7.204075437095965206, -7.204075437095968759, 114.7187500020483810 ) ) ;
#28091=CARTESIAN_POINT ( 'NONE',  ( -10.18810118749999916, 4.220049686691934809, 81.43750000204836681 ) ) ;
#28104=CARTESIAN_POINT ( 'NONE',  ( 4.220049686691941027, -10.18810118749999738, 80.12500000204835260 ) ) ;
#28116=CARTESIAN_POINT ( 'NONE',  ( -11.00000000000000000, 0.000000000000000000, 94.18750000409677625 ) ) ;
#28149=CARTESIAN_POINT ( 'NONE',  ( 11.00000000000000000, 1.347111479062088405E-15, 88.93750000409677625 ) ) ;
#28162=ORIENTED_EDGE ( 'NONE', *, *, #21630, .F. ) ;
#28170=CARTESIAN_POINT ( 'NONE',  ( 10.18810118749999916, 4.220049686691935698, 104.5000000020483668 ) ) ;
#28174=CARTESIAN_POINT ( 'NONE',  ( -10.99999999999999822, -4.556349186104053040, 97.09375000000001421 ) ) ;
#28187=CARTESIAN_POINT ( 'NONE',  ( 10.18810118749999916, 4.220049686691935698, 100.3750000020483952 ) ) ;
#28199=CARTESIAN_POINT ( 'NONE',  ( 7.204075437095966983, 7.204075437095967871, 94.09375000204838102 ) ) ;
#28208=VECTOR ( 'NONE', #11700, 1000.000000000000000 ) ;
#28209=CARTESIAN_POINT ( 'NONE',  ( 7.204075437095966983, 7.204075437095967871, 77.96875000204836681 ) ) ;
#28210=ORIENTED_EDGE ( 'NONE', *, *, #13597, .T. ) ;
#28230=CARTESIAN_POINT ( 'NONE',  ( -10.18810118749999916, 4.220049686691934809, 76.56250000204836681 ) ) ;
#28233=CARTESIAN_POINT ( 'NONE',  ( -10.99999999999999822, -4.556349186104052151, 83.59375000000000000 ) ) ;
#28247=CARTESIAN_POINT ( 'NONE',  ( 11.00000000000010836, -4.556349186103939353, 99.34375000409680467 ) ) ;
#28261=CARTESIAN_POINT ( 'NONE',  ( 4.556349186104045934, 11.00000000000000000, 74.21875000409677625 ) ) ;
#28276=CARTESIAN_POINT ( 'NONE',  ( 10.18810118749999916, 4.220049686691935698, 116.8750000020483952 ) ) ;
#28280=CARTESIAN_POINT ( 'NONE',  ( -4.220049686691937474, -10.18810118749999738, 72.43750000204838102 ) ) ;
#28308=CARTESIAN_POINT ( 'NONE',  ( 0.000000000000000000, 0.000000000000000000, 118.0000000000000000 ) ) ;
#28315=CARTESIAN_POINT ( 'NONE',  ( 7.204075437095966983, 7.204075437095967871, 91.09375000204838102 ) ) ;
#28318=CARTESIAN_POINT ( 'NONE',  ( 11.00000000000000000, 4.556349186104045934, 106.8437500000000000 ) ) ;
#28321=CARTESIAN_POINT ( 'NONE',  ( -4.556349186104045934, 11.00000000000000000, 113.4062500040967620 ) ) ;
#28347=CARTESIAN_POINT ( 'NONE',  ( 11.00000000000000355, -4.556349186104045046, 93.34375000409677625 ) ) ;
#28369=AXIS2_PLACEMENT_3D ( 'NONE', #58372, #13048, #17613 ) ;
#28370=CARTESIAN_POINT ( 'NONE',  ( 4.220049686691941027, -10.18810118749999738, 98.50000000204838102 ) ) ;
#28378=CARTESIAN_POINT ( 'NONE',  ( -7.204075437095967871, 7.204075437095967871, 109.4687500020483810 ) ) ;
#28380=ORIENTED_EDGE ( 'NONE', *, *, #16396, .T. ) ;
#28387=CARTESIAN_POINT ( 'NONE',  ( 4.220049686691941027, -10.18810118749999738, 104.5000000020483668 ) ) ;
#28393=CARTESIAN_POINT ( 'NONE',  ( -11.00000000000000000, 0.000000000000000000, 97.18750000409677625 ) ) ;
#28405=CARTESIAN_POINT ( 'NONE',  ( 4.220049686691934809, 10.18810118749999916, 110.6875000020483810 ) ) ;
#28406=CARTESIAN_POINT ( 'NONE',  ( -11.00000000000000000, 0.000000000000000000, 103.0000000000000000 ) ) ;
#28428=LINE ( 'NONE', #17851, #44714 ) ;
#28432=CARTESIAN_POINT ( 'NONE',  ( -7.778174593052020747, -7.778174593052023411, 109.3750000040967763 ) ) ;
#28455=CARTESIAN_POINT ( 'NONE',  ( -6.238412754330611322E-16, 10.18810118749999916, 88.28125000204836681 ) ) ;
#28460=CARTESIAN_POINT ( 'NONE',  ( 10.18810118749999916, 4.220049686691935698, 116.8750000020483668 ) ) ;
#28467=CARTESIAN_POINT ( 'NONE',  ( 10.18810118749999916, 1.247682550866122264E-15, 76.28125000204836681 ) ) ;
#28481=CARTESIAN_POINT ( 'NONE',  ( 4.220049686691941027, -10.18810118749999738, 75.62500000204838102 ) ) ;
#28484=CARTESIAN_POINT ( 'NONE',  ( 7.778174593052021635, 7.778174593052023411, 109.9375000000000000 ) ) ;
#28491=CARTESIAN_POINT ( 'NONE',  ( 4.556349186104052151, -10.99999999999999822, 75.15625000409677625 ) ) ;
#28493=ORIENTED_EDGE ( 'NONE', *, *, #60214, .T. ) ;
#28502=CARTESIAN_POINT ( 'NONE',  ( -11.00000000000000000, 0.000000000000000000, 118.0000000000000000 ) ) ;
#28516=CARTESIAN_POINT ( 'NONE',  ( 4.556349186104045934, 11.00000000000000000, 107.0312500000000000 ) ) ;
#28520=EDGE_LOOP ( 'NONE', ( #49894, #11144, #65412, #30820 ) ) ;
#28541=CARTESIAN_POINT ( 'NONE',  ( -0.9087844426713385104, 10.88091015416974550, 117.5913480126766473 ) ) ;
#28542=CARTESIAN_POINT ( 'NONE',  ( -10.18810118749999916, 4.220049686691934809, 106.5625000020483668 ) ) ;
#28553=AXIS2_PLACEMENT_3D ( 'NONE', #46829, #1575, #69854 ) ;
#28560=CARTESIAN_POINT ( 'NONE',  ( -7.204075437095967871, 7.204075437095967871, 102.3437500020483668 ) ) ;
#28568=ORIENTED_EDGE ( 'NONE', *, *, #29708, .F. ) ;
#28572=( BOUNDED_CURVE ( )  B_SPLINE_CURVE ( 2, ( #51499, #34172, #35287, #28491, #68478, #57932, #22822, #45838, #11887 ),
 .UNSPECIFIED., .F., .F. ) 
 B_SPLINE_CURVE_WITH_KNOTS ( ( 3, 2, 2, 2, 3 ),
 ( 0.8088235294117646079, 0.8124999999999998890, 0.8161764705882351700, 0.8198529411764704511, 0.8235294117647057321 ),
 .UNSPECIFIED. ) 
 CURVE ( )  GEOMETRIC_REPRESENTATION_ITEM ( )  RATIONAL_B_SPLINE_CURVE ( ( 1.000000000000002220, 0.9238795325112844070, 1.000000000000000000, 0.9238795325112867385, 1.000000000000000000, 0.9238795325112867385, 1.000000000000000000, 0.9238795325112890700, 0.9999999999999976685 ) ) 
 REPRESENTATION_ITEM ( '' )  );
#28573=CARTESIAN_POINT ( 'NONE',  ( -10.18810118749999916, 0.000000000000000000, 96.15625000204838102 ) ) ;
#28583=CARTESIAN_POINT ( 'NONE',  ( 10.18810118750000093, -4.220049686691933921, 80.68750000204836681 ) ) ;
#28601=CARTESIAN_POINT ( 'NONE',  ( 10.18810118749999916, 4.220049686691935698, 76.00000000204835260 ) ) ;
#28604=CARTESIAN_POINT ( 'NONE',  ( -7.778174593052020747, -7.778174593052023411, 82.18750000000000000 ) ) ;
#28607=CARTESIAN_POINT ( 'NONE',  ( 7.778174593052023411, -7.778174593052021635, 114.0625000000000000 ) ) ;
#28631=CARTESIAN_POINT ( 'NONE',  ( 11.00000000000000355, -4.556349186104045046, 75.34375000409676204 ) ) ;
#28647=CARTESIAN_POINT ( 'NONE',  ( 10.18810118749999916, 1.247682550866122264E-15, 71.40625000204836681 ) ) ;
#28683=CARTESIAN_POINT ( 'NONE',  ( -10.18810118749999916, 0.000000000000000000, 90.15625000204838102 ) ) ;
#28684=CARTESIAN_POINT ( 'NONE',  ( 0.000000000000000000, 0.000000000000000000, 118.0000000000000000 ) ) ;
#28685=CARTESIAN_POINT ( 'NONE',  ( -4.556349186104045934, 11.00000000000000000, 99.71875000000000000 ) ) ;
#28687=CARTESIAN_POINT ( 'NONE',  ( 7.778174593052023411, -7.778174593052021635, 87.06249999999998579 ) ) ;
#28715=CARTESIAN_POINT ( 'NONE',  ( 11.00000000000000000, 4.556349186104045934, 93.53125000409676204 ) ) ;
#28737=CARTESIAN_POINT ( 'NONE',  ( -4.220049686691937474, -10.18810118749999738, 98.31250000204836681 ) ) ;
#28741=FACE_OUTER_BOUND ( 'NONE', #63696, .T. ) ;
#28746=CARTESIAN_POINT ( 'NONE',  ( 1.871523826299183495E-15, -10.18810118749999916, 110.0312500020483668 ) ) ;
#28758=CARTESIAN_POINT ( 'NONE',  ( 1.871523826299183495E-15, -10.18810118749999916, 105.9062500020483810 ) ) ;
#28759=CARTESIAN_POINT ( 'NONE',  ( -7.778174593052023411, 7.778174593052023411, 75.81249999999997158 ) ) ;
#28772=CARTESIAN_POINT ( 'NONE',  ( -4.220049686691937474, -10.18810118749999738, 108.4375000020483952 ) ) ;
#28791=CARTESIAN_POINT ( 'NONE',  ( -10.18810118749999738, -4.220049686691941915, 69.62500000204838102 ) ) ;
#28801=CARTESIAN_POINT ( 'NONE',  ( -10.99999999999999822, -4.556349186104052151, 110.7812500040967905 ) ) ;
#28814=ORIENTED_EDGE ( 'NONE', *, *, #123, .F. ) ;
#28819=CARTESIAN_POINT ( 'NONE',  ( 10.99999999999994849, 4.556349186104097448, 103.8437500000000000 ) ) ;
#28820=CARTESIAN_POINT ( 'NONE',  ( -11.00000000000000000, 0.000000000000000000, 117.4999999999999716 ) ) ;
#28823=CARTESIAN_POINT ( 'NONE',  ( -10.18810118749999738, -4.220049686691941915, 82.75000000204838102 ) ) ;
#28827=CARTESIAN_POINT ( 'NONE',  ( 10.18810118749999916, 4.220049686691935698, 115.3750000020483810 ) ) ;
#28835=CARTESIAN_POINT ( 'NONE',  ( -7.204075437095967871, 7.204075437095967871, 79.84375000204838102 ) ) ;
#28848=CARTESIAN_POINT ( 'NONE',  ( 7.204075437095966983, 7.204075437095967871, 68.59375000204836681 ) ) ;
#28883=CARTESIAN_POINT ( 'NONE',  ( 16.00000000000000711, -16.00000000000000000, 20.00000000000000000 ) ) ;
#28894=DIRECTION ( 'NONE',  ( -0.000000000000000000, -0.000000000000000000, -1.000000000000000000 ) ) ;
#28910=( BOUNDED_CURVE ( )  B_SPLINE_CURVE ( 2, ( #24033, #30075, #17262, #64040, #53464, #689, #58396, #35743, #11984 ),
 .UNSPECIFIED., .F., .F. ) 
 B_SPLINE_CURVE_WITH_KNOTS ( ( 3, 2, 2, 2, 3 ),
 ( 0.1029411764705883137, 0.1066176470588236086, 0.1102941176470589035, 0.1139705882352941985, 0.1176470588235294934 ),
 .UNSPECIFIED. ) 
 CURVE ( )  GEOMETRIC_REPRESENTATION_ITEM ( )  RATIONAL_B_SPLINE_CURVE ( ( 0.9999999999999982236, 0.9238795325112885148, 1.000000000000000000, 0.9238795325112867385, 1.000000000000000000, 0.9238795325112867385, 1.000000000000000000, 0.9238795325112849621, 1.000000000000001776 ) ) 
 REPRESENTATION_ITEM ( '' )  );
#28916=ORIENTED_EDGE ( 'NONE', *, *, #32420, .F. ) ;
#28919=CARTESIAN_POINT ( 'NONE',  ( -10.18810118749999916, 4.220049686691934809, 102.0625000020483810 ) ) ;
#28935=CARTESIAN_POINT ( 'NONE',  ( -10.18810118749999916, 4.220049686691934809, 94.93750000204836681 ) ) ;
#28944=EDGE_LOOP ( 'NONE', ( #36940, #36751, #67688, #38054 ) ) ;
#28945=CARTESIAN_POINT ( 'NONE',  ( -11.00000000000031619, 4.556349186103730631, 89.59375000409677625 ) ) ;
#28947=CARTESIAN_POINT ( 'NONE',  ( -4.220049686691937474, -10.18810118749999738, 88.93750000204839523 ) ) ;
#28956=CARTESIAN_POINT ( 'NONE',  ( -4.220049686691935698, 10.18810118749999916, 76.75000000204838102 ) ) ;
#28967=CARTESIAN_POINT ( 'NONE',  ( 2.020667218593132706E-15, -11.00000000000000000, 88.56250000409676204 ) ) ;
#28977=CARTESIAN_POINT ( 'NONE',  ( 2.020667218593132706E-15, -11.00000000000000000, 85.37499999999997158 ) ) ;
#28981=VERTEX_POINT ( 'NONE', #66586 ) ;
#28984=EDGE_CURVE ( 'NONE', #18528, #26793, #4659, .T. ) ;
#29002=CARTESIAN_POINT ( 'NONE',  ( -7.778174593052020747, -7.778174593052023411, 74.68749999999998579 ) ) ;
#29003=CARTESIAN_POINT ( 'NONE',  ( 10.99999999999999467, -4.556349186104054816, 117.1562499999999858 ) ) ;
#29005=CARTESIAN_POINT ( 'NONE',  ( -11.00000000000000000, 0.000000000000000000, 70.18750000409676204 ) ) ;
#29018=CARTESIAN_POINT ( 'NONE',  ( 7.204075437095966983, 7.204075437095967871, 110.9687500020483810 ) ) ;
#29022=CARTESIAN_POINT ( 'NONE',  ( -4.220049686691937474, -10.18810118749999738, 70.93750000204838102 ) ) ;
#29033=( BOUNDED_CURVE ( )  B_SPLINE_CURVE ( 2, ( #51292, #38866, #68646, #34343, #27531, #73932, #57342, #62236, #50543 ),
 .UNSPECIFIED., .F., .F. ) 
 B_SPLINE_CURVE_WITH_KNOTS ( ( 3, 2, 2, 2, 3 ),
 ( 0.7205882352941175295, 0.7242647058823528106, 0.7279411764705880916, 0.7316176470588233727, 0.7352941176470587648 ),
 .UNSPECIFIED. ) 
 CURVE ( )  GEOMETRIC_REPRESENTATION_ITEM ( )  RATIONAL_B_SPLINE_CURVE ( ( 1.000000000000002220, 0.9238795325112844070, 1.000000000000000000, 0.9238795325112867385, 1.000000000000000000, 0.9238795325112867385, 1.000000000000000000, 0.9238795325112890700, 0.9999999999999976685 ) ) 
 REPRESENTATION_ITEM ( '' )  );
#29061=CARTESIAN_POINT ( 'NONE',  ( 4.220049686691941027, -10.18810118749999738, 84.62500000204836681 ) ) ;
#29062=CARTESIAN_POINT ( 'NONE',  ( 11.00000000000000000, 1.347111479062088405E-15, 106.9375000040967763 ) ) ;
#29064=CARTESIAN_POINT ( 'NONE',  ( 4.556349186104045934, 11.00000000000000000, 101.0312499999999858 ) ) ;
#29065=CARTESIAN_POINT ( 'NONE',  ( 0.000000000000000000, 0.000000000000000000, 118.0000000000000000 ) ) ;
#29092=AXIS2_PLACEMENT_3D ( 'NONE', #46149, #74447, #6172 ) ;
#29096=CARTESIAN_POINT ( 'NONE',  ( -7.778174593052023411, 7.778174593052023411, 95.50000000409677625 ) ) ;
#29099=CARTESIAN_POINT ( 'NONE',  ( 10.99999999999993605, -4.556349186104108995, 111.3437500040967620 ) ) ;
#29120=CARTESIAN_POINT ( 'NONE',  ( 7.204075437095966983, 7.204075437095967871, 95.96875000204838102 ) ) ;
#29128=CARTESIAN_POINT ( 'NONE',  ( -10.18810118749999738, -4.220049686691941915, 106.7500000020483668 ) ) ;
#29137=CARTESIAN_POINT ( 'NONE',  ( -10.18810118749999738, -4.220049686691941915, 102.6250000020483810 ) ) ;
#29139=CARTESIAN_POINT ( 'NONE',  ( 11.00000000000000000, 1.347111479062088405E-15, 75.24999999999998579 ) ) ;
#29153=CARTESIAN_POINT ( 'NONE',  ( 1.871523826299183495E-15, -10.18810118749999916, 111.5312500020483668 ) ) ;
#29160=ADVANCED_FACE ( 'NONE', ( #17882 ), #12361, .T. ) ;
#29166=EDGE_CURVE ( 'NONE', #43538, #56060, #2218, .T. ) ;
#29174=CARTESIAN_POINT ( 'NONE',  ( 10.18810118749999916, 4.220049686691935698, 68.87500000204838102 ) ) ;
#29179=FACE_OUTER_BOUND ( 'NONE', #66433, .T. ) ;
#29185=CARTESIAN_POINT ( 'NONE',  ( 2.020667218593132706E-15, -11.00000000000000000, 108.0625000040967905 ) ) ;
#29190=CARTESIAN_POINT ( 'NONE',  ( 0.000000000000000000, 0.000000000000000000, 118.0000000000000000 ) ) ;
#29198=CARTESIAN_POINT ( 'NONE',  ( 11.00000000000000000, 1.347111479062088405E-15, 115.7499999999999858 ) ) ;
#29203=CARTESIAN_POINT ( 'NONE',  ( -11.00000000000010658, 4.556349186103942017, 104.4062500000000142 ) ) ;
#29207=CARTESIAN_POINT ( 'NONE',  ( 7.204075437095966983, 7.204075437095967871, 83.59375000204836681 ) ) ;
#29211=CARTESIAN_POINT ( 'NONE',  ( -10.18810118749999738, -4.220049686691941915, 114.6250000020483810 ) ) ;
#29218=CARTESIAN_POINT ( 'NONE',  ( 1.871523826299183495E-15, -10.18810118749999916, 75.90625000204836681 ) ) ;
#29231=CARTESIAN_POINT ( 'NONE',  ( -4.220049686691935698, 10.18810118749999916, 70.37500000204838102 ) ) ;
#29243=CARTESIAN_POINT ( 'NONE',  ( 11.00000000000000000, 1.347111479062088405E-15, 78.43750000409677625 ) ) ;
#29270=CARTESIAN_POINT ( 'NONE',  ( 2.947433605447500327, 11.00000000000000000, 68.06435453820057546 ) ) ;
#29296=EDGE_LOOP ( 'NONE', ( #60919, #67935, #69054, #36795 ) ) ;
#29298=CARTESIAN_POINT ( 'NONE',  ( -7.204075437095967871, 7.204075437095967871, 98.96875000204838102 ) ) ;
#29315=CARTESIAN_POINT ( 'NONE',  ( 10.18810118749999916, 1.247682550866122264E-15, 97.28125000204838102 ) ) ;
#29321=CARTESIAN_POINT ( 'NONE',  ( 1.871523826299183495E-15, -10.18810118749999916, 77.40625000204836681 ) ) ;
#29328=CARTESIAN_POINT ( 'NONE',  ( 1.871523826299183495E-15, -10.18810118749999916, 92.03125000204836681 ) ) ;
#29338=CARTESIAN_POINT ( 'NONE',  ( 7.204075437095968759, -7.204075437095966983, 74.59375000204838102 ) ) ;
#29358=ORIENTED_EDGE ( 'NONE', *, *, #13130, .T. ) ;
#29359=CARTESIAN_POINT ( 'NONE',  ( -10.18810118749999916, 0.000000000000000000, 70.65625000204836681 ) ) ;
#29362=CARTESIAN_POINT ( 'NONE',  ( -11.00000000000000000, 4.556349186104045934, 84.90624999999998579 ) ) ;
#29365=CYLINDRICAL_SURFACE ( 'NONE', #24189, 11.00000000000000000 ) ;
#29366=ORIENTED_EDGE ( 'NONE', *, *, #25573, .F. ) ;
#29368=FACE_OUTER_BOUND ( 'NONE', #20757, .T. ) ;
#29389=CARTESIAN_POINT ( 'NONE',  ( -7.778174593052020747, -7.778174593052023411, 67.37500000409676204 ) ) ;
#29400=CARTESIAN_POINT ( 'NONE',  ( -10.18810118749999916, 0.000000000000000000, 116.0312500020483810 ) ) ;
#29404=CARTESIAN_POINT ( 'NONE',  ( -15.99999999999999645, 0.000000000000000000, 38.34805510287551300 ) ) ;
#29416=ORIENTED_EDGE ( 'NONE', *, *, #54476, .T. ) ;
#29435=CARTESIAN_POINT ( 'NONE',  ( -4.220049686691937474, -10.18810118749999738, 84.43750000204838102 ) ) ;
#29436=CARTESIAN_POINT ( 'NONE',  ( 11.00000000000000000, 1.347111479062088405E-15, 91.74999999999998579 ) ) ;
#29438=CARTESIAN_POINT ( 'NONE',  ( -4.556349186104045934, 11.00000000000000000, 102.7187499999999858 ) ) ;
#29464=DIRECTION ( 'NONE',  ( -0.000000000000000000, -0.000000000000000000, -1.000000000000000000 ) ) ;
#29466=ORIENTED_EDGE ( 'NONE', *, *, #38502, .T. ) ;
#29469=CARTESIAN_POINT ( 'NONE',  ( -6.735557395310442023E-16, 11.00000000000000000, 87.81250000409676204 ) ) ;
#29493=CARTESIAN_POINT ( 'NONE',  ( 10.18810118749999916, 4.220049686691935698, 94.37500000204839523 ) ) ;
#29501=CARTESIAN_POINT ( 'NONE',  ( 10.18810118749999916, 4.220049686691935698, 107.5000000020483668 ) ) ;
#29508=AXIS2_PLACEMENT_3D ( 'NONE', #61926, #39296, #50601 ) ;
#29510=CARTESIAN_POINT ( 'NONE',  ( 7.204075437095966983, 7.204075437095967871, 101.9687500020483668 ) ) ;
#29524=CARTESIAN_POINT ( 'NONE',  ( -6.238412754330611322E-16, 10.18810118749999916, 103.2812500020483810 ) ) ;
#29541=CARTESIAN_POINT ( 'NONE',  ( -4.556349186104047710, -10.99999999999999822, 116.7812499999999858 ) ) ;
#29553=CARTESIAN_POINT ( 'NONE',  ( -7.778174593052020747, -7.778174593052023411, 101.8750000040967763 ) ) ;
#29571=CARTESIAN_POINT ( 'NONE',  ( 0.000000000000000000, 0.000000000000000000, 118.0000000000000000 ) ) ;
#29574=CARTESIAN_POINT ( 'NONE',  ( -10.18810118749999916, 0.000000000000000000, 85.65625000204838102 ) ) ;
#29578=CARTESIAN_POINT ( 'NONE',  ( -10.18810118749999916, 0.000000000000000000, 110.0312500020483668 ) ) ;
#29585=CARTESIAN_POINT ( 'NONE',  ( -6.238412754330611322E-16, 10.18810118749999916, 79.65625000204836681 ) ) ;
#29598=CARTESIAN_POINT ( 'NONE',  ( 4.220049686691934809, 10.18810118749999916, 70.18750000204838102 ) ) ;
#29600=DIRECTION ( 'NONE',  ( -1.000000000000000000, -3.154042683594195121E-16, 0.000000000000000000 ) ) ;
#29602=VERTEX_POINT ( 'NONE', #59421 ) ;
#29610=CARTESIAN_POINT ( 'NONE',  ( 7.778174593052021635, 7.778174593052023411, 93.62500000409677625 ) ) ;
#29613=ORIENTED_EDGE ( 'NONE', *, *, #21242, .T. ) ;
#29632=CARTESIAN_POINT ( 'NONE',  ( 11.00000000000000000, 1.347111479062088405E-15, 79.74999999999998579 ) ) ;
#29637=CARTESIAN_POINT ( 'NONE',  ( 7.778174593052021635, 7.778174593052023411, 106.9374999999999858 ) ) ;
#29661=CARTESIAN_POINT ( 'NONE',  ( 1.871523826299183495E-15, -10.18810118749999916, 99.53125000204838102 ) ) ;
#29665=DIRECTION ( 'NONE',  ( -0.000000000000000000, -0.000000000000000000, -1.000000000000000000 ) ) ;
#29678=CARTESIAN_POINT ( 'NONE',  ( -7.204075437095967871, 7.204075437095967871, 96.34375000204836681 ) ) ;
#29683=CARTESIAN_POINT ( 'NONE',  ( -4.220049686691937474, -10.18810118749999738, 78.81250000204838102 ) ) ;
#29693=CARTESIAN_POINT ( 'NONE',  ( 10.18810118750000093, -4.220049686691933921, 92.31250000204838102 ) ) ;
#29703=CARTESIAN_POINT ( 'NONE',  ( -7.204075437095967871, 7.204075437095967871, 76.84375000204838102 ) ) ;
#29708=EDGE_CURVE ( 'NONE', #25175, #36433, #27341, .T. ) ;
#29720=ORIENTED_EDGE ( 'NONE', *, *, #70130, .F. ) ;
#29721=CARTESIAN_POINT ( 'NONE',  ( 4.220049686691941027, -10.18810118749999738, 68.12500000204838102 ) ) ;
#29724=CARTESIAN_POINT ( 'NONE',  ( 11.00000000000000000, 4.556349186104045934, 82.84375000000000000 ) ) ;
#29742=CYLINDRICAL_SURFACE ( 'NONE', #6325, 11.00000000000000000 ) ;
#29748=CARTESIAN_POINT ( 'NONE',  ( -7.778174593052020747, -7.778174593052023411, 70.37500000409677625 ) ) ;
#29760=CARTESIAN_POINT ( 'NONE',  ( -10.18810118749999738, -4.220049686691941915, 116.1250000020483810 ) ) ;
#29762=ORIENTED_EDGE ( 'NONE', *, *, #11313, .T. ) ;
#29764=CARTESIAN_POINT ( 'NONE',  ( 7.204075437095968759, -7.204075437095966983, 68.21875000204836681 ) ) ;
#29803=CARTESIAN_POINT ( 'NONE',  ( 10.18810118749999916, 1.247682550866122264E-15, 89.40625000204838102 ) ) ;
#29806=CARTESIAN_POINT ( 'NONE',  ( 7.778174593052021635, 7.778174593052023411, 99.43749999999998579 ) ) ;
#29825=CARTESIAN_POINT ( 'NONE',  ( 11.00000000000000000, 1.347111479062088405E-15, 85.75000000000000000 ) ) ;
#29837=CARTESIAN_POINT ( 'NONE',  ( -4.556349186104047710, -10.99999999999999822, 83.96875000409676204 ) ) ;
#29854=EDGE_LOOP ( 'NONE', ( #30262, #26667, #26431, #10445 ) ) ;
#29855=CARTESIAN_POINT ( 'NONE',  ( -7.778174593052020747, -7.778174593052023411, 100.1874999999999858 ) ) ;
#29862=CARTESIAN_POINT ( 'NONE',  ( -10.18810118749999738, -4.220049686691941915, 90.62500000204836681 ) ) ;
#29868=CARTESIAN_POINT ( 'NONE',  ( -7.204075437095965206, -7.204075437095968759, 106.8437500020483810 ) ) ;
#29877=CARTESIAN_POINT ( 'NONE',  ( 7.204075437095968759, -7.204075437095966983, 101.5937500020483668 ) ) ;
#29880=CARTESIAN_POINT ( 'NONE',  ( 11.00000000000000000, 1.347111479062088405E-15, 118.0000000000000000 ) ) ;
#29882=CARTESIAN_POINT ( 'NONE',  ( -11.00000000000000000, 0.000000000000000000, 77.68750000409677625 ) ) ;
#29893=CARTESIAN_POINT ( 'NONE',  ( 4.220049686691934809, 10.18810118749999916, 103.1875000020483810 ) ) ;
#29910=CARTESIAN_POINT ( 'NONE',  ( -11.00000000000000000, 0.000000000000000000, 116.4999999999999858 ) ) ;
#29921=CARTESIAN_POINT ( 'NONE',  ( 7.778174593052021635, 7.778174593052023411, 107.1250000040967763 ) ) ;
#29939=DIRECTION ( 'NONE',  ( -1.000000000000000000, 0.000000000000000000, 0.000000000000000000 ) ) ;
#29942=CARTESIAN_POINT ( 'NONE',  ( -7.204075437095967871, 7.204075437095967871, 80.96875000204836681 ) ) ;
#29947=CARTESIAN_POINT ( 'NONE',  ( 10.18810118750000093, -4.220049686691933921, 110.6875000020483952 ) ) ;
#29950=LINE ( 'NONE', #69947, #26238 ) ;
#29955=CARTESIAN_POINT ( 'NONE',  ( 4.220049686691934809, 10.18810118749999916, 79.56250000204836681 ) ) ;
#29966=CARTESIAN_POINT ( 'NONE',  ( -10.18810118749999738, -4.220049686691941915, 69.25000000204836681 ) ) ;
#29969=VERTEX_POINT ( 'NONE', #20717 ) ;
#30007=CARTESIAN_POINT ( 'NONE',  ( -4.556349186104045934, 11.00000000000000000, 75.90625000409677625 ) ) ;
#30030=ORIENTED_EDGE ( 'NONE', *, *, #41924, .T. ) ;
#30031=CARTESIAN_POINT ( 'NONE',  ( -4.951871933616136978, 9.664417241377410761, 117.6512260359776150 ) ) ;
#30032=CARTESIAN_POINT ( 'NONE',  ( 10.18810118749999916, 4.220049686691935698, 98.50000000204838102 ) ) ;
#30045=CARTESIAN_POINT ( 'NONE',  ( -7.778174593052020747, -7.778174593052023411, 73.18749999999998579 ) ) ;
#30046=CARTESIAN_POINT ( 'NONE',  ( -11.00000000000021139, 4.556349186103834548, 83.59375000409677625 ) ) ;
#30050=CARTESIAN_POINT ( 'NONE',  ( 7.204075437095968759, -7.204075437095966983, 95.59375000204838102 ) ) ;
#30056=CARTESIAN_POINT ( 'NONE',  ( -10.18810118749999916, 0.000000000000000000, 80.03125000204836681 ) ) ;
#30064=CARTESIAN_POINT ( 'NONE',  ( 10.18810118749999916, 4.220049686691935698, 88.00000000204836681 ) ) ;
#30072=CARTESIAN_POINT ( 'NONE',  ( -4.220049686691937474, -10.18810118749999738, 77.31250000204836681 ) ) ;
#30075=CARTESIAN_POINT ( 'NONE',  ( 10.99999999999992006, -4.556349186104122317, 112.6562499999999716 ) ) ;
#30091=CARTESIAN_POINT ( 'NONE',  ( -4.556349186104047710, -10.99999999999999822, 79.28124999999998579 ) ) ;
#30103=ADVANCED_FACE ( 'NONE', ( #42064 ), #42435, .T. ) ;
#30118=CARTESIAN_POINT ( 'NONE',  ( -7.778174593052023411, 7.778174593052023411, 67.00000000409676204 ) ) ;
#30120=CARTESIAN_POINT ( 'NONE',  ( -7.778174593052023411, 7.778174593052023411, 71.50000000409677625 ) ) ;
#30133=CARTESIAN_POINT ( 'NONE',  ( -7.204075437095965206, -7.204075437095968759, 114.7187500020483810 ) ) ;
#30135=VERTEX_POINT ( 'NONE', #13385 ) ;
#30146=AXIS2_PLACEMENT_3D ( 'NONE', #8744, #37796, #60792 ) ;
#30164=ORIENTED_EDGE ( 'NONE', *, *, #59906, .F. ) ;
#30171=CARTESIAN_POINT ( 'NONE',  ( 1.871523826299183495E-15, -10.18810118749999916, 89.03125000204836681 ) ) ;
#30173=CARTESIAN_POINT ( 'NONE',  ( -4.556349186104047710, -10.99999999999999822, 101.7812499999999858 ) ) ;
#30174=LINE ( 'NONE', #70900, #19350 ) ;
#30201=CARTESIAN_POINT ( 'NONE',  ( -4.556349186104047710, -10.99999999999999822, 85.46875000409677625 ) ) ;
#30205=CARTESIAN_POINT ( 'NONE',  ( -11.00000000000005151, 4.556349186103993532, 101.4062500000000000 ) ) ;
#30210=EDGE_CURVE ( 'NONE', #42385, #69514, #65886, .T. ) ;
#30227=CARTESIAN_POINT ( 'NONE',  ( 4.220049686691934809, 10.18810118749999916, 93.06250000204839523 ) ) ;
#30233=CARTESIAN_POINT ( 'NONE',  ( -4.220049686691937474, -10.18810118749999738, 102.4375000020483810 ) ) ;
#30242=CARTESIAN_POINT ( 'NONE',  ( 10.18810118749999916, 4.220049686691935698, 95.87500000204838102 ) ) ;
#30262=ORIENTED_EDGE ( 'NONE', *, *, #6641, .T. ) ;
#30263=CARTESIAN_POINT ( 'NONE',  ( 10.18810118750000093, -4.220049686691933033, 104.3125000020483810 ) ) ;
#30272=ORIENTED_EDGE ( 'NONE', *, *, #18919, .F. ) ;
#30279=CARTESIAN_POINT ( 'NONE',  ( -4.220049686691937474, -10.18810118749999738, 68.31250000204838102 ) ) ;
#30291=CARTESIAN_POINT ( 'NONE',  ( 7.778174593052023411, -7.778174593052021635, 105.2500000040967763 ) ) ;
#30294=CARTESIAN_POINT ( 'NONE',  ( -7.778174593052023411, 7.778174593052023411, 95.50000000409677625 ) ) ;
#30313=CARTESIAN_POINT ( 'NONE',  ( 7.204075437095968759, -7.204075437095966983, 110.5937500020483810 ) ) ;
#30321=CARTESIAN_POINT ( 'NONE',  ( -7.204075437095967871, 7.204075437095967871, 69.34375000204836681 ) ) ;
#30323=ORIENTED_EDGE ( 'NONE', *, *, #26499, .F. ) ;
#30334=CARTESIAN_POINT ( 'NONE',  ( -10.18810118749999916, 4.220049686691934809, 72.06250000204836681 ) ) ;
#30340=EDGE_CURVE ( 'NONE', #46864, #12752, #72221, .T. ) ;
#30351=CARTESIAN_POINT ( 'NONE',  ( -10.18810118749999916, 0.000000000000000000, 117.5312500020483810 ) ) ;
#30372=CARTESIAN_POINT ( 'NONE',  ( 7.778174593052023411, -7.778174593052021635, 69.25000000409677625 ) ) ;
#30401=CARTESIAN_POINT ( 'NONE',  ( -7.204075437095965206, -7.204075437095968759, 100.8437500020483668 ) ) ;
#30416=CARTESIAN_POINT ( 'NONE',  ( -10.18810118749999916, 0.000000000000000000, 90.53125000204836681 ) ) ;
#30418=ORIENTED_EDGE ( 'NONE', *, *, #69616, .T. ) ;
#30423=CARTESIAN_POINT ( 'NONE',  ( -10.18810118749999916, 0.000000000000000000, 75.53125000204836681 ) ) ;
#30431=CARTESIAN_POINT ( 'NONE',  ( 7.204075437095968759, -7.204075437095966983, 90.71875000204838102 ) ) ;
#30442=CARTESIAN_POINT ( 'NONE',  ( 4.220049686691934809, 10.18810118749999916, 73.56250000204835260 ) ) ;
#30444=( BOUNDED_CURVE ( )  B_SPLINE_CURVE ( 2, ( #42440, #59807, #36429, #35693, #58708, #7757, #53042, #65459, #8121 ),
 .UNSPECIFIED., .F., .F. ) 
 B_SPLINE_CURVE_WITH_KNOTS ( ( 3, 2, 2, 2, 3 ),
 ( 0.04411764705882356002, 0.04779411764705884802, 0.05147058823529414989, 0.05514705882352945177, 0.05882352941176474670 ),
 .UNSPECIFIED. ) 
 CURVE ( )  GEOMETRIC_REPRESENTATION_ITEM ( )  RATIONAL_B_SPLINE_CURVE ( ( 0.9999999999999994449, 0.9238795325112872936, 1.000000000000000000, 0.9238795325112867385, 1.000000000000000000, 0.9238795325112867385, 1.000000000000000000, 0.9238795325112858503, 1.000000000000000888 ) ) 
 REPRESENTATION_ITEM ( '' )  );
#30446=( BOUNDED_CURVE ( )  B_SPLINE_CURVE ( 2, ( #41863, #2245, #8270, #25238, #18856, #64875, #41499, #53195, #13540 ),
 .UNSPECIFIED., .F., .F. ) 
 B_SPLINE_CURVE_WITH_KNOTS ( ( 3, 2, 2, 2, 3 ),
 ( 0.2058823529411765996, 0.2095588235294118529, 0.2132352941176470507, 0.2169117647058823040, 0.2205882352941175018 ),
 .UNSPECIFIED. ) 
 CURVE ( )  GEOMETRIC_REPRESENTATION_ITEM ( )  RATIONAL_B_SPLINE_CURVE ( ( 0.9999999999999971134, 0.9238795325112896251, 1.000000000000000000, 0.9238795325112867385, 1.000000000000000000, 0.9238795325112867385, 1.000000000000000000, 0.9238795325112896251, 0.9999999999999971134 ) ) 
 REPRESENTATION_ITEM ( '' )  );
#30460=CARTESIAN_POINT ( 'NONE',  ( 10.18810118750000093, -4.220049686691933033, 69.81250000204835260 ) ) ;
#30463=CARTESIAN_POINT ( 'NONE',  ( -7.778174593052023411, 7.778174593052023411, 78.81249999999998579 ) ) ;
#30466=CARTESIAN_POINT ( 'NONE',  ( -11.00000000000004796, -4.556349186104000637, 113.5937499999999858 ) ) ;
#30488=CARTESIAN_POINT ( 'NONE',  ( 4.220049686691934809, 10.18810118749999916, 85.56250000204838102 ) ) ;
#30489=CARTESIAN_POINT ( 'NONE',  ( 7.778174593052023411, -7.778174593052021635, 70.75000000409677625 ) ) ;
#30500=CARTESIAN_POINT ( 'NONE',  ( 10.18810118750000093, -4.220049686691933033, 113.6875000020483810 ) ) ;
#30504=CARTESIAN_POINT ( 'NONE',  ( -7.204075437095967871, 7.204075437095967871, 67.46875000204836681 ) ) ;
#30511=LINE ( 'NONE', #65948, #13117 ) ;
#30533=CARTESIAN_POINT ( 'NONE',  ( 2.020667218593132706E-15, -11.00000000000000000, 98.87499999999998579 ) ) ;
#30541=CARTESIAN_POINT ( 'NONE',  ( 10.18810118749999916, 4.220049686691935698, 86.50000000204836681 ) ) ;
#30543=CARTESIAN_POINT ( 'NONE',  ( -7.778174593052020747, -7.778174593052023411, 92.68749999999998579 ) ) ;
#30552=( BOUNDED_CURVE ( )  B_SPLINE_CURVE ( 2, ( #59710, #64629, #2734, #25722, #71375, #48743, #36331, #31026, #48000 ),
 .UNSPECIFIED., .F., .F. ) 
 B_SPLINE_CURVE_WITH_KNOTS ( ( 3, 2, 2, 2, 3 ),
 ( 0.1911764705882354198, 0.1948529411764707286, 0.1985294117647060097, 0.2022058823529413463, 0.2058823529411766273 ),
 .UNSPECIFIED. ) 
 CURVE ( )  GEOMETRIC_REPRESENTATION_ITEM ( )  RATIONAL_B_SPLINE_CURVE ( ( 0.9999999999999971134, 0.9238795325112896251, 1.000000000000000000, 0.9238795325112867385, 1.000000000000000000, 0.9238795325112867385, 1.000000000000000000, 0.9238795325112832968, 1.000000000000003553 ) ) 
 REPRESENTATION_ITEM ( '' )  );
#30571=CARTESIAN_POINT ( 'NONE',  ( -7.778174593052023411, 7.778174593052023411, 89.50000000409677625 ) ) ;
#30596=CARTESIAN_POINT ( 'NONE',  ( 10.18810118749999916, 1.247682550866122264E-15, 89.78125000204836681 ) ) ;
#30600=CARTESIAN_POINT ( 'NONE',  ( -4.220049686691935698, 10.18810118749999916, 103.3750000020484094 ) ) ;
#30610=CARTESIAN_POINT ( 'NONE',  ( -6.238412754330611322E-16, 10.18810118749999916, 100.6562500020483810 ) ) ;
#30627=CARTESIAN_POINT ( 'NONE',  ( -4.220049686691935698, 10.18810118749999916, 103.3750000020483952 ) ) ;
#30638=CARTESIAN_POINT ( 'NONE',  ( 7.778174593052021635, 7.778174593052023411, 73.93749999999998579 ) ) ;
#30645=CARTESIAN_POINT ( 'NONE',  ( 4.556349186104045934, 11.00000000000000000, 114.5312500000000142 ) ) ;
#30659=CARTESIAN_POINT ( 'NONE',  ( 11.00000000000000000, 4.556349186104045934, 102.5312500040967905 ) ) ;
#30671=CARTESIAN_POINT ( 'NONE',  ( 11.00000000000000355, -4.556349186104044158, 67.84375000409677625 ) ) ;
#30681=ADVANCED_FACE ( 'NONE', ( #13666 ), #58616, .T. ) ;
#30682=CARTESIAN_POINT ( 'NONE',  ( -4.220049686691937474, -10.18810118749999738, 111.8125000020484094 ) ) ;
#30689=CARTESIAN_POINT ( 'NONE',  ( 10.18810118749999916, 1.247682550866122264E-15, 68.78125000204838102 ) ) ;
#30692=VERTEX_POINT ( 'NONE', #36338 ) ;
#30701=CARTESIAN_POINT ( 'NONE',  ( -6.238412754330611322E-16, 10.18810118749999916, 67.28125000204838102 ) ) ;
#30734=DIRECTION ( 'NONE',  ( -0.000000000000000000, -0.000000000000000000, -1.000000000000000000 ) ) ;
#30757=CARTESIAN_POINT ( 'NONE',  ( -4.556349186104048599, -10.99999999999999822, 104.9687500040967620 ) ) ;
#30764=FACE_OUTER_BOUND ( 'NONE', #25171, .T. ) ;
#30765=CARTESIAN_POINT ( 'NONE',  ( 7.204075437095968759, -7.204075437095966983, 93.71875000204838102 ) ) ;
#30768=LINE ( 'NONE', #23632, #44834 ) ;
#30777=CARTESIAN_POINT ( 'NONE',  ( 11.00000000000000000, 1.347111479062088405E-15, 82.93750000409677625 ) ) ;
#30781=CARTESIAN_POINT ( 'NONE',  ( 10.18810118750000093, -4.220049686691933033, 89.68750000204838102 ) ) ;
#30784=ORIENTED_EDGE ( 'NONE', *, *, #5070, .T. ) ;
#30788=CARTESIAN_POINT ( 'NONE',  ( 4.220049686691941027, -10.18810118749999738, 76.00000000204838102 ) ) ;
#30794=CARTESIAN_POINT ( 'NONE',  ( 10.18810118749999916, 1.247682550866122264E-15, 83.40625000204838102 ) ) ;
#30799=EDGE_LOOP ( 'NONE', ( #17764, #55229, #43398, #63375 ) ) ;
#30805=CARTESIAN_POINT ( 'NONE',  ( -7.204075437095967871, 7.204075437095967871, 70.84375000204836681 ) ) ;
#30820=ORIENTED_EDGE ( 'NONE', *, *, #30210, .F. ) ;
#30824=CARTESIAN_POINT ( 'NONE',  ( 7.778174593052023411, -7.778174593052021635, 78.06249999999998579 ) ) ;
#30828=VERTEX_POINT ( 'NONE', #37828 ) ;
#30834=CARTESIAN_POINT ( 'NONE',  ( 4.556349186104051263, -10.99999999999999822, 115.6562500040967905 ) ) ;
#30838=DIRECTION ( 'NONE',  ( -0.000000000000000000, -0.000000000000000000, -1.000000000000000000 ) ) ;
#30853=CARTESIAN_POINT ( 'NONE',  ( 1.871523826299183495E-15, -10.18810118749999916, 87.90625000204838102 ) ) ;
#30854=CARTESIAN_POINT ( 'NONE',  ( -7.204075437095967871, 7.204075437095967871, 115.4687500020483810 ) ) ;
#30868=CARTESIAN_POINT ( 'NONE',  ( -6.238412754330611322E-16, 10.18810118749999916, 108.1562500020483668 ) ) ;
#30872=CARTESIAN_POINT ( 'NONE',  ( -4.220049686691935698, 10.18810118749999916, 67.37500000204838102 ) ) ;
#30894=CARTESIAN_POINT ( 'NONE',  ( 11.00000000000010658, 4.556349186103942017, 72.34374999999997158 ) ) ;
#30903=EDGE_LOOP ( 'NONE', ( #23827, #72379, #51180 ) ) ;
#30904=CARTESIAN_POINT ( 'NONE',  ( -7.204075437095965206, -7.204075437095968759, 78.34375000204838102 ) ) ;
#30906=CARTESIAN_POINT ( 'NONE',  ( -10.99999999999999822, -4.556349186104052151, 94.09375000000001421 ) ) ;
#30918=DIRECTION ( 'NONE',  ( 0.000000000000000000, 1.000000000000000000, 0.000000000000000000 ) ) ;
#30935=CARTESIAN_POINT ( 'NONE',  ( 11.00000000000000355, -4.556349186104045046, 85.84375000409676204 ) ) ;
#30960=EDGE_CURVE ( 'NONE', #71006, #32560, #56229, .T. ) ;
#30961=CARTESIAN_POINT ( 'NONE',  ( 4.220049686691934809, 10.18810118749999916, 94.56250000204838102 ) ) ;
#30967=CARTESIAN_POINT ( 'NONE',  ( -10.18810118749999738, -4.220049686691941915, 102.2500000020483952 ) ) ;
#30976=CARTESIAN_POINT ( 'NONE',  ( -10.18810118749999916, 0.000000000000000000, 98.03125000204838102 ) ) ;
#30981=AXIS2_PLACEMENT_3D ( 'NONE', #65796, #55618, #49943 ) ;
#30990=ORIENTED_EDGE ( 'NONE', *, *, #23939, .F. ) ;
#30991=VERTEX_POINT ( 'NONE', #16648 ) ;
#30992=CARTESIAN_POINT ( 'NONE',  ( -6.238412754330611322E-16, 10.18810118749999916, 101.7812500020483810 ) ) ;
#31001=ORIENTED_EDGE ( 'NONE', *, *, #49985, .F. ) ;
#31002=CARTESIAN_POINT ( 'NONE',  ( 0.000000000000000000, 2.348141146763140925E-15, 0.000000000000000000 ) ) ;
#31008=CARTESIAN_POINT ( 'NONE',  ( 4.556349186104052151, -10.99999999999999822, 91.65625000409680467 ) ) ;
#31009=CARTESIAN_POINT ( 'NONE',  ( -6.735557395310442023E-16, 11.00000000000000000, 114.6249999999999858 ) ) ;
#31013=CARTESIAN_POINT ( 'NONE',  ( -10.99999999999994671, -4.556349186104105442, 101.5937500000000000 ) ) ;
#31022=CARTESIAN_POINT ( 'NONE',  ( 11.00000000000000355, -4.556349186104045046, 102.3437500040967905 ) ) ;
#31026=CARTESIAN_POINT ( 'NONE',  ( -11.00000000000015632, -4.556349186103894944, 107.5937499999999716 ) ) ;
#31036=ORIENTED_EDGE ( 'NONE', *, *, #16971, .T. ) ;
#31044=CARTESIAN_POINT ( 'NONE',  ( -7.204075437095967871, 7.204075437095967871, 108.3437500020483810 ) ) ;
#31049=CYLINDRICAL_SURFACE ( 'NONE', #12220, 11.00000000000000000 ) ;
#31050=CARTESIAN_POINT ( 'NONE',  ( -4.220049686691935698, 10.18810118749999916, 69.25000000204836681 ) ) ;
#31062=CARTESIAN_POINT ( 'NONE',  ( -10.18810118749999738, -4.220049686691941915, 116.1250000020483810 ) ) ;
#31075=( BOUNDED_CURVE ( )  B_SPLINE_CURVE ( 2, ( #72127, #54427, #55927, #55177, #43841 ),
 .UNSPECIFIED., .F., .F. ) 
 B_SPLINE_CURVE_WITH_KNOTS ( ( 3, 2, 3 ),
 ( 0.009783017809147894275, 0.01102941176470588480, 0.01470588235294118667 ),
 .UNSPECIFIED. ) 
 CURVE ( )  GEOMETRIC_REPRESENTATION_ITEM ( )  RATIONAL_B_SPLINE_CURVE ( ( 0.9658850645339760455, 0.9741937033643668364, 1.000000000000000000, 0.9238795325112865164, 1.000000000000000222 ) ) 
 REPRESENTATION_ITEM ( '' )  );
#31094=CARTESIAN_POINT ( 'NONE',  ( 11.00000000000000000, 1.347111479062088405E-15, 115.9375000040967763 ) ) ;
#31103=LINE ( 'NONE', #49578, #2041 ) ;
#31110=FACE_OUTER_BOUND ( 'NONE', #5568, .T. ) ;
#31128=CARTESIAN_POINT ( 'NONE',  ( 0.000000000000000000, 0.000000000000000000, 118.0000000000000000 ) ) ;
#31129=CARTESIAN_POINT ( 'NONE',  ( 10.18810118749999916, 1.247682550866122264E-15, 92.40625000204836681 ) ) ;
#31132=CARTESIAN_POINT ( 'NONE',  ( 11.00000000000000000, 1.347111479062088405E-15, 118.0000000000000000 ) ) ;
#31137=VERTEX_POINT ( 'NONE', #38750 ) ;
#31139=EDGE_CURVE ( 'NONE', #36860, #62341, #65906, .T. ) ;
#31145=CARTESIAN_POINT ( 'NONE',  ( 1.871523826299183495E-15, -10.18810118749999916, 89.40625000204838102 ) ) ;
#31152=CARTESIAN_POINT ( 'NONE',  ( 7.204075437095968759, -7.204075437095966983, 73.09375000204838102 ) ) ;
#31160=CARTESIAN_POINT ( 'NONE',  ( -7.204075437095967871, 7.204075437095967871, 82.46875000204836681 ) ) ;
#31162=ADVANCED_FACE ( 'NONE', ( #20246 ), #31959, .F. ) ;
#31171=AXIS2_PLACEMENT_3D ( 'NONE', #66556, #38654, #5066 ) ;
#31174=CARTESIAN_POINT ( 'NONE',  ( 1.871523826299183495E-15, -10.18810118749999916, 71.40625000204836681 ) ) ;
#31197=CARTESIAN_POINT ( 'NONE',  ( 4.556349186104051263, -10.99999999999999822, 77.96874999999998579 ) ) ;
#31224=CARTESIAN_POINT ( 'NONE',  ( -4.220049686691937474, -10.18810118749999738, 89.31250000204838102 ) ) ;
#31226=CARTESIAN_POINT ( 'NONE',  ( -10.18810118749999738, -4.220049686691941915, 111.2500000020483952 ) ) ;
#31238=CARTESIAN_POINT ( 'NONE',  ( -10.18810118749999916, 0.000000000000000000, 107.0312500020483810 ) ) ;
#31255=AXIS2_PLACEMENT_3D ( 'NONE', #4684, #28054, #57493 ) ;
#31270=CARTESIAN_POINT ( 'NONE',  ( -11.00000000000010658, 4.556349186103942017, 83.40624999999998579 ) ) ;
#31275=CARTESIAN_POINT ( 'NONE',  ( -6.238412754330611322E-16, 10.18810118749999916, 82.28125000204838102 ) ) ;
#31278=CARTESIAN_POINT ( 'NONE',  ( 4.556349186104051263, -10.99999999999999822, 92.96875000000000000 ) ) ;
#31289=DIRECTION ( 'NONE',  ( 1.000000000000000000, 0.000000000000000000, 0.000000000000000000 ) ) ;
#31296=( BOUNDED_CURVE ( )  B_SPLINE_CURVE ( 2, ( #46764, #23761, #58845, #7892, #30533, #36199, #65596, #70888, #58478 ),
 .UNSPECIFIED., .F., .F. ) 
 B_SPLINE_CURVE_WITH_KNOTS ( ( 3, 2, 2, 2, 3 ),
 ( 0.3676470588235293824, 0.3713235294117646634, 0.3750000000000000000, 0.3786764705882352811, 0.3823529411764705621 ),
 .UNSPECIFIED. ) 
 CURVE ( )  GEOMETRIC_REPRESENTATION_ITEM ( )  RATIONAL_B_SPLINE_CURVE ( ( 1.000000000000001110, 0.9238795325112856283, 1.000000000000000000, 0.9238795325112867385, 1.000000000000000000, 0.9238795325112867385, 1.000000000000000000, 0.9238795325112867385, 1.000000000000000000 ) ) 
 REPRESENTATION_ITEM ( '' )  );
#31302=EDGE_LOOP ( 'NONE', ( #7608, #29466, #55864, #12732 ) ) ;
#31306=CARTESIAN_POINT ( 'NONE',  ( 11.00000000000000000, 1.347111479062088405E-15, 79.93750000409677625 ) ) ;
#31321=ORIENTED_EDGE ( 'NONE', *, *, #54673, .F. ) ;
#31323=CARTESIAN_POINT ( 'NONE',  ( -10.18810118749999916, 0.000000000000000000, 76.65625000204836681 ) ) ;
#31331=CARTESIAN_POINT ( 'NONE',  ( -6.238412754330611322E-16, 10.18810118749999916, 87.15625000204838102 ) ) ;
#31332=VERTEX_POINT ( 'NONE', #45071 ) ;
#31336=CARTESIAN_POINT ( 'NONE',  ( 1.871523826299183495E-15, -10.18810118749999916, 102.5312500020483810 ) ) ;
#31344=CARTESIAN_POINT ( 'NONE',  ( -4.220049686691937474, -10.18810118749999738, 96.81250000204839523 ) ) ;
#31352=EDGE_CURVE ( 'NONE', #56611, #55577, #66331, .T. ) ;
#31365=CARTESIAN_POINT ( 'NONE',  ( 4.220049686691934809, 10.18810118749999916, 97.18750000204836681 ) ) ;
#31385=CARTESIAN_POINT ( 'NONE',  ( 11.00000000000000000, 4.556349186104045934, 114.3437499999999858 ) ) ;
#31397=CARTESIAN_POINT ( 'NONE',  ( -7.778174593052023411, 7.778174593052023411, 98.50000000409677625 ) ) ;
#31420=CARTESIAN_POINT ( 'NONE',  ( 1.871523826299183495E-15, -10.18810118749999916, 105.9062500020483810 ) ) ;
#31429=CARTESIAN_POINT ( 'NONE',  ( 10.18810118749999916, 4.220049686691935698, 73.37500000204838102 ) ) ;
#31443=( BOUNDED_CURVE ( )  B_SPLINE_CURVE ( 2, ( #4195, #8724, #27184, #21893, #50201, #31736, #49071, #49453, #14364 ),
 .UNSPECIFIED., .F., .F. ) 
 B_SPLINE_CURVE_WITH_KNOTS ( ( 3, 2, 2, 2, 3 ),
 ( 0.3970588235294116863, 0.4007352941176470229, 0.4044117647058823040, 0.4080882352941175850, 0.4117647058823528661 ),
 .UNSPECIFIED. ) 
 CURVE ( )  GEOMETRIC_REPRESENTATION_ITEM ( )  RATIONAL_B_SPLINE_CURVE ( ( 1.000000000000001110, 0.9238795325112856283, 1.000000000000000000, 0.9238795325112867385, 1.000000000000000000, 0.9238795325112867385, 1.000000000000000000, 0.9238795325112878487, 0.9999999999999988898 ) ) 
 REPRESENTATION_ITEM ( '' )  );
#31444=CARTESIAN_POINT ( 'NONE',  ( 10.18810118749999916, 1.247682550866122264E-15, 68.40625000204836681 ) ) ;
#31461=CARTESIAN_POINT ( 'NONE',  ( 10.18810118749999916, 1.247682550866122264E-15, 116.4062500020483810 ) ) ;
#31474=CARTESIAN_POINT ( 'NONE',  ( 4.556349186104045934, 11.00000000000000000, 87.71875000409677625 ) ) ;
#31481=CARTESIAN_POINT ( 'NONE',  ( -7.778174593052020747, -7.778174593052023411, 89.68749999999998579 ) ) ;
#31511=CARTESIAN_POINT ( 'NONE',  ( 4.220049686691941027, -10.18810118749999738, 96.62500000204838102 ) ) ;
#31525=CARTESIAN_POINT ( 'NONE',  ( 7.204075437095966983, 7.204075437095967871, 86.96875000204836681 ) ) ;
#31527=EDGE_LOOP ( 'NONE', ( #74490, #39761, #50574, #54200 ) ) ;
#31531=CARTESIAN_POINT ( 'NONE',  ( 10.18810118749999916, 4.220049686691935698, 71.87500000204836681 ) ) ;
#31539=CARTESIAN_POINT ( 'NONE',  ( 1.871523826299183495E-15, -10.18810118749999916, 84.53125000204836681 ) ) ;
#31573=CARTESIAN_POINT ( 'NONE',  ( 4.556349186104045934, 11.00000000000000000, 77.03125000000000000 ) ) ;
#31584=CARTESIAN_POINT ( 'NONE',  ( 11.00000000000000355, -4.556349186104045046, 114.3437500040967763 ) ) ;
#31601=CARTESIAN_POINT ( 'NONE',  ( -7.204075437095965206, -7.204075437095968759, 86.21875000204836681 ) ) ;
#31602=CARTESIAN_POINT ( 'NONE',  ( 4.220049686691934809, 10.18810118749999916, 113.6875000020483952 ) ) ;
#31614=CARTESIAN_POINT ( 'NONE',  ( 10.18810118749999916, 1.247682550866122264E-15, 104.7812500020483810 ) ) ;
#31626=ADVANCED_FACE ( 'NONE', ( #24637 ), #52223, .T. ) ;
#31650=EDGE_CURVE ( 'NONE', #40937, #11029, #31742, .T. ) ;
#31655=CARTESIAN_POINT ( 'NONE',  ( 10.18810118750000093, -4.220049686691933033, 81.81250000204838102 ) ) ;
#31658=CARTESIAN_POINT ( 'NONE',  ( 4.556349186104051263, -10.99999999999999822, 94.46874999999998579 ) ) ;
#31685=CARTESIAN_POINT ( 'NONE',  ( -11.00000000000000000, 0.000000000000000000, 80.68750000409677625 ) ) ;
#31687=CARTESIAN_POINT ( 'NONE',  ( 7.778174593052021635, 7.778174593052023411, 78.62500000409677625 ) ) ;
#31704=CARTESIAN_POINT ( 'NONE',  ( 7.204075437095966983, 7.204075437095967871, 74.59375000204838102 ) ) ;
#31706=DIRECTION ( 'NONE',  ( -0.000000000000000000, -0.000000000000000000, -1.000000000000000000 ) ) ;
#31712=CARTESIAN_POINT ( 'NONE',  ( 10.18810118749999916, 4.220049686691935698, 85.37500000204839523 ) ) ;
#31714=EDGE_CURVE ( 'NONE', #30991, #27901, #34190, .T. ) ;
#31718=CARTESIAN_POINT ( 'NONE',  ( 10.18810118749999916, 1.247682550866122264E-15, 102.9062500020483810 ) ) ;
#31726=CARTESIAN_POINT ( 'NONE',  ( 7.204075437095968759, -7.204075437095966983, 95.59375000204838102 ) ) ;
#31734=DIRECTION ( 'NONE',  ( -1.224646799147353207E-16, 1.000000000000000000, 0.000000000000000000 ) ) ;
#31736=CARTESIAN_POINT ( 'NONE',  ( -4.556349186104048599, -10.99999999999999822, 95.96875000409676204 ) ) ;
#31739=DIRECTION ( 'NONE',  ( -0.000000000000000000, -0.000000000000000000, -1.000000000000000000 ) ) ;
#31742=( BOUNDED_CURVE ( )  B_SPLINE_CURVE ( 2, ( #8406, #44241, #54068, #14799, #65745, #32558, #37838, #54820, #60835 ),
 .UNSPECIFIED., .F., .F. ) 
 B_SPLINE_CURVE_WITH_KNOTS ( ( 3, 2, 2, 2, 3 ),
 ( 0.8970588235294117974, 0.9007352941176470784, 0.9044117647058823595, 0.9080882352941176405, 0.9117647058823529216 ),
 .UNSPECIFIED. ) 
 CURVE ( )  GEOMETRIC_REPRESENTATION_ITEM ( )  RATIONAL_B_SPLINE_CURVE ( ( 1.000000000000000000, 0.9238795325112867385, 1.000000000000000000, 0.9238795325112867385, 1.000000000000000000, 0.9238795325112867385, 1.000000000000000000, 0.9238795325112867385, 1.000000000000000000 ) ) 
 REPRESENTATION_ITEM ( '' )  );
#31743=ORIENTED_EDGE ( 'NONE', *, *, #69031, .T. ) ;
#31744=CARTESIAN_POINT ( 'NONE',  ( 10.18810118750000093, -4.220049686691933033, 98.31250000204836681 ) ) ;
#31762=CARTESIAN_POINT ( 'NONE',  ( 2.020667218593132706E-15, -11.00000000000000000, 113.8749999999999858 ) ) ;
#31764=( BOUNDED_CURVE ( )  B_SPLINE_CURVE ( 2, ( #53442, #2117, #59107, #7414, #1402, #24387, #70417, #25110, #47395 ),
 .UNSPECIFIED., .F., .F. ) 
 B_SPLINE_CURVE_WITH_KNOTS ( ( 3, 2, 2, 2, 3 ),
 ( 0.2941176470588234837, 0.2977941176470587648, 0.3014705882352940458, 0.3051470588235293824, 0.3088235294117646634 ),
 .UNSPECIFIED. ) 
 CURVE ( )  GEOMETRIC_REPRESENTATION_ITEM ( )  RATIONAL_B_SPLINE_CURVE ( ( 1.000000000000001110, 0.9238795325112856283, 1.000000000000000000, 0.9238795325112867385, 1.000000000000000000, 0.9238795325112867385, 1.000000000000000000, 0.9238795325112878487, 0.9999999999999988898 ) ) 
 REPRESENTATION_ITEM ( '' )  );
#31775=CARTESIAN_POINT ( 'NONE',  ( -10.99999999999999822, -4.556349186104052151, 98.78125000409679046 ) ) ;
#31784=ADVANCED_FACE ( 'NONE', ( #49892 ), #25742, .T. ) ;
#31798=CARTESIAN_POINT ( 'NONE',  ( -11.00000000000000000, 0.000000000000000000, 73.18750000409676204 ) ) ;
#31801=CARTESIAN_POINT ( 'NONE',  ( -4.220049686691935698, 10.18810118749999916, 102.2500000020483952 ) ) ;
#31808=CARTESIAN_POINT ( 'NONE',  ( -7.204075437095967871, 7.204075437095967871, 72.34375000204836681 ) ) ;
#31810=ORIENTED_EDGE ( 'NONE', *, *, #66443, .F. ) ;
#31811=CARTESIAN_POINT ( 'NONE',  ( 10.18810118749999916, 4.220049686691935698, 116.5000000020483810 ) ) ;
#31821=CARTESIAN_POINT ( 'NONE',  ( -4.220049686691937474, -10.18810118749999738, 116.3125000020483668 ) ) ;
#31835=CARTESIAN_POINT ( 'NONE',  ( -6.238412754330611322E-16, 10.18810118749999916, 115.2812500020483810 ) ) ;
#31851=CARTESIAN_POINT ( 'NONE',  ( -11.00000000000000000, 0.000000000000000000, 110.4999999999999858 ) ) ;
#31875=CARTESIAN_POINT ( 'NONE',  ( 7.778174593052023411, -7.778174593052021635, 105.2500000040967763 ) ) ;
#31885=CARTESIAN_POINT ( 'NONE',  ( 10.18810118749999916, 4.220049686691935698, 94.00000000204838102 ) ) ;
#31899=CARTESIAN_POINT ( 'NONE',  ( -4.220049686691937474, -10.18810118749999738, 90.81250000204838102 ) ) ;
#31914=CARTESIAN_POINT ( 'NONE',  ( 10.18810118750000093, -4.220049686691933921, 86.31250000204838102 ) ) ;
#31926=CARTESIAN_POINT ( 'NONE',  ( 4.556349186104052151, -10.99999999999999822, 76.46874999999998579 ) ) ;
#31930=DIRECTION ( 'NONE',  ( -7.885106708985487801E-17, 1.000000000000000000, -0.000000000000000000 ) ) ;
#31937=CARTESIAN_POINT ( 'NONE',  ( 7.778174593052023411, -7.778174593052021635, 93.06249999999998579 ) ) ;
#31946=CARTESIAN_POINT ( 'NONE',  ( -7.778174593052023411, 7.778174593052023411, 69.81249999999998579 ) ) ;
#31956=CARTESIAN_POINT ( 'NONE',  ( -6.735557395310442023E-16, 11.00000000000000000, 114.8125000040967763 ) ) ;
#31959=PLANE ( 'NONE',  #56660 ) ;
#31973=CARTESIAN_POINT ( 'NONE',  ( 1.871523826299183495E-15, -10.18810118749999916, 84.90625000204838102 ) ) ;
#31975=CARTESIAN_POINT ( 'NONE',  ( 4.220049686691941027, -10.18810118749999738, 113.1250000020483810 ) ) ;
#31979=CARTESIAN_POINT ( 'NONE',  ( -11.00000000000000000, 0.000000000000000000, 118.0000000000000000 ) ) ;
#31987=DIRECTION ( 'NONE',  ( 0.000000000000000000, 0.000000000000000000, -1.000000000000000000 ) ) ;
#31991=CARTESIAN_POINT ( 'NONE',  ( -7.204075437095965206, -7.204075437095968759, 104.2187500020483810 ) ) ;
#32016=CARTESIAN_POINT ( 'NONE',  ( -4.556349186104048599, -10.99999999999999822, 77.96875000409677625 ) ) ;
#32028=ORIENTED_EDGE ( 'NONE', *, *, #69346, .T. ) ;
#32029=CARTESIAN_POINT ( 'NONE',  ( 10.18810118749999916, 1.247682550866122264E-15, 81.90625000204838102 ) ) ;
#32032=CARTESIAN_POINT ( 'NONE',  ( -7.778174593052020747, -7.778174593052023411, 95.68750000000000000 ) ) ;
#32036=CARTESIAN_POINT ( 'NONE',  ( -4.556349186104048599, -10.99999999999999822, 83.78124999999998579 ) ) ;
#32044=LINE ( 'NONE', #53572, #2346 ) ;
#32061=CARTESIAN_POINT ( 'NONE',  ( -7.778174593052023411, 7.778174593052023411, 82.00000000409676204 ) ) ;
#32079=CARTESIAN_POINT ( 'NONE',  ( -4.220049686691937474, -10.18810118749999738, 79.93750000204839523 ) ) ;
#32088=CARTESIAN_POINT ( 'NONE',  ( -4.220049686691935698, 10.18810118749999916, 85.75000000204838102 ) ) ;
#32089=VERTEX_POINT ( 'NONE', #6318 ) ;
#32094=CARTESIAN_POINT ( 'NONE',  ( 10.18810118750000093, -4.220049686691933921, 95.31250000204838102 ) ) ;
#32103=CARTESIAN_POINT ( 'NONE',  ( 1.871523826299183495E-15, -10.18810118749999916, 92.40625000204836681 ) ) ;
#32104=VECTOR ( 'NONE', #35699, 1000.000000000000000 ) ;
#32120=CARTESIAN_POINT ( 'NONE',  ( 10.18810118749999916, 1.247682550866122264E-15, 96.90625000204838102 ) ) ;
#32133=ORIENTED_EDGE ( 'NONE', *, *, #72520, .F. ) ;
#32140=CARTESIAN_POINT ( 'NONE',  ( -4.556349186104045934, 11.00000000000000000, 116.2187500000000000 ) ) ;
#32153=CARTESIAN_POINT ( 'NONE',  ( -4.556349186104047710, -10.99999999999999822, 97.46875000409677625 ) ) ;
#32161=CIRCLE ( 'NONE', #57434, 11.00000000000000000 ) ;
#32176=DIRECTION ( 'NONE',  ( -0.000000000000000000, -0.000000000000000000, -1.000000000000000000 ) ) ;
#32177=CARTESIAN_POINT ( 'NONE',  ( 10.18810118749999916, 1.247682550866122264E-15, 101.7812500020483810 ) ) ;
#32183=CARTESIAN_POINT ( 'NONE',  ( -6.238412754330611322E-16, 10.18810118749999916, 67.65625000204836681 ) ) ;
#32186=CARTESIAN_POINT ( 'NONE',  ( -7.204075437095965206, -7.204075437095968759, 112.8437500020483810 ) ) ;
#32196=CARTESIAN_POINT ( 'NONE',  ( -10.18810118749999916, 0.000000000000000000, 67.65625000204836681 ) ) ;
#32237=CYLINDRICAL_SURFACE ( 'NONE', #55405, 11.00000000000000000 ) ;
#32256=FACE_OUTER_BOUND ( 'NONE', #3401, .T. ) ;
#32266=CARTESIAN_POINT ( 'NONE',  ( 1.871523826299183495E-15, -10.18810118749999916, 96.53125000204838102 ) ) ;
#32272=CARTESIAN_POINT ( 'NONE',  ( -7.778174593052020747, -7.778174593052023411, 95.68750000000000000 ) ) ;
#32281=CARTESIAN_POINT ( 'NONE',  ( 4.220049686691941027, -10.18810118749999738, 83.50000000204839523 ) ) ;
#32293=CARTESIAN_POINT ( 'NONE',  ( -10.18810118749999916, 4.220049686691934809, 81.06250000204836681 ) ) ;
#32306=B_SPLINE_CURVE_WITH_KNOTS ( 'NONE', 1,
 ( #3952, #15615 ),
 .UNSPECIFIED., .F., .F.,
 ( 2, 2 ),
 ( 0.000000000000000000, 1.000000000000000000 ),
 .UNSPECIFIED. ) ;
#32311=EDGE_CURVE ( 'NONE', #72648, #68675, #26982, .T. ) ;
#32331=CARTESIAN_POINT ( 'NONE',  ( -7.778174593052020747, -7.778174593052023411, 71.68749999999998579 ) ) ;
#32337=EDGE_CURVE ( 'NONE', #64267, #9770, #60166, .T. ) ;
#32343=FACE_OUTER_BOUND ( 'NONE', #1668, .T. ) ;
#32347=CARTESIAN_POINT ( 'NONE',  ( 11.00000000000000000, 1.347111479062088405E-15, 111.2499999999999858 ) ) ;
#32357=CARTESIAN_POINT ( 'NONE',  ( 4.220049686691934809, 10.18810118749999916, 115.1875000020483668 ) ) ;
#32361=CARTESIAN_POINT ( 'NONE',  ( 4.556349186104052151, -10.99999999999999822, 106.4687499999999716 ) ) ;
#32370=CARTESIAN_POINT ( 'NONE',  ( -4.220049686691937474, -10.18810118749999738, 108.8125000020483952 ) ) ;
#32372=ORIENTED_EDGE ( 'NONE', *, *, #66274, .T. ) ;
#32380=CARTESIAN_POINT ( 'NONE',  ( 2.020667218593132706E-15, -11.00000000000000000, 72.06250000409677625 ) ) ;
#32391=ORIENTED_EDGE ( 'NONE', *, *, #65738, .T. ) ;
#32410=CARTESIAN_POINT ( 'NONE',  ( 4.220049686691941027, -10.18810118749999738, 81.62500000204836681 ) ) ;
#32413=CARTESIAN_POINT ( 'NONE',  ( 2.020667218593132706E-15, -11.00000000000000000, 89.87499999999998579 ) ) ;
#32420=EDGE_CURVE ( 'NONE', #22788, #32460, #16026, .T. ) ;
#32427=CARTESIAN_POINT ( 'NONE',  ( -11.00000000000000000, 0.000000000000000000, 98.68750000409677625 ) ) ;
#32439=CARTESIAN_POINT ( 'NONE',  ( 2.020667218593132706E-15, -11.00000000000000000, 71.87500000000000000 ) ) ;
#32444=CARTESIAN_POINT ( 'NONE',  ( 7.778174593052021635, 7.778174593052023411, 81.62500000409677625 ) ) ;
#32460=VERTEX_POINT ( 'NONE', #27349 ) ;
#32462=CARTESIAN_POINT ( 'NONE',  ( -10.18810118749999738, -4.220049686691941915, 75.25000000204836681 ) ) ;
#32470=CARTESIAN_POINT ( 'NONE',  ( -4.220049686691937474, -10.18810118749999738, 87.81250000204838102 ) ) ;
#32476=CARTESIAN_POINT ( 'NONE',  ( -7.204075437095967871, 7.204075437095967871, 94.46875000204838102 ) ) ;
#32478=ORIENTED_EDGE ( 'NONE', *, *, #31650, .F. ) ;
#32485=CARTESIAN_POINT ( 'NONE',  ( 10.18810118749999916, 1.247682550866122264E-15, 92.78125000204836681 ) ) ;
#32492=VERTEX_POINT ( 'NONE', #55300 ) ;
#32496=ADVANCED_FACE ( 'NONE', ( #72643 ), #39059, .T. ) ;
#32502=CARTESIAN_POINT ( 'NONE',  ( -7.204075437095965206, -7.204075437095968759, 99.34375000204836681 ) ) ;
#32505=CARTESIAN_POINT ( 'NONE',  ( 11.00000000000000000, 4.556349186104045934, 105.3437499999999858 ) ) ;
#32537=CARTESIAN_POINT ( 'NONE',  ( 11.00000000000000000, 4.556349186104045934, 96.53125000409677625 ) ) ;
#32558=CARTESIAN_POINT ( 'NONE',  ( -4.556349186104048599, -10.99999999999999822, 70.46875000409677625 ) ) ;
#32559=CARTESIAN_POINT ( 'NONE',  ( -10.18810118749999738, -4.220049686691941915, 104.1250000020483810 ) ) ;
#32560=VERTEX_POINT ( 'NONE', #26460 ) ;
#32564=CARTESIAN_POINT ( 'NONE',  ( 7.778174593052021635, 7.778174593052023411, 97.93749999999998579 ) ) ;
#32569=CARTESIAN_POINT ( 'NONE',  ( -10.18810118749999916, 4.220049686691934809, 115.5625000020483810 ) ) ;
#32575=DIRECTION ( 'NONE',  ( -1.000000000000000000, 0.000000000000000000, 0.000000000000000000 ) ) ;
#32579=CARTESIAN_POINT ( 'NONE',  ( 10.18810118749999916, 4.220049686691935698, 110.8750000020483810 ) ) ;
#32582=LINE ( 'NONE', #4274, #64349 ) ;
#32587=AXIS2_PLACEMENT_3D ( 'NONE', #18613, #41624, #25729 ) ;
#32590=CARTESIAN_POINT ( 'NONE',  ( -10.18810118749999916, 0.000000000000000000, 69.53125000204838102 ) ) ;
#32623=CARTESIAN_POINT ( 'NONE',  ( 0.000000000000000000, 0.000000000000000000, 118.0000000000000000 ) ) ;
#32648=CARTESIAN_POINT ( 'NONE',  ( 10.18810118749999916, 1.247682550866122264E-15, 90.90625000204836681 ) ) ;
#32653=AXIS2_PLACEMENT_3D ( 'NONE', #52020, #11651, #5628 ) ;
#32656=CARTESIAN_POINT ( 'NONE',  ( -11.00000000000000000, 4.556349186104045934, 77.40624999999998579 ) ) ;
#32662=CARTESIAN_POINT ( 'NONE',  ( 4.220049686691934809, 10.18810118749999916, 84.06250000204838102 ) ) ;
#32676=CARTESIAN_POINT ( 'NONE',  ( 10.18810118749999916, 4.220049686691935698, 74.50000000204838102 ) ) ;
#32680=CARTESIAN_POINT ( 'NONE',  ( -11.00000000000000000, 0.000000000000000000, 110.4999999999999858 ) ) ;
#32689=CARTESIAN_POINT ( 'NONE',  ( -7.778174593052020747, -7.778174593052023411, 76.18749999999998579 ) ) ;
#32690=CARTESIAN_POINT ( 'NONE',  ( 2.020667218593132706E-15, -11.00000000000000000, 73.56250000409676204 ) ) ;
#32694=CARTESIAN_POINT ( 'NONE',  ( 10.99999999999999467, 11.00000000000000355, 41.99999999999999289 ) ) ;
#32710=CARTESIAN_POINT ( 'NONE',  ( 7.778174593052021635, 7.778174593052023411, 72.43749999999998579 ) ) ;
#32717=CARTESIAN_POINT ( 'NONE',  ( -7.778174593052020747, -7.778174593052023411, 113.8750000040967763 ) ) ;
#32735=ORIENTED_EDGE ( 'NONE', *, *, #48044, .F. ) ;
#32736=CARTESIAN_POINT ( 'NONE',  ( 1.871523826299183495E-15, -10.18810118749999916, 107.0312500020483810 ) ) ;
#32746=EDGE_CURVE ( 'NONE', #72571, #5227, #52904, .T. ) ;
#32751=CARTESIAN_POINT ( 'NONE',  ( -6.238412754330611322E-16, 10.18810118749999916, 102.1562500020483810 ) ) ;
#32771=CARTESIAN_POINT ( 'NONE',  ( -10.18810118749999916, 0.000000000000000000, 78.53125000204836681 ) ) ;
#32790=CARTESIAN_POINT ( 'NONE',  ( -10.18810118749999916, 0.000000000000000000, 76.65625000204836681 ) ) ;
#32793=CARTESIAN_POINT ( 'NONE',  ( 4.556349186104045934, 11.00000000000000000, 92.03124999999998579 ) ) ;
#32822=CARTESIAN_POINT ( 'NONE',  ( 11.00000000000000355, -4.556349186104045046, 82.84375000409676204 ) ) ;
#32836=CARTESIAN_POINT ( 'NONE',  ( -7.204075437095967871, 7.204075437095967871, 117.3437500020483810 ) ) ;
#32837=ORIENTED_EDGE ( 'NONE', *, *, #51131, .T. ) ;
#32839=CARTESIAN_POINT ( 'NONE',  ( 4.220049686691941027, -10.18810118749999738, 77.12500000204838102 ) ) ;
#32841=CYLINDRICAL_SURFACE ( 'NONE', #64177, 11.00000000000000000 ) ;
#32850=CARTESIAN_POINT ( 'NONE',  ( -7.204075437095967871, 7.204075437095967871, 84.34375000204836681 ) ) ;
#32854=CARTESIAN_POINT ( 'NONE',  ( -7.778174593052020747, -7.778174593052023411, 89.87500000409677625 ) ) ;
#32857=CARTESIAN_POINT ( 'NONE',  ( -7.204075437095965206, -7.204075437095968759, 96.34375000204836681 ) ) ;
#32863=ADVANCED_FACE ( 'NONE', ( #15519 ), #22293, .T. ) ;
#32865=CARTESIAN_POINT ( 'NONE',  ( -4.220049686691937474, -10.18810118749999738, 92.31250000204838102 ) ) ;
#32884=CARTESIAN_POINT ( 'NONE',  ( -4.220049686691937474, -10.18810118749999738, 97.93750000204836681 ) ) ;
#32887=CARTESIAN_POINT ( 'NONE',  ( 11.00000000000000000, 1.347111479062088405E-15, 106.7500000000000000 ) ) ;
#32891=AXIS2_PLACEMENT_3D ( 'NONE', #73200, #26403, #20758 ) ;
#32918=CARTESIAN_POINT ( 'NONE',  ( 7.778174593052023411, -7.778174593052021635, 96.25000000409677625 ) ) ;
#32939=CARTESIAN_POINT ( 'NONE',  ( -10.18810118749999916, 4.220049686691934809, 100.9375000020483810 ) ) ;
#32948=CARTESIAN_POINT ( 'NONE',  ( 7.204075437095968759, -7.204075437095966983, 113.2187500020483810 ) ) ;
#32958=CARTESIAN_POINT ( 'NONE',  ( -10.18810118749999738, -4.220049686691941915, 110.1250000020483810 ) ) ;
#32964=ORIENTED_EDGE ( 'NONE', *, *, #35325, .F. ) ;
#33018=ORIENTED_EDGE ( 'NONE', *, *, #32746, .T. ) ;
#33019=EDGE_CURVE ( 'NONE', #2280, #2612, #72125, .T. ) ;
#33027=CARTESIAN_POINT ( 'NONE',  ( 1.871523826299183495E-15, -10.18810118749999916, 89.03125000204836681 ) ) ;
#33028=FACE_OUTER_BOUND ( 'NONE', #11106, .T. ) ;
#33030=CARTESIAN_POINT ( 'NONE',  ( -11.00000000000000000, 0.000000000000000000, 106.0000000000000000 ) ) ;
#33042=CARTESIAN_POINT ( 'NONE',  ( 7.204075437095968759, -7.204075437095966983, 80.59375000204838102 ) ) ;
#33054=ORIENTED_EDGE ( 'NONE', *, *, #6221, .F. ) ;
#33056=CARTESIAN_POINT ( 'NONE',  ( -10.18810118749999916, 0.000000000000000000, 78.15625000204836681 ) ) ;
#33084=CARTESIAN_POINT ( 'NONE',  ( 11.00000000000000000, 1.347111479062088405E-15, 109.7499999999999858 ) ) ;
#33088=VERTEX_POINT ( 'NONE', #66469 ) ;
#33093=CARTESIAN_POINT ( 'NONE',  ( -10.99999999999999822, -4.556349186104052151, 68.59374999999997158 ) ) ;
#33121=CARTESIAN_POINT ( 'NONE',  ( -10.18810118749999916, 0.000000000000000000, 105.1562500020483810 ) ) ;
#33134=EDGE_CURVE ( 'NONE', #21890, #33983, #41877, .T. ) ;
#33135=CARTESIAN_POINT ( 'NONE',  ( -10.18810118749999916, 0.000000000000000000, 102.5312500020483810 ) ) ;
#33148=AXIS2_PLACEMENT_3D ( 'NONE', #45196, #3721, #33160 ) ;
#33155=CARTESIAN_POINT ( 'NONE',  ( 10.18810118749999916, 1.247682550866122264E-15, 83.78125000204838102 ) ) ;
#33156=ORIENTED_EDGE ( 'NONE', *, *, #43034, .F. ) ;
#33160=DIRECTION ( 'NONE',  ( -1.000000000000000000, 0.000000000000000000, 0.000000000000000000 ) ) ;
#33167=EDGE_CURVE ( 'NONE', #3255, #72883, #61934, .T. ) ;
#33170=ORIENTED_EDGE ( 'NONE', *, *, #65929, .T. ) ;
#33172=CARTESIAN_POINT ( 'NONE',  ( 7.204075437095966983, 7.204075437095967871, 73.09375000204838102 ) ) ;
#33175=CARTESIAN_POINT ( 'NONE',  ( 4.556349186104045934, 11.00000000000000000, 90.53125000000000000 ) ) ;
#33180=CYLINDRICAL_SURFACE ( 'NONE', #69692, 11.00000000000000000 ) ;
#33199=CARTESIAN_POINT ( 'NONE',  ( -4.556349186104048599, -10.99999999999999822, 71.78125000000000000 ) ) ;
#33204=CARTESIAN_POINT ( 'NONE',  ( 11.00000000000000000, 4.556349186104045934, 74.03125000409677625 ) ) ;
#33217=VERTEX_POINT ( 'NONE', #68709 ) ;
#33219=CARTESIAN_POINT ( 'NONE',  ( 10.18810118750000093, -4.220049686691933921, 69.81250000204835260 ) ) ;
#33226=CARTESIAN_POINT ( 'NONE',  ( -10.18810118749999916, 4.220049686691934809, 79.93750000204839523 ) ) ;
#33238=CARTESIAN_POINT ( 'NONE',  ( -10.18810118749999916, 4.220049686691934809, 90.43750000204836681 ) ) ;
#33253=CARTESIAN_POINT ( 'NONE',  ( 7.204075437095966983, 7.204075437095967871, 89.59375000204838102 ) ) ;
#33256=CARTESIAN_POINT ( 'NONE',  ( 4.556349186104045934, 11.00000000000000000, 110.0312500000000000 ) ) ;
#33265=DIRECTION ( 'NONE',  ( 1.000000000000000000, 0.000000000000000000, -0.000000000000000000 ) ) ;
#33285=CARTESIAN_POINT ( 'NONE',  ( 7.778174593052023411, -7.778174593052021635, 94.75000000409677625 ) ) ;
#33308=CARTESIAN_POINT ( 'NONE',  ( 10.18810118749999916, 4.220049686691935698, 100.3750000020484094 ) ) ;
#33318=CARTESIAN_POINT ( 'NONE',  ( 10.18810118749999916, 1.247682550866122264E-15, 111.9062500020483810 ) ) ;
#33325=CARTESIAN_POINT ( 'NONE',  ( -7.778174593052020747, -7.778174593052023411, 103.3750000040967763 ) ) ;
#33326=CARTESIAN_POINT ( 'NONE',  ( -6.238412754330611322E-16, 10.18810118749999916, 112.6562500020483810 ) ) ;
#33328=CARTESIAN_POINT ( 'NONE',  ( -11.00000000000000000, 4.556349186104045934, 75.90624999999998579 ) ) ;
#33330=( BOUNDED_CURVE ( )  B_SPLINE_CURVE ( 2, ( #55430, #49758, #20323, #60321, #73145, #32036, #50129, #20704, #55805 ),
 .UNSPECIFIED., .F., .F. ) 
 B_SPLINE_CURVE_WITH_KNOTS ( ( 3, 2, 2, 2, 3 ),
 ( 0.6617647058823528106, 0.6654411764705880916, 0.6691176470588233727, 0.6727941176470587648, 0.6764705882352940458 ),
 .UNSPECIFIED. ) 
 CURVE ( )  GEOMETRIC_REPRESENTATION_ITEM ( )  RATIONAL_B_SPLINE_CURVE ( ( 1.000000000000002220, 0.9238795325112844070, 1.000000000000000000, 0.9238795325112867385, 1.000000000000000000, 0.9238795325112867385, 1.000000000000000000, 0.9238795325112890700, 0.9999999999999976685 ) ) 
 REPRESENTATION_ITEM ( '' )  );
#33335=CARTESIAN_POINT ( 'NONE',  ( -10.18810118749999916, 4.220049686691934809, 69.43750000204838102 ) ) ;
#33341=CARTESIAN_POINT ( 'NONE',  ( 4.220049686691941027, -10.18810118749999738, 108.6250000020483668 ) ) ;
#33364=CARTESIAN_POINT ( 'NONE',  ( 5.094045771088254959, 8.823157229062946527, 67.15552375567561683 ) ) ;
#33373=CARTESIAN_POINT ( 'NONE',  ( 11.00000000000000000, 1.347111479062088405E-15, 118.0000000000000000 ) ) ;
#33378=DIRECTION ( 'NONE',  ( -0.000000000000000000, -0.000000000000000000, -1.000000000000000000 ) ) ;
#33385=CARTESIAN_POINT ( 'NONE',  ( 4.556349186104045934, 11.00000000000000000, 104.0312499999999858 ) ) ;
#33391=CARTESIAN_POINT ( 'NONE',  ( -10.18810118749999916, 0.000000000000000000, 87.15625000204838102 ) ) ;
#33395=CARTESIAN_POINT ( 'NONE',  ( 2.020667218593132706E-15, -11.00000000000000000, 73.56250000409676204 ) ) ;
#33405=CARTESIAN_POINT ( 'NONE',  ( -10.18810118749999916, 0.000000000000000000, 86.03125000204836681 ) ) ;
#33419=CARTESIAN_POINT ( 'NONE',  ( 10.18810118749999916, 1.247682550866122264E-15, 78.90625000204836681 ) ) ;
#33452=CARTESIAN_POINT ( 'NONE',  ( 11.00000000000000000, 1.347111479062088405E-15, 118.0000000000000000 ) ) ;
#33457=CARTESIAN_POINT ( 'NONE',  ( 7.778174593052023411, -7.778174593052021635, 72.06249999999998579 ) ) ;
#33466=EDGE_CURVE ( 'NONE', #11029, #30991, #1825, .T. ) ;
#33475=ORIENTED_EDGE ( 'NONE', *, *, #27549, .F. ) ;
#33483=CARTESIAN_POINT ( 'NONE',  ( 4.220049686691934809, 10.18810118749999916, 106.1875000020483810 ) ) ;
#33499=CARTESIAN_POINT ( 'NONE',  ( 1.871523826299183495E-15, -10.18810118749999916, 101.4062500020483810 ) ) ;
#33501=ORIENTED_EDGE ( 'NONE', *, *, #66030, .F. ) ;
#33522=CARTESIAN_POINT ( 'NONE',  ( 10.18810118749999916, 4.220049686691935698, 79.37500000204838102 ) ) ;
#33529=CYLINDRICAL_SURFACE ( 'NONE', #33148, 11.00000000000000000 ) ;
#33541=CARTESIAN_POINT ( 'NONE',  ( 10.18810118750000093, -4.220049686691933033, 77.31250000204836681 ) ) ;
#33544=CARTESIAN_POINT ( 'NONE',  ( -7.778174593052020747, -7.778174593052023411, 89.68749999999998579 ) ) ;
#33571=CARTESIAN_POINT ( 'NONE',  ( 7.778174593052021635, 7.778174593052023411, 77.12500000409677625 ) ) ;
#33588=CARTESIAN_POINT ( 'NONE',  ( -10.18810118749999916, 0.000000000000000000, 69.15625000204836681 ) ) ;
#33597=CARTESIAN_POINT ( 'NONE',  ( -7.204075437095965206, -7.204075437095968759, 81.71875000204836681 ) ) ;
#33625=CARTESIAN_POINT ( 'NONE',  ( 4.220049686691934809, 10.18810118749999916, 91.18750000204836681 ) ) ;
#33628=CARTESIAN_POINT ( 'NONE',  ( -11.00000000000000000, 0.000000000000000000, 104.5000000000000000 ) ) ;
#33652=CARTESIAN_POINT ( 'NONE',  ( 7.778174593052023411, -7.778174593052021635, 88.56249999999998579 ) ) ;
#33657=CARTESIAN_POINT ( 'NONE',  ( -7.778174593052020747, -7.778174593052023411, 92.87500000409677625 ) ) ;
#33682=CARTESIAN_POINT ( 'NONE',  ( -7.204075437095967871, 7.204075437095967871, 96.34375000204836681 ) ) ;
#33690=ORIENTED_EDGE ( 'NONE', *, *, #44530, .T. ) ;
#33691=CARTESIAN_POINT ( 'NONE',  ( 7.204075437095968759, -7.204075437095966983, 116.2187500020483810 ) ) ;
#33699=CARTESIAN_POINT ( 'NONE',  ( 1.871523826299183495E-15, -10.18810118749999916, 108.9062500020483668 ) ) ;
#33717=CARTESIAN_POINT ( 'NONE',  ( -7.204075437095965206, -7.204075437095968759, 108.3437500020483810 ) ) ;
#33733=CARTESIAN_POINT ( 'NONE',  ( 4.556349186104045934, 11.00000000000000000, 107.2187500040967905 ) ) ;
#33740=ORIENTED_EDGE ( 'NONE', *, *, #67182, .T. ) ;
#33742=CARTESIAN_POINT ( 'NONE',  ( -4.556349186104045934, 11.00000000000000000, 113.4062500040967763 ) ) ;
#33760=CARTESIAN_POINT ( 'NONE',  ( 11.00000000000000000, 1.347111479062088405E-15, 103.7500000000000000 ) ) ;
#33766=CARTESIAN_POINT ( 'NONE',  ( 1.871523826299183495E-15, -10.18810118749999916, 92.03125000204836681 ) ) ;
#33774=LINE ( 'NONE', #39777, #44302 ) ;
#33779=CARTESIAN_POINT ( 'NONE',  ( 10.18810118749999916, 4.220049686691935698, 83.87500000204836681 ) ) ;
#33796=CARTESIAN_POINT ( 'NONE',  ( -10.18810118749999738, -4.220049686691941915, 75.25000000204836681 ) ) ;
#33806=CARTESIAN_POINT ( 'NONE',  ( 11.00000000000000000, 1.347111479062088405E-15, 93.43750000409677625 ) ) ;
#33858=CARTESIAN_POINT ( 'NONE',  ( -7.204075437095965206, -7.204075437095968759, 106.8437500020483810 ) ) ;
#33874=CARTESIAN_POINT ( 'NONE',  ( -10.18810118749999916, 0.000000000000000000, 101.0312500020483810 ) ) ;
#33886=( BOUNDED_CURVE ( )  B_SPLINE_CURVE ( 2, ( #9213, #61268, #38643, #72963, #22013, #43917, #3558, #55251, #9964 ),
 .UNSPECIFIED., .F., .F. ) 
 B_SPLINE_CURVE_WITH_KNOTS ( ( 3, 2, 2, 2, 3 ),
 ( 0.1323529411764707009, 0.1360294117647059819, 0.1397058823529412908, 0.1433823529411765718, 0.1470588235294118806 ),
 .UNSPECIFIED. ) 
 CURVE ( )  GEOMETRIC_REPRESENTATION_ITEM ( )  RATIONAL_B_SPLINE_CURVE ( ( 0.9999999999999976685, 0.9238795325112890700, 1.000000000000000000, 0.9238795325112867385, 1.000000000000000000, 0.9238795325112867385, 1.000000000000000000, 0.9238795325112844070, 1.000000000000002220 ) ) 
 REPRESENTATION_ITEM ( '' )  );
#33895=( BOUNDED_CURVE ( )  B_SPLINE_CURVE ( 2, ( #12296, #1368, #25078, #47725, #59075, #8116, #13387, #52665, #35331 ),
 .UNSPECIFIED., .F., .F. ) 
 B_SPLINE_CURVE_WITH_KNOTS ( ( 3, 2, 2, 2, 3 ),
 ( 0.2941176470588234282, 0.2977941176470587092, 0.3014705882352939903, 0.3051470588235293269, 0.3088235294117646079 ),
 .UNSPECIFIED. ) 
 CURVE ( )  GEOMETRIC_REPRESENTATION_ITEM ( )  RATIONAL_B_SPLINE_CURVE ( ( 1.000000000000002220, 0.9238795325112844070, 1.000000000000000000, 0.9238795325112867385, 1.000000000000000000, 0.9238795325112867385, 1.000000000000000000, 0.9238795325112890700, 0.9999999999999976685 ) ) 
 REPRESENTATION_ITEM ( '' )  );
#33898=CARTESIAN_POINT ( 'NONE',  ( -7.204075437095967871, 7.204075437095967871, 78.34375000204838102 ) ) ;
#33902=VECTOR ( 'NONE', #61652, 1000.000000000000000 ) ;
#33916=CARTESIAN_POINT ( 'NONE',  ( -7.204075437095965206, -7.204075437095968759, 76.84375000204838102 ) ) ;
#33919=CARTESIAN_POINT ( 'NONE',  ( 7.778174593052023411, -7.778174593052021635, 81.06249999999998579 ) ) ;
#33939=CARTESIAN_POINT ( 'NONE',  ( 11.00000000000000000, 1.347111479062088405E-15, 118.0000000000000000 ) ) ;
#33942=CARTESIAN_POINT ( 'NONE',  ( 11.00000000000000000, 1.347111479062088405E-15, 75.24999999999998579 ) ) ;
#33945=CARTESIAN_POINT ( 'NONE',  ( 4.556349186104045934, 11.00000000000000000, 77.21875000409679046 ) ) ;
#33954=CARTESIAN_POINT ( 'NONE',  ( -4.556349186104045934, 11.00000000000000000, 98.40625000409677625 ) ) ;
#33966=CARTESIAN_POINT ( 'NONE',  ( -7.204075437095965206, -7.204075437095968759, 73.84375000204838102 ) ) ;
#33976=CARTESIAN_POINT ( 'NONE',  ( -7.204075437095965206, -7.204075437095968759, 78.71875000204836681 ) ) ;
#33977=ORIENTED_EDGE ( 'NONE', *, *, #23102, .T. ) ;
#33983=VERTEX_POINT ( 'NONE', #4823 ) ;
#33990=( BOUNDED_CURVE ( )  B_SPLINE_CURVE ( 2, ( #48117, #12321, #42458, #7772, #40999, #53430, #30045, #47383, #18723 ),
 .UNSPECIFIED., .F., .T. ) 
 B_SPLINE_CURVE_WITH_KNOTS ( ( 3, 2, 2, 2, 3 ),
 ( 0.8676470588235295489, 0.8713235294117648300, 0.8750000000000001110, 0.8786764705882353921, 0.8823529411764706731 ),
 .UNSPECIFIED. ) 
 CURVE ( )  GEOMETRIC_REPRESENTATION_ITEM ( )  RATIONAL_B_SPLINE_CURVE ( ( 0.9999999999999976685, 0.9238795325112890700, 1.000000000000000000, 0.9238795325112867385, 1.000000000000000000, 0.9238795325112867385, 1.000000000000000000, 0.9238795325112844070, 1.000000000000002220 ) ) 
 REPRESENTATION_ITEM ( '' )  );
#34005=CARTESIAN_POINT ( 'NONE',  ( -10.18810118749999916, 0.000000000000000000, 91.65625000204836681 ) ) ;
#34008=CARTESIAN_POINT ( 'NONE',  ( 7.778174593052021635, 7.778174593052023411, 108.4374999999999858 ) ) ;
#34014=CARTESIAN_POINT ( 'NONE',  ( 11.00000000000000000, 1.347111479062088405E-15, 87.43750000409677625 ) ) ;
#34024=CARTESIAN_POINT ( 'NONE',  ( -4.556349186104045934, 11.00000000000000000, 86.21874999999998579 ) ) ;
#34037=CARTESIAN_POINT ( 'NONE',  ( 7.778174593052021635, 7.778174593052023411, 95.12500000409676204 ) ) ;
#34045=VECTOR ( 'NONE', #66675, 1000.000000000000000 ) ;
#34054=ADVANCED_FACE ( 'NONE', ( #57250 ), #73841, .T. ) ;
#34060=CARTESIAN_POINT ( 'NONE',  ( 1.871523826299183495E-15, -10.18810118749999916, 99.90625000204838102 ) ) ;
#34068=CARTESIAN_POINT ( 'NONE',  ( -7.204075437095965206, -7.204075437095968759, 105.3437500020483810 ) ) ;
#34070=ORIENTED_EDGE ( 'NONE', *, *, #44390, .T. ) ;
#34076=CARTESIAN_POINT ( 'NONE',  ( 10.18810118749999916, 4.220049686691935698, 107.8750000020483668 ) ) ;
#34081=ORIENTED_EDGE ( 'NONE', *, *, #7352, .T. ) ;
#34090=ORIENTED_EDGE ( 'NONE', *, *, #22932, .T. ) ;
#34091=CARTESIAN_POINT ( 'NONE',  ( 10.18810118750000093, -4.220049686691933033, 113.3125000020483668 ) ) ;
#34111=DIRECTION ( 'NONE',  ( -1.000000000000000000, 0.000000000000000000, 0.000000000000000000 ) ) ;
#34116=CARTESIAN_POINT ( 'NONE',  ( 4.556349186104051263, -10.99999999999999822, 112.6562500040968047 ) ) ;
#34129=ORIENTED_EDGE ( 'NONE', *, *, #62692, .F. ) ;
#34131=CARTESIAN_POINT ( 'NONE',  ( 11.00000000000000000, 1.347111479062088405E-15, 118.0000000000000000 ) ) ;
#34138=CARTESIAN_POINT ( 'NONE',  ( -10.18810118749999916, 4.220049686691934809, 87.06250000204838102 ) ) ;
#34143=CARTESIAN_POINT ( 'NONE',  ( 1.871523826299183495E-15, -10.18810118749999916, 114.9062500020483810 ) ) ;
#34145=CARTESIAN_POINT ( 'NONE',  ( -11.00000000000000000, 0.000000000000000000, 109.1875000040967763 ) ) ;
#34150=CARTESIAN_POINT ( 'NONE',  ( -10.18810118749999738, -4.220049686691941915, 80.12500000204836681 ) ) ;
#34162=CARTESIAN_POINT ( 'NONE',  ( 1.871523826299183495E-15, -10.18810118749999916, 77.03125000204836681 ) ) ;
#34171=ADVANCED_FACE ( 'NONE', ( #70053 ), #12686, .T. ) ;
#34172=CARTESIAN_POINT ( 'NONE',  ( 11.00000000000010836, -4.556349186103939353, 75.34375000409674783 ) ) ;
#34190=( BOUNDED_CURVE ( )  B_SPLINE_CURVE ( 2, ( #3882, #20841, #2377, #9159, #43100, #55196, #8787, #72146, #19720 ),
 .UNSPECIFIED., .F., .F. ) 
 B_SPLINE_CURVE_WITH_KNOTS ( ( 3, 2, 2, 2, 3 ),
 ( 0.9411764705882355031, 0.9448529411764707842, 0.9485294117647060652, 0.9522058823529412352, 0.9558823529411766273 ),
 .UNSPECIFIED. ) 
 CURVE ( )  GEOMETRIC_REPRESENTATION_ITEM ( )  RATIONAL_B_SPLINE_CURVE ( ( 0.9999999999999954481, 0.9238795325112912904, 1.000000000000000000, 0.9238795325112867385, 1.000000000000000000, 0.9238795325112867385, 1.000000000000000000, 0.9238795325112844070, 1.000000000000002220 ) ) 
 REPRESENTATION_ITEM ( '' )  );
#34202=ADVANCED_FACE ( 'NONE', ( #47394 ), #35720, .T. ) ;
#34218=( BOUNDED_CURVE ( )  B_SPLINE_CURVE ( 2, ( #45106, #9670, #73033, #4377, #32690, #55699, #39446, #50757, #67001 ),
 .UNSPECIFIED., .F., .F. ) 
 B_SPLINE_CURVE_WITH_KNOTS ( ( 3, 2, 2, 2, 3 ),
 ( 0.8382352941176470784, 0.8419117647058823595, 0.8455882352941176405, 0.8492647058823529216, 0.8529411764705882026 ),
 .UNSPECIFIED. ) 
 CURVE ( )  GEOMETRIC_REPRESENTATION_ITEM ( )  RATIONAL_B_SPLINE_CURVE ( ( 1.000000000000000000, 0.9238795325112867385, 1.000000000000000000, 0.9238795325112867385, 1.000000000000000000, 0.9238795325112867385, 1.000000000000000000, 0.9238795325112867385, 1.000000000000000000 ) ) 
 REPRESENTATION_ITEM ( '' )  );
#34219=CARTESIAN_POINT ( 'NONE',  ( 10.49999999999998224, 1.316495309083403434E-15, 118.0000000000000000 ) ) ;
#34225=CARTESIAN_POINT ( 'NONE',  ( -10.68301270189220098, 0.000000000000000000, 117.8169872981077617 ) ) ;
#34226=CARTESIAN_POINT ( 'NONE',  ( 10.18810118749999916, 4.220049686691935698, 107.5000000020483668 ) ) ;
#34243=CARTESIAN_POINT ( 'NONE',  ( 10.18810118749999916, 1.247682550866122264E-15, 103.2812500020483810 ) ) ;
#34245=VERTEX_POINT ( 'NONE', #7046 ) ;
#34257=CARTESIAN_POINT ( 'NONE',  ( -7.204075437095965206, -7.204075437095968759, 97.84375000204836681 ) ) ;
#34266=CARTESIAN_POINT ( 'NONE',  ( 10.18810118749999916, 4.220049686691935698, 83.87500000204835260 ) ) ;
#34285=CARTESIAN_POINT ( 'NONE',  ( 10.18810118749999916, 1.247682550866122264E-15, 72.90625000204836681 ) ) ;
#34288=CARTESIAN_POINT ( 'NONE',  ( -4.556349186104045934, 11.00000000000000000, 83.21874999999998579 ) ) ;
#34292=AXIS2_PLACEMENT_3D ( 'NONE', #59414, #65799, #59782 ) ;
#34316=CARTESIAN_POINT ( 'NONE',  ( -7.778174593052023411, 7.778174593052023411, 77.50000000409676204 ) ) ;
#34324=( BOUNDED_CURVE ( )  B_SPLINE_CURVE ( 2, ( #72784, #28247, #50138, #4498, #22200, #16532, #21825, #39572, #32427 ),
 .UNSPECIFIED., .F., .F. ) 
 B_SPLINE_CURVE_WITH_KNOTS ( ( 3, 2, 2, 2, 3 ),
 ( 0.3382352941176469674, 0.3419117647058822484, 0.3455882352941175295, 0.3492647058823528661, 0.3529411764705882026 ),
 .UNSPECIFIED. ) 
 CURVE ( )  GEOMETRIC_REPRESENTATION_ITEM ( )  RATIONAL_B_SPLINE_CURVE ( ( 1.000000000000002220, 0.9238795325112844070, 1.000000000000000000, 0.9238795325112867385, 1.000000000000000000, 0.9238795325112867385, 1.000000000000000000, 0.9238795325112878487, 0.9999999999999988898 ) ) 
 REPRESENTATION_ITEM ( '' )  );
#34336=CARTESIAN_POINT ( 'NONE',  ( 10.18810118750000093, -4.220049686691933921, 72.81250000204836681 ) ) ;
#34343=CARTESIAN_POINT ( 'NONE',  ( 4.556349186104052151, -10.99999999999999822, 79.65625000409676204 ) ) ;
#34374=CARTESIAN_POINT ( 'NONE',  ( 10.18810118749999916, 4.220049686691935698, 94.00000000204838102 ) ) ;
#34375=FACE_OUTER_BOUND ( 'NONE', #13250, .T. ) ;
#34377=CARTESIAN_POINT ( 'NONE',  ( -11.00000000000000000, 4.556349186104045934, 101.4062500000000000 ) ) ;
#34379=CARTESIAN_POINT ( 'NONE',  ( 4.556349186104052151, -10.99999999999999822, 86.96875000000000000 ) ) ;
#34406=CARTESIAN_POINT ( 'NONE',  ( 4.556349186104045934, 11.00000000000000000, 95.21875000409679046 ) ) ;
#34419=FACE_OUTER_BOUND ( 'NONE', #64386, .T. ) ;
#34426=( NAMED_UNIT ( * ) PLANE_ANGLE_UNIT ( ) SI_UNIT ( $, .RADIAN. ) );
#34431=CARTESIAN_POINT ( 'NONE',  ( -10.18810118749999916, 0.000000000000000000, 98.03125000204838102 ) ) ;
#34440=ORIENTED_EDGE ( 'NONE', *, *, #24555, .T. ) ;
#34441=CARTESIAN_POINT ( 'NONE',  ( 7.204075437095968759, -7.204075437095966983, 107.2187500020483810 ) ) ;
#34449=CARTESIAN_POINT ( 'NONE',  ( -4.220049686691935698, 10.18810118749999916, 103.7500000020483668 ) ) ;
#34457=EDGE_CURVE ( 'NONE', #50622, #34951, #50032, .T. ) ;
#34459=DIRECTION ( 'NONE',  ( 1.000000000000000000, 0.000000000000000000, 0.000000000000000000 ) ) ;
#34465=EDGE_LOOP ( 'NONE', ( #69721, #65716, #74188, #24042 ) ) ;
#34466=CARTESIAN_POINT ( 'NONE',  ( 4.220049686691941027, -10.18810118749999738, 111.6250000020483810 ) ) ;
#34482=CARTESIAN_POINT ( 'NONE',  ( -11.00000000000000000, 4.556349186104045934, 117.9062499999999858 ) ) ;
#34494=CARTESIAN_POINT ( 'NONE',  ( 11.00000000000000355, -4.556349186104045046, 108.3437500040967763 ) ) ;
#34517=CARTESIAN_POINT ( 'NONE',  ( -7.204075437095967871, 7.204075437095967871, 85.46875000204836681 ) ) ;
#34521=CARTESIAN_POINT ( 'NONE',  ( -4.220049686691935698, 10.18810118749999916, 115.7500000020483668 ) ) ;
#34528=CARTESIAN_POINT ( 'NONE',  ( 1.871523826299183495E-15, -10.18810118749999916, 74.40625000204836681 ) ) ;
#34539=CARTESIAN_POINT ( 'NONE',  ( 4.220049686691934809, 10.18810118749999916, 68.68750000204836681 ) ) ;
#34562=VERTEX_POINT ( 'NONE', #59955 ) ;
#34569=CARTESIAN_POINT ( 'NONE',  ( -11.00000000000010658, 4.556349186103942017, 80.40624999999998579 ) ) ;
#34599=CARTESIAN_POINT ( 'NONE',  ( 10.18810118750000093, -4.220049686691933921, 102.8125000020483952 ) ) ;
#34608=ORIENTED_EDGE ( 'NONE', *, *, #16283, .T. ) ;
#34616=CARTESIAN_POINT ( 'NONE',  ( 7.204075437095966983, 7.204075437095967871, 97.46875000204838102 ) ) ;
#34630=CARTESIAN_POINT ( 'NONE',  ( 1.871523826299183495E-15, -10.18810118749999916, 87.53125000204836681 ) ) ;
#34640=CARTESIAN_POINT ( 'NONE',  ( 7.204075437095966983, 7.204075437095967871, 71.96875000204836681 ) ) ;
#34660=ORIENTED_EDGE ( 'NONE', *, *, #46613, .T. ) ;
#34661=CARTESIAN_POINT ( 'NONE',  ( -4.220049686691935698, 10.18810118749999916, 67.37500000204838102 ) ) ;
#34664=CARTESIAN_POINT ( 'NONE',  ( -7.778174593052023411, 7.778174593052023411, 83.31249999999998579 ) ) ;
#34667=CARTESIAN_POINT ( 'NONE',  ( 0.000000000000000000, 0.000000000000000000, 118.0000000000000000 ) ) ;
#34686=CARTESIAN_POINT ( 'NONE',  ( -4.556349186104045934, 11.00000000000000000, 66.90625000409677625 ) ) ;
#34688=CARTESIAN_POINT ( 'NONE',  ( -4.556349186104047710, -10.99999999999999822, 74.96875000409677625 ) ) ;
#34700=CARTESIAN_POINT ( 'NONE',  ( 10.18810118749999916, 1.247682550866122264E-15, 112.2812500020483810 ) ) ;
#34703=CARTESIAN_POINT ( 'NONE',  ( -7.204075437095967871, 7.204075437095967871, 73.46875000204838102 ) ) ;
#34738=CARTESIAN_POINT ( 'NONE',  ( 7.778174593052021635, 7.778174593052023411, 78.62500000409677625 ) ) ;
#34744=ORIENTED_EDGE ( 'NONE', *, *, #73567, .F. ) ;
#34746=CARTESIAN_POINT ( 'NONE',  ( 10.18810118750000093, -4.220049686691933033, 84.81250000204838102 ) ) ;
#34747=CYLINDRICAL_SURFACE ( 'NONE', #67082, 11.00000000000000000 ) ;
#34749=CARTESIAN_POINT ( 'NONE',  ( -7.778174593052023411, 7.778174593052023411, 101.3124999999999858 ) ) ;
#34780=CARTESIAN_POINT ( 'NONE',  ( -11.00000000000000000, 0.000000000000000000, 92.68750000409677625 ) ) ;
#34803=CARTESIAN_POINT ( 'NONE',  ( 10.18810118749999916, 4.220049686691935698, 97.37500000204839523 ) ) ;
#34809=CARTESIAN_POINT ( 'NONE',  ( -4.220049686691935698, 10.18810118749999916, 109.3750000020483810 ) ) ;
#34818=CARTESIAN_POINT ( 'NONE',  ( -4.556349186104045934, 11.00000000000000000, 96.71874999999998579 ) ) ;
#34819=CARTESIAN_POINT ( 'NONE',  ( 10.18810118749999916, 1.247682550866122264E-15, 103.2812500020483810 ) ) ;
#34827=ADVANCED_FACE ( 'NONE', ( #57297, #21452 ), #4123, .T. ) ;
#34829=ADVANCED_FACE ( 'NONE', ( #74257 ), #33180, .T. ) ;
#34835=CARTESIAN_POINT ( 'NONE',  ( 7.204075437095966983, 7.204075437095967871, 107.5937500020483810 ) ) ;
#34853=CARTESIAN_POINT ( 'NONE',  ( 4.220049686691941027, -10.18810118749999738, 70.00000000204836681 ) ) ;
#34859=CARTESIAN_POINT ( 'NONE',  ( 11.00000000000000000, 1.347111479062088405E-15, 111.4375000040967763 ) ) ;
#34865=CARTESIAN_POINT ( 'NONE',  ( -11.00000000000000000, 4.556349186104045934, 110.5937500040967905 ) ) ;
#34869=FACE_OUTER_BOUND ( 'NONE', #47436, .T. ) ;
#34878=VERTEX_POINT ( 'NONE', #67856 ) ;
#34882=CARTESIAN_POINT ( 'NONE',  ( 11.00000000000000000, 1.347111479062088405E-15, 118.0000000000000000 ) ) ;
#34886=CARTESIAN_POINT ( 'NONE',  ( 7.204075437095968759, -7.204075437095966983, 86.21875000204836681 ) ) ;
#34890=CARTESIAN_POINT ( 'NONE',  ( -7.204075437095967871, 7.204075437095967871, 117.3437500020483810 ) ) ;
#34897=CARTESIAN_POINT ( 'NONE',  ( 10.18810118749999916, 4.220049686691935698, 77.87500000204838102 ) ) ;
#34910=CARTESIAN_POINT ( 'NONE',  ( 10.18810118750000093, -4.220049686691933921, 72.81250000204836681 ) ) ;
#34925=ORIENTED_EDGE ( 'NONE', *, *, #51992, .T. ) ;
#34942=CARTESIAN_POINT ( 'NONE',  ( -7.778174593052023411, 7.778174593052023411, 80.31249999999998579 ) ) ;
#34951=VERTEX_POINT ( 'NONE', #73888 ) ;
#34972=CARTESIAN_POINT ( 'NONE',  ( 4.220049686691941027, -10.18810118749999738, 104.1250000020483810 ) ) ;
#34989=CARTESIAN_POINT ( 'NONE',  ( -4.220049686691937474, -10.18810118749999738, 95.31250000204838102 ) ) ;
#35004=CARTESIAN_POINT ( 'NONE',  ( 1.871523826299183495E-15, -10.18810118749999916, 89.03125000204836681 ) ) ;
#35013=CARTESIAN_POINT ( 'NONE',  ( -7.204075437095967871, 7.204075437095967871, 75.34375000204838102 ) ) ;
#35017=DIRECTION ( 'NONE',  ( -0.000000000000000000, -0.000000000000000000, -1.000000000000000000 ) ) ;
#35019=CARTESIAN_POINT ( 'NONE',  ( -4.556349186104048599, -10.99999999999999822, 92.96875000409676204 ) ) ;
#35029=CARTESIAN_POINT ( 'NONE',  ( 10.18810118750000093, -4.220049686691933033, 68.31250000204836681 ) ) ;
#35032=CARTESIAN_POINT ( 'NONE',  ( -6.735557395310442023E-16, 11.00000000000000000, 81.62499999999998579 ) ) ;
#35042=ADVANCED_FACE ( 'NONE', ( #63305 ), #18408, .T. ) ;
#35053=FACE_OUTER_BOUND ( 'NONE', #29296, .T. ) ;
#35059=CARTESIAN_POINT ( 'NONE',  ( 2.020667218593132706E-15, -11.00000000000000000, 69.06250000409677625 ) ) ;
#35071=CARTESIAN_POINT ( 'NONE',  ( -4.220049686691935698, 10.18810118749999916, 114.2500000020483952 ) ) ;
#35089=VECTOR ( 'NONE', #14773, 1000.000000000000000 ) ;
#35111=CARTESIAN_POINT ( 'NONE',  ( -10.18810118749999916, 0.000000000000000000, 85.65625000204838102 ) ) ;
#35113=CARTESIAN_POINT ( 'NONE',  ( -11.00000000000000000, 4.556349186104045934, 98.40625000000000000 ) ) ;
#35125=MECHANICAL_DESIGN_GEOMETRIC_PRESENTATION_REPRESENTATION('',(#71226),#61608);
#35132=CARTESIAN_POINT ( 'NONE',  ( 4.556349186104045934, 11.00000000000000000, 86.03124999999998579 ) ) ;
#35137=CARTESIAN_POINT ( 'NONE',  ( 4.556349186104045934, 11.00000000000000000, 99.53125000000000000 ) ) ;
#35140=ORIENTED_EDGE ( 'NONE', *, *, #4386, .F. ) ;
#35145=CARTESIAN_POINT ( 'NONE',  ( 4.556349186104051263, -10.99999999999999822, 84.15625000409676204 ) ) ;
#35166=CARTESIAN_POINT ( 'NONE',  ( -11.00000000000000000, 4.556349186104045934, 91.09375000409676204 ) ) ;
#35169=CARTESIAN_POINT ( 'NONE',  ( -10.18810118749999738, -4.220049686691941915, 93.62500000204838102 ) ) ;
#35175=CARTESIAN_POINT ( 'NONE',  ( -7.204075437095967871, 7.204075437095967871, 104.9687500020483810 ) ) ;
#35183=CARTESIAN_POINT ( 'NONE',  ( 10.18810118749999916, 4.220049686691935698, 103.3750000020484094 ) ) ;
#35199=CARTESIAN_POINT ( 'NONE',  ( 7.204075437095966983, 7.204075437095967871, 104.5937500020483810 ) ) ;
#35200=CARTESIAN_POINT ( 'NONE',  ( -11.00000000000000000, 0.000000000000000000, 103.0000000000000000 ) ) ;
#35217=CARTESIAN_POINT ( 'NONE',  ( 1.871523826299183495E-15, -10.18810118749999916, 69.90625000204836681 ) ) ;
#35222=CARTESIAN_POINT ( 'NONE',  ( -10.99999999999999822, -4.556349186104053040, 97.28125000409677625 ) ) ;
#35229=CARTESIAN_POINT ( 'NONE',  ( -7.778174593052023411, 7.778174593052023411, 112.0000000040967763 ) ) ;
#35245=FACE_OUTER_BOUND ( 'NONE', #58693, .T. ) ;
#35248=CARTESIAN_POINT ( 'NONE',  ( 10.18810118749999916, 1.247682550866122264E-15, 84.90625000204838102 ) ) ;
#35251=ADVANCED_FACE ( 'NONE', ( #29368 ), #58051, .T. ) ;
#35252=CARTESIAN_POINT ( 'NONE',  ( -7.204075437095967871, 7.204075437095967871, 112.8437500020483810 ) ) ;
#35255=LINE ( 'NONE', #6573, #43225 ) ;
#35262=CARTESIAN_POINT ( 'NONE',  ( 10.18810118749999916, 4.220049686691935698, 79.37500000204838102 ) ) ;
#35276=CARTESIAN_POINT ( 'NONE',  ( 10.18810118749999916, 1.247682550866122264E-15, 71.40625000204836681 ) ) ;
#35287=CARTESIAN_POINT ( 'NONE',  ( 7.778174593052023411, -7.778174593052021635, 75.25000000409676204 ) ) ;
#35299=ORIENTED_EDGE ( 'NONE', *, *, #5392, .T. ) ;
#35309=CARTESIAN_POINT ( 'NONE',  ( -6.735557395310442023E-16, 11.00000000000000000, 80.12499999999998579 ) ) ;
#35322=CARTESIAN_POINT ( 'NONE',  ( -10.99999999999989342, 4.556349186104152515, 68.59375000409677625 ) ) ;
#35325=EDGE_CURVE ( 'NONE', #9770, #69514, #54602, .T. ) ;
#35331=CARTESIAN_POINT ( 'NONE',  ( 11.00000000000000000, 1.347111479062088405E-15, 100.9375000040967763 ) ) ;
#35341=CARTESIAN_POINT ( 'NONE',  ( 4.220049686691934809, 10.18810118749999916, 100.1875000020483668 ) ) ;
#35357=CARTESIAN_POINT ( 'NONE',  ( -10.18810118749999916, 0.000000000000000000, 96.53125000204838102 ) ) ;
#35364=CARTESIAN_POINT ( 'NONE',  ( -10.18810118749999916, 4.220049686691934809, 76.93750000204839523 ) ) ;
#35368=ORIENTED_EDGE ( 'NONE', *, *, #21630, .T. ) ;
#35371=CARTESIAN_POINT ( 'NONE',  ( -7.204075437095965206, -7.204075437095968759, 87.34375000204836681 ) ) ;
#35381=CARTESIAN_POINT ( 'NONE',  ( 7.204075437095968759, -7.204075437095966983, 76.09375000204838102 ) ) ;
#35398=CARTESIAN_POINT ( 'NONE',  ( -10.18810118749999916, 0.000000000000000000, 69.15625000204836681 ) ) ;
#35401=CARTESIAN_POINT ( 'NONE',  ( -4.556349186104047710, -10.99999999999999822, 82.28124999999998579 ) ) ;
#35428=CARTESIAN_POINT ( 'NONE',  ( -4.556349186104047710, -10.99999999999999822, 70.46875000409679046 ) ) ;
#35433=( BOUNDED_CURVE ( )  B_SPLINE_CURVE ( 2, ( #16442, #43351, #74171, #37714, #60714, #56837, #2634, #60333, #14299 ),
 .UNSPECIFIED., .F., .F. ) 
 B_SPLINE_CURVE_WITH_KNOTS ( ( 3, 2, 2, 2, 3 ),
 ( 0.07352941176470592644, 0.07720588235294122137, 0.08088235294117651630, 0.08455882352941181124, 0.08823529411764710617 ),
 .UNSPECIFIED. ) 
 CURVE ( )  GEOMETRIC_REPRESENTATION_ITEM ( )  RATIONAL_B_SPLINE_CURVE ( ( 0.9999999999999991118, 0.9238795325112876267, 1.000000000000000000, 0.9238795325112867385, 1.000000000000000000, 0.9238795325112867385, 1.000000000000000000, 0.9238795325112858503, 1.000000000000000888 ) ) 
 REPRESENTATION_ITEM ( '' )  );
#35438=CARTESIAN_POINT ( 'NONE',  ( 10.18810118749999916, 4.220049686691935698, 110.8750000020483810 ) ) ;
#35473=CARTESIAN_POINT ( 'NONE',  ( 10.18810118749999916, 4.220049686691935698, 83.50000000204839523 ) ) ;
#35475=CARTESIAN_POINT ( 'NONE',  ( 2.020667218593132706E-15, -11.00000000000000000, 100.3749999999999858 ) ) ;
#35486=CIRCLE ( 'NONE', #41503, 11.00000000000000000 ) ;
#35494=CARTESIAN_POINT ( 'NONE',  ( 10.99999999999989342, 4.556349186104152515, 85.84375000000000000 ) ) ;
#35505=CARTESIAN_POINT ( 'NONE',  ( 7.778174593052021635, 7.778174593052023411, 84.62500000409677625 ) ) ;
#35521=CARTESIAN_POINT ( 'NONE',  ( -4.556349186104048599, -10.99999999999999822, 100.2812499999999858 ) ) ;
#35530=CARTESIAN_POINT ( 'NONE',  ( 10.18810118749999916, 4.220049686691935698, 92.87500000204838102 ) ) ;
#35535=CARTESIAN_POINT ( 'NONE',  ( -6.238412754330611322E-16, 10.18810118749999916, 107.7812500020483810 ) ) ;
#35545=CARTESIAN_POINT ( 'NONE',  ( 4.220049686691941027, -10.18810118749999738, 101.5000000020483810 ) ) ;
#35560=ORIENTED_EDGE ( 'NONE', *, *, #13144, .F. ) ;
#35562=CARTESIAN_POINT ( 'NONE',  ( 10.18810118749999916, 1.247682550866122264E-15, 107.4062500020483668 ) ) ;
#35570=ADVANCED_FACE ( 'NONE', ( #17196 ), #63973, .T. ) ;
#35576=CARTESIAN_POINT ( 'NONE',  ( -15.99999999999999645, -16.00000000000000355, 20.00000000000000000 ) ) ;
#35578=CARTESIAN_POINT ( 'NONE',  ( 7.778174593052021635, 7.778174593052023411, 72.62500000409677625 ) ) ;
#35579=CARTESIAN_POINT ( 'NONE',  ( 4.556349186104051263, -10.99999999999999822, 116.9687500000000142 ) ) ;
#35586=DIRECTION ( 'NONE',  ( -1.000000000000000000, -7.885106708985487801E-17, 0.000000000000000000 ) ) ;
#35590=CARTESIAN_POINT ( 'NONE',  ( -10.99999999999999822, -4.556349186104052151, 103.2812500040967763 ) ) ;
#35593=CARTESIAN_POINT ( 'NONE',  ( -4.556349186104045934, 11.00000000000000000, 95.40625000409677625 ) ) ;
#35610=CARTESIAN_POINT ( 'NONE',  ( 10.18810118750000093, -4.220049686691933921, 84.81250000204838102 ) ) ;
#35614=CARTESIAN_POINT ( 'NONE',  ( 10.18810118750000093, -4.220049686691933921, 112.1875000020483810 ) ) ;
#35621=CARTESIAN_POINT ( 'NONE',  ( 4.220049686691934809, 10.18810118749999916, 75.06250000204836681 ) ) ;
#35634=CARTESIAN_POINT ( 'NONE',  ( 7.204075437095968759, -7.204075437095966983, 74.21875000204836681 ) ) ;
#35659=ORIENTED_EDGE ( 'NONE', *, *, #16441, .F. ) ;
#35670=CARTESIAN_POINT ( 'NONE',  ( -4.556349186104048599, -10.99999999999999822, 68.96875000409677625 ) ) ;
#35693=CARTESIAN_POINT ( 'NONE',  ( 4.556349186104052151, -10.99999999999999822, 115.4687500000000000 ) ) ;
#35698=CARTESIAN_POINT ( 'NONE',  ( -10.18810118749999738, -4.220049686691941915, 100.7500000020483526 ) ) ;
#35699=DIRECTION ( 'NONE',  ( -0.000000000000000000, -0.000000000000000000, -1.000000000000000000 ) ) ;
#35716=CARTESIAN_POINT ( 'NONE',  ( -10.18810118749999916, 0.000000000000000000, 93.53125000204836681 ) ) ;
#35720=CYLINDRICAL_SURFACE ( 'NONE', #17925, 11.00000000000000000 ) ;
#35722=CARTESIAN_POINT ( 'NONE',  ( 7.204075437095966983, 7.204075437095967871, 79.46875000204836681 ) ) ;
#35727=CARTESIAN_POINT ( 'NONE',  ( 10.99999999999989342, 4.556349186104152515, 89.03125000409679046 ) ) ;
#35729=CARTESIAN_POINT ( 'NONE',  ( -10.18810118749999916, 0.000000000000000000, 91.65625000204836681 ) ) ;
#35738=CARTESIAN_POINT ( 'NONE',  ( -10.18810118749999916, 0.000000000000000000, 72.53125000204838102 ) ) ;
#35743=CARTESIAN_POINT ( 'NONE',  ( -11.00000000000007816, -4.556349186103974880, 112.0937499999999858 ) ) ;
#35757=CARTESIAN_POINT ( 'NONE',  ( -10.18810118749999916, 4.220049686691934809, 69.06250000204838102 ) ) ;
#35760=CARTESIAN_POINT ( 'NONE',  ( -4.556349186104045934, 11.00000000000000000, 80.21874999999997158 ) ) ;
#35772=EDGE_CURVE ( 'NONE', #1216, #64267, #13438, .T. ) ;
#35782=DIRECTION ( 'NONE',  ( -1.000000000000000000, 0.000000000000000000, 0.000000000000000000 ) ) ;
#35784=ORIENTED_EDGE ( 'NONE', *, *, #31352, .F. ) ;
#35788=CARTESIAN_POINT ( 'NONE',  ( 2.947434672556987323, 11.00000000000000000, 66.75185452034084221 ) ) ;
#35797=CARTESIAN_POINT ( 'NONE',  ( 4.556349186104045934, 11.00000000000000000, 108.5312500000000142 ) ) ;
#35799=CARTESIAN_POINT ( 'NONE',  ( -7.204075437095967871, 7.204075437095967871, 114.3437500020483810 ) ) ;
#35820=VECTOR ( 'NONE', #3334, 1000.000000000000000 ) ;
#35825=CARTESIAN_POINT ( 'NONE',  ( 7.778174593052023411, -7.778174593052021635, 78.25000000409676204 ) ) ;
#35838=CARTESIAN_POINT ( 'NONE',  ( -4.220049686691935698, 10.18810118749999916, 83.87500000204836681 ) ) ;
#35841=CARTESIAN_POINT ( 'NONE',  ( 4.556349186104045934, 11.00000000000000000, 102.5312500000000142 ) ) ;
#35843=CARTESIAN_POINT ( 'NONE',  ( -4.556349186104048599, -10.99999999999999822, 86.78124999999998579 ) ) ;
#35857=CARTESIAN_POINT ( 'NONE',  ( 11.00000000000000000, 1.347111479062088405E-15, 118.0000000000000000 ) ) ;
#35866=LINE ( 'NONE', #59250, #59987 ) ;
#35872=CARTESIAN_POINT ( 'NONE',  ( -7.778174593052020747, -7.778174593052023411, 86.87500000409677625 ) ) ;
#35885=( BOUNDED_CURVE ( )  B_SPLINE_CURVE ( 2, ( #17894, #58280, #1304, #57907, #40534, #11497, #46189, #5845, #18638 ),
 .UNSPECIFIED., .F., .F. ) 
 B_SPLINE_CURVE_WITH_KNOTS ( ( 3, 2, 2, 2, 3 ),
 ( 0.4264705882352941013, 0.4301470588235294379, 0.4338235294117647189, 0.4375000000000000000, 0.4411764705882352811 ),
 .UNSPECIFIED. ) 
 CURVE ( )  GEOMETRIC_REPRESENTATION_ITEM ( )  RATIONAL_B_SPLINE_CURVE ( ( 1.000000000000000000, 0.9238795325112867385, 1.000000000000000000, 0.9238795325112867385, 1.000000000000000000, 0.9238795325112867385, 1.000000000000000000, 0.9238795325112867385, 1.000000000000000000 ) ) 
 REPRESENTATION_ITEM ( '' )  );
#35897=CARTESIAN_POINT ( 'NONE',  ( 10.18810118749999916, 1.247682550866122264E-15, 91.28125000204836681 ) ) ;
#35903=CARTESIAN_POINT ( 'NONE',  ( 7.204075437095966983, 7.204075437095967871, 98.59375000204836681 ) ) ;
#35912=CARTESIAN_POINT ( 'NONE',  ( -10.18810118749999916, 4.220049686691934809, 97.93750000204836681 ) ) ;
#35918=CARTESIAN_POINT ( 'NONE',  ( 4.556349186104052151, -10.99999999999999822, 80.96874999999995737 ) ) ;
#35925=CARTESIAN_POINT ( 'NONE',  ( -4.556349186104045934, 11.00000000000000000, 84.71874999999998579 ) ) ;
#35928=ORIENTED_EDGE ( 'NONE', *, *, #64300, .T. ) ;
#35929=CARTESIAN_POINT ( 'NONE',  ( 10.18810118749999916, 1.247682550866122264E-15, 104.4062500020483810 ) ) ;
#35938=FACE_OUTER_BOUND ( 'NONE', #59373, .T. ) ;
#35944=CARTESIAN_POINT ( 'NONE',  ( 5.094039351226809842, 8.823160935565649510, 67.53052393240218976 ) ) ;
#35947=EDGE_CURVE ( 'NONE', #545, #50184, #24724, .T. ) ;
#35956=CARTESIAN_POINT ( 'NONE',  ( 11.00000000000000355, -4.556349186104045046, 105.3437500040967763 ) ) ;
#35959=CARTESIAN_POINT ( 'NONE',  ( -6.735557395310442023E-16, 11.00000000000000000, 71.12500000000000000 ) ) ;
#35962=CARTESIAN_POINT ( 'NONE',  ( -11.00000000000000000, 0.000000000000000000, 88.00000000000000000 ) ) ;
#35964=ADVANCED_FACE ( 'NONE', ( #7026 ), #65830, .T. ) ;
#35972=ORIENTED_EDGE ( 'NONE', *, *, #26071, .T. ) ;
#35974=( BOUNDED_CURVE ( )  B_SPLINE_CURVE ( 2, ( #27522, #27899, #32836, #22227, #68265, #62595, #1, #28276, #56959, #50534, #44888, #22989, #22601, #45995, #27150, #29760, #29400, #63714, #1838, #24824, #23727, #6394, #70135, #23354, #40709, #18069, #46368, #70495, #1112, #47097, #30133, #12037, #47838, #70860, #35799, #35071, #24464, #1483, #24088, #18442, #40338, #30500, #58083, #18813, #6756, #52409, #46732, #63340, #11665, #47472, #12404, #41456, #64469, #17692, #53149, #69756, #34700, #58815, #7125, #64827, #12767, #744, #41817, #13131, #36165, #59185, #57708, #7495, #53519, #6014, #29018, #35438, #52037, #69382, #41085, #64095, #373, #58448, #52774, #65935, #25933, #49329, #26306, #65186, #26691, #20274, #72344, #48576, #20657, #37280, #71960, #25563, #19909, #32370, #19171, #3694, #14242, #66686, #2574, #43674, #30868, #55012, #37656, #7863, #8976, #13861, #48949, #14989, #59547, #53886, #38027, #55385, #31238, #13498, #42916, #2198, #66311, #60273, #25194, #61027, #14617, #9351, #48207, #49713, #42174, #3318, #43296, #36536, #71586, #36904, #71215, #65564, #19535, #8600, #42553, #59912, #31614, #8228, #54635, #54264, #2944, #60654, #31991, #39516, #39880, #62145, #4441, #21772, #16104, #5558, #15364, #56874, #34243, #38400, #57245, #16479, #27069, #73096, #10097, #67440, #33135, #56131, #28560, #45171, #32751, #51198, #10468, #61780, #21403, #72727, #21031, #27432, #33499, #44799, #4075, #38777, #33874, #9729, #27814, #44055, #50825, #50447, #5190, #28187, #22142, #56501, #73464, #62882, #68182, #67065, #50083, #44425, #67812, #61403, #39140, #4818, #73836, #68551, #62514, #10840, #74209, #22512, #45534, #16854, #55759, #15738, #11215, #1396, #5934, #41737, #63256, #51566, #17610, #6674, #34616, #51953, #29315, #57622, #7042, #12326, #58369, #47017, #70049, #24382, #35357, #46280, #29678, #7409, #74584, #22898, #52694, #64011, #64747, #291, #30050, #17985, #69299, #34989, #1028, #24008, #40254, #28935, #13045, #23646, #18358, #41373, #46653, #52324, #45910, #53063, #68923, #40628, #58005, #64383, #18728, #12682, #35716, #36083, #6310, #661, #47389, #70412, #69672, #59102, #11581, #17233, #41004, #23271, #58731, #63628, #11958, #7777, #25842, #36817, #25105, #66219, #59826, #59464, #48122, #36451, #37187, #42090, #42464, #60186, #14899, #31899, #65102, #54920, #30416, #14524, #54547, #24739, #8142, #71128, #70773, #2111, #3229, #30781, #53802, #48862, #31145, #26216, #43578, #65480, #47749, #54177, #19087, #2854, #2483, #13413, #49236, #71871, #19451, #13773, #25475, #66594, #72250, #60562, #42826, #14152, #48493, #71496, #19820, #20564, #65844, #8509, #31525, #20185, #53437, #43203, #37563, #37937, #8886, #60936, #1758, #68093, #33405, #67723, #44337, #74118, #56405, #26598, #16382, #45441, #49620, #68456, #27719, #38310, #9641, #21315, #3987, #67348, #61316, #39051, #15646, #39421, #9258, #32662, #22052, #33779, #55670, #16757, #38687, #32281, #39782, #62420, #56042, #16021, #62054, #26976, #73745, #61689, #55295, #4724, #50730, #56779, #10379, #49990, #44708, #3601, #72636, #45079, #20940, #10745, #5100, #28091, #51106, #4351, #43961, #15274, #10010, #73006, #66970, #22419, #33042, #27342, #50358, #73377, #21682, #34150, #70320, #57150, #28835, #46186, #29585, #29955, #936, #35262, #52968, #69204, #11862, #41277, #563, #5466, #52598, #69579, #52231, #23918, #6579, #51475, #46927, #69952, #23546, #34897, #68826, #51854, #18261, #74488, #17890, #11127, #40905, #17138, #17515, #64287, #1301, #46558, #40531, #57904, #6212, #18635, #28467, #40163, #63537, #62785, #29218, #63913, #12225, #58635, #12593, #58277, #198, #23174, #24283, #35621, #22795, #6943, #47294, #45815, #11494, #63168, #34528, #57533, #5841, #71403, #24646, #42001, #19356, #47657, #71778, #2385, #48399, #31429, #65010, #26122, #49142, #37092, #36356, #25750, #2763, #25382, #19728, #54077, #31808, #13318, #20094, #8045, #59371, #42738, #72153, #65385, #54829, #41644, #43107, #66125, #3138, #65753, #14432, #48771, #12952, #64654, #14055, #7682, #25008, #8414, #8795, #54456, #60096, #35992, #48027, #13683, #37465, #60466, #59009, #7314, #30321, #31050, #53339, #1665, #70678, #18995, #30689, #53708, #2019, #71037, #42370, #36724, #59736, #3509, #20849, #55204, #61594, #20464, #32183, #61222, #9913 ),
 .UNSPECIFIED., .F., .F. ) 
 B_SPLINE_CURVE_WITH_KNOTS ( ( 3, 2, 2, 2, 2, 2, 2, 2, 2, 2, 2, 2, 2, 2, 2, 2, 2, 2, 2, 2, 2, 2, 2, 2, 2, 2, 2, 2, 2, 2, 2, 2, 2, 2, 2, 2, 2, 2, 2, 2, 2, 2, 2, 2, 2, 2, 2, 2, 2, 2, 2, 2, 2, 2, 2, 2, 2, 2, 2, 2, 2, 2, 2, 2, 2, 2, 2, 2, 2, 2, 2, 2, 2, 2, 2, 2, 2, 2, 2, 2, 2, 2, 2, 2, 2, 2, 2, 2, 2, 2, 2, 2, 2, 2, 2, 2, 2, 2, 2, 2, 2, 2, 2, 2, 2, 2, 2, 2, 2, 2, 2, 2, 2, 2, 2, 2, 2, 2, 2, 2, 2, 2, 2, 2, 2, 2, 2, 2, 2, 2, 2, 2, 2, 2, 2, 2, 2, 2, 2, 2, 2, 2, 2, 2, 2, 2, 2, 2, 2, 2, 2, 2, 2, 2, 2, 2, 2, 2, 2, 2, 2, 2, 2, 2, 2, 2, 2, 2, 2, 2, 2, 2, 2, 2, 2, 2, 2, 2, 2, 2, 2, 2, 2, 2, 2, 2, 2, 2, 2, 2, 2, 2, 2, 2, 2, 2, 2, 2, 2, 2, 2, 2, 2, 2, 2, 2, 2, 2, 2, 2, 2, 2, 2, 2, 2, 2, 2, 2, 2, 2, 2, 2, 2, 2, 2, 2, 2, 2, 2, 2, 2, 2, 2, 2, 2, 2, 2, 2, 2, 2, 2, 2, 2, 2, 2, 2, 2, 2, 2, 2, 2, 2, 2, 2, 2, 2, 2, 2, 2, 2, 2, 2, 2, 2, 2, 2, 2, 3 ),
 ( 0.000000000000000000, 0.003750026888355633900, 0.007500053776711267800, 0.01125008066506690170, 0.01500010755342253560, 0.01875013444177817123, 0.02250016133013380340, 0.02625018821848943557, 0.03000021510684507120, 0.03375024199520070683, 0.03750026888355634247, 0.04125029577191197117, 0.04500032266026760680, 0.04875034954862323550, 0.05250037643697887113, 0.05625040332533450677, 0.06000043021369014240, 0.06375045710204577110, 0.06750048399040141367, 0.07125051087875704237, 0.07500053776711268494, 0.07875056465546831364, 0.08250059154382394233, 0.08625061843217958490, 0.09000064532053521360, 0.09375067220889085617, 0.09750069909724647099, 0.1012507259856021136, 0.1050007528739577423, 0.1087507797623133710, 0.1125008066506690135, 0.1162508335390246422, 0.1200008604273802848, 0.1237508873157359135, 0.1275009142040915422, 0.1312509410924471709, 0.1350009679808028273, 0.1387509948691584283, 0.1425010217575140847, 0.1462510486458697134, 0.1500010755342253699, 0.1537511024225809708, 0.1575011293109366273, 0.1612511561992922560, 0.1650011830876478847, 0.1687512099760035134, 0.1725012368643591698, 0.1762512637527147985, 0.1800012906410704272, 0.1837513175294260559, 0.1875013444177817123, 0.1912513713061373133, 0.1950013981944929420, 0.1987514250828485984, 0.2025014519712042271, 0.2062514788595598558, 0.2100015057479154845, 0.2137515326362711410, 0.2175015595246267419, 0.2212515864129823984, 0.2250016133013380271, 0.2287516401896936835, 0.2325016670780492845, 0.2362516939664049409, 0.2400017208547605696, 0.2437517477431161983, 0.2475017746314718270, 0.2512518015198274557, 0.2550018284081830844, 0.2587518552965387131, 0.2625018821848943418, 0.2662519090732500260, 0.2700019359616056547, 0.2737519628499612834, 0.2775019897383168566, 0.2812520166266725408, 0.2850020435150281695, 0.2887520704033837982, 0.2925020972917394269, 0.2962521241800951111, 0.3000021510684507398, 0.3037521779568063129, 0.3075022048451619416, 0.3112522317335176258, 0.3150022586218732545, 0.3187522855102288832, 0.3225023123985845119, 0.3262523392869401406, 0.3300023661752957693, 0.3337523930636513980, 0.3375024199520070267, 0.3412524468403626554, 0.3450024737287183396, 0.3487525006170739683, 0.3525025275054295970, 0.3562525543937851702, 0.3600025812821408544, 0.3637526081704964831, 0.3675026350588521118, 0.3712526619472077405, 0.3750026888355634247, 0.3787527157239190534, 0.3825027426122746266, 0.3862527695006302553, 0.3900027963889858840, 0.3937528232773415682, 0.3975028501656971969, 0.4012528770540528256, 0.4050029039424084543, 0.4087529308307640830, 0.4125029577191197117, 0.4162529846074753404, 0.4200030114958309690, 0.4237530383841866533, 0.4275030652725422819, 0.4312530921608979106, 0.4350031190492534838, 0.4387531459376091680, 0.4425031728259647967, 0.4462531997143204254, 0.4500032266026760541, 0.4537532534910316828, 0.4575032803793873670, 0.4612533072677429402, 0.4650033341560985689, 0.4687533610444541976, 0.4725033879328098818, 0.4762534148211655105, 0.4800034417095211392, 0.4837534685978767679, 0.4875034954862323966, 0.4912535223745880253, 0.4950035492629436540, 0.4987535761512992827, 0.5025036030396549114, 0.5062536299280105956, 0.5100036568163661688, 0.5137536837047218530, 0.5175037105930774262, 0.5212537374814331104, 0.5250037643697886836, 0.5287537912581443678, 0.5325038181465000520, 0.5362538450348556252, 0.5400038719232113094, 0.5437538988115668825, 0.5475039256999225667, 0.5512539525882781399, 0.5550039794766337131, 0.5587540063649895083, 0.5625040332533450815, 0.5662540601417007657, 0.5700040870300563389, 0.5737541139184120231, 0.5775041408067675963, 0.5812541676951231695, 0.5850041945834788537, 0.5887542214718344269, 0.5925042483601902221, 0.5962542752485457953, 0.6000043021369014795, 0.6037543290252570527, 0.6075043559136126259, 0.6112543828019683101, 0.6150044096903238833, 0.6187544365786795675, 0.6225044634670352517, 0.6262544903553909359, 0.6300045172437465091, 0.6337545441321020823, 0.6375045710204577665, 0.6412545979088133397, 0.6450046247971690239, 0.6487546516855245970, 0.6525046785738802813, 0.6562547054622359655, 0.6600047323505915386, 0.6637547592389472229, 0.6675047861273027960, 0.6712548130156584802, 0.6750048399040140534, 0.6787548667923697376, 0.6825048936807253108, 0.6862549205690809950, 0.6900049474574366792, 0.6937549743457922524, 0.6975050012341479366, 0.7012550281225035098, 0.7050050550108591940, 0.7087550818992147672, 0.7125051087875703404, 0.7162551356759260246, 0.7200051625642817088, 0.7237551894526373930, 0.7275052163409929662, 0.7312552432293486504, 0.7350052701177042236, 0.7387552970060597968, 0.7425053238944154810, 0.7462553507827710542, 0.7500053776711268494, 0.7537554045594824226, 0.7575054314478381068, 0.7612554583361936800, 0.7650054852245492532, 0.7687555121129049374, 0.7725055390012605105, 0.7762555658896161948, 0.7800055927779717679, 0.7837556196663275632, 0.7875056465546831364, 0.7912556734430387095, 0.7950057003313943937, 0.7987557272197499669, 0.8025057541081056511, 0.8062557809964612243, 0.8100058078848169085, 0.8137558347731725927, 0.8175058616615281659, 0.8212558885498838501, 0.8250059154382394233, 0.8287559423265951075, 0.8325059692149506807, 0.8362559961033063649, 0.8400060229916619381, 0.8437560498800175113, 0.8475060767683733065, 0.8512561036567288797, 0.8550061305450845639, 0.8587561574334401371, 0.8625061843217958213, 0.8662562112101513945, 0.8700062380985069677, 0.8737562649868626519, 0.8775062918752183361, 0.8812563187635740203, 0.8850063456519295935, 0.8887563725402852777, 0.8925063994286408509, 0.8962564263169964240, 0.9000064532053521082, 0.9037564800937076814, 0.9075065069820633656, 0.9112565338704190498, 0.9150065607587747341, 0.9187565876471303072, 0.9225066145354858804, 0.9262566414238415646, 0.9300066683121971378, 0.9337566952005528220, 0.9375067220889083952, 0.9412567489772641904, 0.9450067758656197636, 0.9487568027539753368, 0.9525068296423310210, 0.9562568565306865942, 0.9600068834190422784, 0.9637569103073978516, 0.9675069371957535358, 0.9712569640841091090, 0.9750069909724647932, 0.9787570178608204774, 0.9825070447491760506, 0.9862570716375317348, 0.9900070985258873080, 0.9937571254142429922, 0.9975071523025985654, 1.000000000000000000 ),
 .UNSPECIFIED. ) 
 CURVE ( )  GEOMETRIC_REPRESENTATION_ITEM ( )  RATIONAL_B_SPLINE_CURVE ( ( 1.000000000000000000, 0.9238795325112867385, 1.000000000000000000, 0.9238795325112867385, 1.000000000000000000, 0.9238795325112867385, 1.000000000000000000, 0.9238795325112867385, 1.000000000000000000, 0.9238795325112867385, 1.000000000000000000, 0.9238795325112867385, 1.000000000000000000, 0.9238795325112867385, 1.000000000000000000, 0.9238795325112867385, 1.000000000000000000, 0.9238795325112867385, 1.000000000000000000, 0.9238795325112867385, 1.000000000000000000, 0.9238795325112867385, 1.000000000000000000, 0.9238795325112867385, 1.000000000000000000, 0.9238795325112867385, 1.000000000000000000, 0.9238795325112867385, 1.000000000000000000, 0.9238795325112867385, 1.000000000000000000, 0.9238795325112867385, 1.000000000000000000, 0.9238795325112867385, 1.000000000000000000, 0.9238795325112867385, 1.000000000000000000, 0.9238795325112867385, 1.000000000000000000, 0.9238795325112867385, 1.000000000000000000, 0.9238795325112867385, 1.000000000000000000, 0.9238795325112867385, 1.000000000000000000, 0.9238795325112867385, 1.000000000000000000, 0.9238795325112867385, 1.000000000000000000, 0.9238795325112867385, 1.000000000000000000, 0.9238795325112867385, 1.000000000000000000, 0.9238795325112867385, 1.000000000000000000, 0.9238795325112867385, 1.000000000000000000, 0.9238795325112867385, 1.000000000000000000, 0.9238795325112867385, 1.000000000000000000, 0.9238795325112867385, 1.000000000000000000, 0.9238795325112867385, 1.000000000000000000, 0.9238795325112867385, 1.000000000000000000, 0.9238795325112867385, 1.000000000000000000, 0.9238795325112867385, 1.000000000000000000, 0.9238795325112867385, 1.000000000000000000, 0.9238795325112867385, 1.000000000000000000, 0.9238795325112867385, 1.000000000000000000, 0.9238795325112867385, 1.000000000000000000, 0.9238795325112867385, 1.000000000000000000, 0.9238795325112867385, 1.000000000000000000, 0.9238795325112867385, 1.000000000000000000, 0.9238795325112867385, 1.000000000000000000, 0.9238795325112867385, 1.000000000000000000, 0.9238795325112867385, 1.000000000000000000, 0.9238795325112867385, 1.000000000000000000, 0.9238795325112867385, 1.000000000000000000, 0.9238795325112867385, 1.000000000000000000, 0.9238795325112867385, 1.000000000000000000, 0.9238795325112867385, 1.000000000000000000, 0.9238795325112867385, 1.000000000000000000, 0.9238795325112867385, 1.000000000000000000, 0.9238795325112867385, 1.000000000000000000, 0.9238795325112867385, 1.000000000000000000, 0.9238795325112867385, 1.000000000000000000, 0.9238795325112867385, 1.000000000000000000, 0.9238795325112867385, 1.000000000000000000, 0.9238795325112867385, 1.000000000000000000, 0.9238795325112867385, 1.000000000000000000, 0.9238795325112867385, 1.000000000000000000, 0.9238795325112867385, 1.000000000000000000, 0.9238795325112867385, 1.000000000000000000, 0.9238795325112867385, 1.000000000000000000, 0.9238795325112867385, 1.000000000000000000, 0.9238795325112867385, 1.000000000000000000, 0.9238795325112867385, 1.000000000000000000, 0.9238795325112867385, 1.000000000000000000, 0.9238795325112867385, 1.000000000000000000, 0.9238795325112867385, 1.000000000000000000, 0.9238795325112867385, 1.000000000000000000, 0.9238795325112867385, 1.000000000000000000, 0.9238795325112867385, 1.000000000000000000, 0.9238795325112867385, 1.000000000000000000, 0.9238795325112867385, 1.000000000000000000, 0.9238795325112867385, 1.000000000000000000, 0.9238795325112867385, 1.000000000000000000, 0.9238795325112867385, 1.000000000000000000, 0.9238795325112867385, 1.000000000000000000, 0.9238795325112867385, 1.000000000000000000, 0.9238795325112867385, 1.000000000000000000, 0.9238795325112867385, 1.000000000000000000, 0.9238795325112867385, 1.000000000000000000, 0.9238795325112867385, 1.000000000000000000, 0.9238795325112867385, 1.000000000000000000, 0.9238795325112867385, 1.000000000000000000, 0.9238795325112867385, 1.000000000000000000, 0.9238795325112867385, 1.000000000000000000, 0.9238795325112867385, 1.000000000000000000, 0.9238795325112867385, 1.000000000000000000, 0.9238795325112867385, 1.000000000000000000, 0.9238795325112867385, 1.000000000000000000, 0.9238795325112867385, 1.000000000000000000, 0.9238795325112867385, 1.000000000000000000, 0.9238795325112867385, 1.000000000000000000, 0.9238795325112867385, 1.000000000000000000, 0.9238795325112867385, 1.000000000000000000, 0.9238795325112867385, 1.000000000000000000, 0.9238795325112867385, 1.000000000000000000, 0.9238795325112867385, 1.000000000000000000, 0.9238795325112867385, 1.000000000000000000, 0.9238795325112867385, 1.000000000000000000, 0.9238795325112867385, 1.000000000000000000, 0.9238795325112867385, 1.000000000000000000, 0.9238795325112867385, 1.000000000000000000, 0.9238795325112867385, 1.000000000000000000, 0.9238795325112867385, 1.000000000000000000, 0.9238795325112867385, 1.000000000000000000, 0.9238795325112867385, 1.000000000000000000, 0.9238795325112867385, 1.000000000000000000, 0.9238795325112867385, 1.000000000000000000, 0.9238795325112867385, 1.000000000000000000, 0.9238795325112867385, 1.000000000000000000, 0.9238795325112867385, 1.000000000000000000, 0.9238795325112867385, 1.000000000000000000, 0.9238795325112867385, 1.000000000000000000, 0.9238795325112867385, 1.000000000000000000, 0.9238795325112867385, 1.000000000000000000, 0.9238795325112867385, 1.000000000000000000, 0.9238795325112867385, 1.000000000000000000, 0.9238795325112867385, 1.000000000000000000, 0.9238795325112867385, 1.000000000000000000, 0.9238795325112867385, 1.000000000000000000, 0.9238795325112867385, 1.000000000000000000, 0.9238795325112867385, 1.000000000000000000, 0.9238795325112867385, 1.000000000000000000, 0.9238795325112867385, 1.000000000000000000, 0.9238795325112867385, 1.000000000000000000, 0.9238795325112867385, 1.000000000000000000, 0.9238795325112867385, 1.000000000000000000, 0.9238795325112867385, 1.000000000000000000, 0.9238795325112867385, 1.000000000000000000, 0.9238795325112867385, 1.000000000000000000, 0.9238795325112867385, 1.000000000000000000, 0.9238795325112867385, 1.000000000000000000, 0.9238795325112867385, 1.000000000000000000, 0.9238795325112867385, 1.000000000000000000, 0.9238795325112867385, 1.000000000000000000, 0.9238795325112867385, 1.000000000000000000, 0.9238795325112867385, 1.000000000000000000, 0.9238795325112867385, 1.000000000000000000, 0.9238795325112867385, 1.000000000000000000, 0.9238795325112867385, 1.000000000000000000, 0.9238795325112867385, 1.000000000000000000, 0.9238795325112867385, 1.000000000000000000, 0.9238795325112867385, 1.000000000000000000, 0.9238795325112867385, 1.000000000000000000, 0.9238795325112867385, 1.000000000000000000, 0.9238795325112867385, 1.000000000000000000, 0.9238795325112867385, 1.000000000000000000, 0.9238795325112867385, 1.000000000000000000, 0.9238795325112867385, 1.000000000000000000, 0.9238795325112867385, 1.000000000000000000, 0.9238795325112867385, 1.000000000000000000, 0.9238795325112867385, 1.000000000000000000, 0.9238795325112867385, 1.000000000000000000, 0.9238795325112867385, 1.000000000000000000, 0.9238795325112867385, 1.000000000000000000, 0.9238795325112867385, 1.000000000000000000, 0.9238795325112867385, 1.000000000000000000, 0.9238795325112867385, 1.000000000000000000, 0.9238795325112867385, 1.000000000000000000, 0.9238795325112867385, 1.000000000000000000, 0.9238795325112867385, 1.000000000000000000, 0.9238795325112867385, 1.000000000000000000, 0.9238795325112867385, 1.000000000000000000, 0.9238795325112867385, 1.000000000000000000, 0.9238795325112867385, 1.000000000000000000, 0.9238795325112867385, 1.000000000000000000, 0.9238795325112867385, 1.000000000000000000, 0.9238795325112867385, 1.000000000000000000, 0.9238795325112867385, 1.000000000000000000, 0.9238795325112867385, 1.000000000000000000, 0.9238795325112867385, 1.000000000000000000, 0.9238795325112867385, 1.000000000000000000, 0.9238795325112867385, 1.000000000000000000, 0.9238795325112867385, 1.000000000000000000, 0.9238795325112867385, 1.000000000000000000, 0.9238795325112867385, 1.000000000000000000, 0.9238795325112867385, 1.000000000000000000, 0.9238795325112867385, 1.000000000000000000, 0.9238795325112867385, 1.000000000000000000, 0.9238795325112867385, 1.000000000000000000, 0.9238795325112867385, 1.000000000000000000, 0.9238795325112867385, 1.000000000000000000, 0.9238795325112867385, 1.000000000000000000, 0.9238795325112867385, 1.000000000000000000, 0.9238795325112867385, 1.000000000000000000, 0.9238795325112867385, 1.000000000000000000, 0.9238795325112867385, 1.000000000000000000, 0.9238795325112867385, 1.000000000000000000, 0.9238795325112867385, 1.000000000000000000, 0.9238795325112867385, 1.000000000000000000, 0.9238795325112867385, 1.000000000000000000, 0.9238795325112867385, 1.000000000000000000, 0.9238795325112867385, 1.000000000000000000, 0.9238795325112867385, 1.000000000000000000, 0.9238795325112867385, 1.000000000000000000, 0.9238795325112867385, 1.000000000000000000, 0.9238795325112867385, 1.000000000000000000, 0.9238795325112867385, 1.000000000000000000, 0.9238795325112867385, 1.000000000000000000, 0.9238795325112867385, 1.000000000000000000, 0.9238795325112867385, 1.000000000000000000, 0.9238795325112867385, 1.000000000000000000, 0.9238795325112867385, 1.000000000000000000, 0.9238795325112867385, 1.000000000000000000, 0.9238795325112867385, 1.000000000000000000, 0.9238795325112867385, 1.000000000000000000, 0.9238795325112867385, 1.000000000000000000, 0.9238795325112867385, 1.000000000000000000, 0.9238795325112867385, 1.000000000000000000, 0.9238795325112867385, 1.000000000000000000, 0.9238795325112867385, 1.000000000000000000, 0.9238795325112867385, 1.000000000000000000, 0.9238795325112867385, 1.000000000000000000, 0.9238795325112867385, 1.000000000000000000, 0.9238795325112867385, 1.000000000000000000, 0.9238795325112867385, 1.000000000000000000, 0.9238795325112867385, 1.000000000000000000, 0.9238795325112867385, 1.000000000000000000, 0.9238795325112867385, 1.000000000000000000, 0.9238795325112867385, 1.000000000000000000, 0.9238795325112867385, 1.000000000000000000, 0.9238795325112867385, 1.000000000000000000, 0.9238795325112867385, 1.000000000000000000, 0.9238795325112867385, 1.000000000000000000, 0.9238795325112867385, 1.000000000000000000, 0.9238795325112867385, 1.000000000000000000, 0.9238795325112867385, 1.000000000000000000, 0.9238795325112867385, 1.000000000000000000, 0.9238795325112867385, 1.000000000000000000, 0.9238795325112867385, 1.000000000000000000, 0.9238795325112867385, 1.000000000000000000, 0.9238795325112867385, 1.000000000000000000, 0.9238795325112867385, 1.000000000000000000, 0.9238795325112867385, 1.000000000000000000, 0.9238795325112867385, 1.000000000000000000, 0.9238795325112867385, 1.000000000000000000, 0.9238795325112867385, 1.000000000000000000, 0.9238795325112867385, 1.000000000000000000, 0.9238795325112867385, 1.000000000000000000, 0.9238795325112867385, 1.000000000000000000, 0.9238795325112867385, 1.000000000000000000, 0.9238795325112867385, 1.000000000000000000, 0.9238795325112867385, 1.000000000000000000, 0.9238795325112867385, 1.000000000000000000, 0.9238795325112867385, 1.000000000000000000, 0.9238795325112867385, 1.000000000000000000, 0.9238795325112867385, 1.000000000000000000, 0.9238795325112867385, 1.000000000000000000, 0.9238795325112867385, 1.000000000000000000, 0.9238795325112867385, 1.000000000000000000, 0.9238795325112867385, 1.000000000000000000, 0.9238795325112867385, 1.000000000000000000, 0.9238795325112867385, 1.000000000000000000, 0.9238795325112867385, 1.000000000000000000, 0.9238795325112867385, 1.000000000000000000, 0.9238795325112867385, 1.000000000000000000, 0.9238795325112867385, 1.000000000000000000, 0.9238795325112867385, 1.000000000000000000, 0.9238795325112867385, 1.000000000000000000, 0.9238795325112867385, 1.000000000000000000, 0.9238795325112867385, 1.000000000000000000, 0.9238795325112867385, 1.000000000000000000, 0.9238795325112867385, 1.000000000000000000, 0.9238795325112867385, 1.000000000000000000, 0.9493985675959865089, 0.9660722070829228514 ) ) 
 REPRESENTATION_ITEM ( '' )  );
#35979=CARTESIAN_POINT ( 'NONE',  ( -4.220049686691935698, 10.18810118749999916, 83.87500000204835260 ) ) ;
#35981=AXIS2_PLACEMENT_3D ( 'NONE', #16524, #73146, #39564 ) ;
#35984=CARTESIAN_POINT ( 'NONE',  ( -4.220049686691935698, 10.18810118749999916, 108.2500000020483810 ) ) ;
#35988=CYLINDRICAL_SURFACE ( 'NONE', #19553, 11.00000000000000000 ) ;
#35992=CARTESIAN_POINT ( 'NONE',  ( 4.220049686691941027, -10.18810118749999738, 70.00000000204836681 ) ) ;
#35995=FACE_OUTER_BOUND ( 'NONE', #41844, .T. ) ;
#36003=CARTESIAN_POINT ( 'NONE',  ( -4.220049686691937474, -10.18810118749999738, 73.93750000204838102 ) ) ;
#36036=CARTESIAN_POINT ( 'NONE',  ( -11.00000000000000000, 4.556349186104045934, 116.5937500040967763 ) ) ;
#36068=CARTESIAN_POINT ( 'NONE',  ( -10.18810118749999916, 4.220049686691934809, 100.5625000020483668 ) ) ;
#36076=ADVANCED_FACE ( 'NONE', ( #33028 ), #3216, .T. ) ;
#36083=CARTESIAN_POINT ( 'NONE',  ( -10.18810118749999916, 4.220049686691934809, 93.43750000204836681 ) ) ;
#36088=CARTESIAN_POINT ( 'NONE',  ( 2.020667218593132706E-15, -11.00000000000000000, 102.0625000040967763 ) ) ;
#36089=CARTESIAN_POINT ( 'NONE',  ( 7.204075437095966983, 7.204075437095967871, 76.46875000204836681 ) ) ;
#36094=EDGE_CURVE ( 'NONE', #56146, #11062, #39903, .T. ) ;
#36098=CARTESIAN_POINT ( 'NONE',  ( -6.238412754330611322E-16, 10.18810118749999916, 89.78125000204836681 ) ) ;
#36107=CARTESIAN_POINT ( 'NONE',  ( 10.18810118749999916, 4.220049686691935698, 76.37500000204838102 ) ) ;
#36123=CARTESIAN_POINT ( 'NONE',  ( 10.18810118749999916, 4.220049686691935698, 68.50000000204838102 ) ) ;
#36126=CARTESIAN_POINT ( 'NONE',  ( -11.00000000000000000, 4.556349186104045934, 75.90624999999998579 ) ) ;
#36133=CARTESIAN_POINT ( 'NONE',  ( -11.00000000000000000, 0.000000000000000000, 82.18750000409677625 ) ) ;
#36140=CARTESIAN_POINT ( 'NONE',  ( 11.00000000000000355, -4.556349186104044158, 70.65625000000000000 ) ) ;
#36154=CARTESIAN_POINT ( 'NONE',  ( -6.735557395310442023E-16, 11.00000000000000000, 71.31250000409677625 ) ) ;
#36163=CARTESIAN_POINT ( 'NONE',  ( 0.000000000000000000, 0.000000000000000000, 117.4999999999999716 ) ) ;
#36165=CARTESIAN_POINT ( 'NONE',  ( -10.18810118749999916, 0.000000000000000000, 111.5312500020483668 ) ) ;
#36185=ORIENTED_EDGE ( 'NONE', *, *, #23608, .F. ) ;
#36199=CARTESIAN_POINT ( 'NONE',  ( -4.556349186104048599, -10.99999999999999822, 98.78124999999998579 ) ) ;
#36206=CARTESIAN_POINT ( 'NONE',  ( 10.18810118749999916, 4.220049686691935698, 88.00000000204836681 ) ) ;
#36208=CARTESIAN_POINT ( 'NONE',  ( -10.99999999999999822, -4.556349186104052151, 95.59374999999998579 ) ) ;
#36218=CIRCLE ( 'NONE', #45850, 34.85072926314708042 ) ;
#36235=ORIENTED_EDGE ( 'NONE', *, *, #42516, .T. ) ;
#36239=CARTESIAN_POINT ( 'NONE',  ( -4.556349186104047710, -10.99999999999999822, 86.96875000409677625 ) ) ;
#36243=CARTESIAN_POINT ( 'NONE',  ( -15.99999999999999645, -16.00000000000000355, 20.00000000000000000 ) ) ;
#36248=EDGE_CURVE ( 'NONE', #66203, #69053, #16745, .T. ) ;
#36259=CARTESIAN_POINT ( 'NONE',  ( -7.778174593052023411, 7.778174593052023411, 92.50000000409677625 ) ) ;
#36264=CARTESIAN_POINT ( 'NONE',  ( 10.18810118749999916, 4.220049686691935698, 91.37500000204838102 ) ) ;
#36270=CARTESIAN_POINT ( 'NONE',  ( 7.204075437095968759, -7.204075437095966983, 104.2187500020483810 ) ) ;
#36279=CARTESIAN_POINT ( 'NONE',  ( -10.18810118749999916, 4.220049686691934809, 100.9375000020483810 ) ) ;
#36296=CARTESIAN_POINT ( 'NONE',  ( 10.18810118749999916, 4.220049686691935698, 103.0000000020483668 ) ) ;
#36307=CARTESIAN_POINT ( 'NONE',  ( 0.000000000000000000, 0.000000000000000000, 41.99999999999999289 ) ) ;
#36314=CARTESIAN_POINT ( 'NONE',  ( 4.556349186104051263, -10.99999999999999822, 115.4687500000000000 ) ) ;
#36319=DIRECTION ( 'NONE',  ( -0.000000000000000000, -0.000000000000000000, -1.000000000000000000 ) ) ;
#36327=CARTESIAN_POINT ( 'NONE',  ( -10.99999999999999822, -4.556349186104052151, 104.7812500040967763 ) ) ;
#36330=CARTESIAN_POINT ( 'NONE',  ( 7.778174593052021635, 7.778174593052023411, 70.93749999999998579 ) ) ;
#36331=CARTESIAN_POINT ( 'NONE',  ( -7.778174593052020747, -7.778174593052023411, 107.6874999999999858 ) ) ;
#36338=CARTESIAN_POINT ( 'NONE',  ( 11.00000000000000000, 1.347111479062088405E-15, 87.25000000000000000 ) ) ;
#36343=FACE_OUTER_BOUND ( 'NONE', #27335, .T. ) ;
#36348=CARTESIAN_POINT ( 'NONE',  ( 7.204075437095966983, 7.204075437095967871, 112.4687500020483810 ) ) ;
#36356=CARTESIAN_POINT ( 'NONE',  ( 1.871523826299183495E-15, -10.18810118749999916, 72.90625000204836681 ) ) ;
#36359=FACE_OUTER_BOUND ( 'NONE', #53380, .T. ) ;
#36367=CARTESIAN_POINT ( 'NONE',  ( 2.729893485599593106, 10.18810118750000093, 67.22060438569887708 ) ) ;
#36393=VERTEX_POINT ( 'NONE', #54065 ) ;
#36425=CARTESIAN_POINT ( 'NONE',  ( -11.00000000000000000, 0.000000000000000000, 111.9999999999999858 ) ) ;
#36429=CARTESIAN_POINT ( 'NONE',  ( 7.778174593052023411, -7.778174593052021635, 115.5625000000000000 ) ) ;
#36433=VERTEX_POINT ( 'NONE', #47646 ) ;
#36435=CARTESIAN_POINT ( 'NONE',  ( 1.871523826299183495E-15, -10.18810118749999916, 95.03125000204836681 ) ) ;
#36443=ORIENTED_EDGE ( 'NONE', *, *, #70336, .F. ) ;
#36451=CARTESIAN_POINT ( 'NONE',  ( 10.18810118749999916, 4.220049686691935698, 91.37500000204838102 ) ) ;
#36456=CARTESIAN_POINT ( 'NONE',  ( 7.778174593052023411, -7.778174593052021635, 102.2500000040967763 ) ) ;
#36457=CARTESIAN_POINT ( 'NONE',  ( 10.18810118749999916, 1.247682550866122264E-15, 73.28125000204838102 ) ) ;
#36463=CARTESIAN_POINT ( 'NONE',  ( 4.220049686691934809, 10.18810118749999916, 80.68750000204836681 ) ) ;
#36474=CARTESIAN_POINT ( 'NONE',  ( 4.220049686691934809, 10.18810118749999916, 69.06250000204839523 ) ) ;
#36495=CARTESIAN_POINT ( 'NONE',  ( 7.778174593052023411, -7.778174593052021635, 76.56249999999997158 ) ) ;
#36501=CARTESIAN_POINT ( 'NONE',  ( -11.00000000000000000, 0.000000000000000000, 118.0000000000000000 ) ) ;
#36508=CARTESIAN_POINT ( 'NONE',  ( 11.00000000000000000, 1.347111479062088405E-15, 115.9375000040967763 ) ) ;
#36524=CARTESIAN_POINT ( 'NONE',  ( 4.220049686691934809, 10.18810118749999916, 84.06250000204838102 ) ) ;
#36525=CARTESIAN_POINT ( 'NONE',  ( 7.778174593052021635, 7.778174593052023411, 71.12500000409677625 ) ) ;
#36536=CARTESIAN_POINT ( 'NONE',  ( -10.18810118749999738, -4.220049686691941915, 105.6250000020483668 ) ) ;
#36552=EDGE_CURVE ( 'NONE', #67207, #47217, #19718, .T. ) ;
#36572=CARTESIAN_POINT ( 'NONE',  ( -4.220049686691935698, 10.18810118749999916, 79.37500000204838102 ) ) ;
#36574=CARTESIAN_POINT ( 'NONE',  ( 2.020667218593132706E-15, -11.00000000000000000, 97.37499999999998579 ) ) ;
#36583=CARTESIAN_POINT ( 'NONE',  ( 5.398500733969330945, 9.350505071208255359, 67.88208643086591110 ) ) ;
#36591=FACE_OUTER_BOUND ( 'NONE', #11575, .T. ) ;
#36595=DIRECTION ( 'NONE',  ( -0.000000000000000000, -0.000000000000000000, -1.000000000000000000 ) ) ;
#36602=ORIENTED_EDGE ( 'NONE', *, *, #47285, .T. ) ;
#36606=CARTESIAN_POINT ( 'NONE',  ( 11.00000000000000000, 4.556349186104045934, 84.53125000409677625 ) ) ;
#36633=CARTESIAN_POINT ( 'NONE',  ( -4.220049686691937474, -10.18810118749999738, 89.31250000204838102 ) ) ;
#36634=ORIENTED_EDGE ( 'NONE', *, *, #33167, .T. ) ;
#36638=CARTESIAN_POINT ( 'NONE',  ( -10.18810118749999916, 0.000000000000000000, 103.6562500020483810 ) ) ;
#36640=ORIENTED_EDGE ( 'NONE', *, *, #14377, .T. ) ;
#36647=CARTESIAN_POINT ( 'NONE',  ( -10.18810118749999738, -4.220049686691941915, 98.12500000204836681 ) ) ;
#36660=CARTESIAN_POINT ( 'NONE',  ( -11.00000000000000000, 0.000000000000000000, 84.99999999999998579 ) ) ;
#36661=CIRCLE ( 'NONE', #13745, 38.34805510287551300 ) ;
#36664=EDGE_LOOP ( 'NONE', ( #8205, #22136, #60753, #39617 ) ) ;
#36665=CARTESIAN_POINT ( 'NONE',  ( -4.220049686691937474, -10.18810118749999738, 103.9375000020483810 ) ) ;
#36682=CARTESIAN_POINT ( 'NONE',  ( 4.556349186104045934, 11.00000000000000000, 111.5312500000000142 ) ) ;
#36695=CARTESIAN_POINT ( 'NONE',  ( -4.556349186104045934, 11.00000000000000000, 102.9062500040967905 ) ) ;
#36699=CARTESIAN_POINT ( 'NONE',  ( 7.778174593052021635, 7.778174593052023411, 71.12500000409677625 ) ) ;
#36711=DIRECTION ( 'NONE',  ( 2.168404344971008868E-16, -1.000000000000000000, 0.000000000000000000 ) ) ;
#36716=CARTESIAN_POINT ( 'NONE',  ( -4.220049686691937474, -10.18810118749999738, 110.3125000020483810 ) ) ;
#36717=ORIENTED_EDGE ( 'NONE', *, *, #65730, .F. ) ;
#36724=CARTESIAN_POINT ( 'NONE',  ( -4.220049686691937474, -10.18810118749999738, 68.31250000204836681 ) ) ;
#36726=ORIENTED_EDGE ( 'NONE', *, *, #42517, .F. ) ;
#36739=CARTESIAN_POINT ( 'NONE',  ( -10.18810118749999916, 4.220049686691934809, 114.4375000020483668 ) ) ;
#36751=ORIENTED_EDGE ( 'NONE', *, *, #21008, .T. ) ;
#36754=CARTESIAN_POINT ( 'NONE',  ( 2.020667218593132706E-15, -11.00000000000000000, 84.06250000409676204 ) ) ;
#36768=CARTESIAN_POINT ( 'NONE',  ( 7.778174593052023411, -7.778174593052021635, 94.56250000000000000 ) ) ;
#36776=CARTESIAN_POINT ( 'NONE',  ( 10.99999999999989342, 4.556349186104152515, 75.53125000409677625 ) ) ;
#36795=ORIENTED_EDGE ( 'NONE', *, *, #44530, .F. ) ;
#36801=CARTESIAN_POINT ( 'NONE',  ( 4.627539443576518252, 9.975780150077198982, 117.5133370941326945 ) ) ;
#36802=CARTESIAN_POINT ( 'NONE',  ( -6.238412754330611322E-16, 10.18810118749999916, 92.78125000204836681 ) ) ;
#36810=VERTEX_POINT ( 'NONE', #9905 ) ;
#36817=CARTESIAN_POINT ( 'NONE',  ( -10.18810118749999916, 4.220049686691934809, 91.93750000204836681 ) ) ;
#36820=CARTESIAN_POINT ( 'NONE',  ( 11.00000000000000000, 1.347111479062088405E-15, 115.9375000040967763 ) ) ;
#36823=CARTESIAN_POINT ( 'NONE',  ( 10.18810118750000093, -4.220049686691933921, 74.68750000204836681 ) ) ;
#36832=CARTESIAN_POINT ( 'NONE',  ( -4.220049686691937474, -10.18810118749999738, 85.93750000204839523 ) ) ;
#36845=CARTESIAN_POINT ( 'NONE',  ( -7.204075437095967871, 7.204075437095967871, 69.34375000204836681 ) ) ;
#36860=VERTEX_POINT ( 'NONE', #31798 ) ;
#36865=CARTESIAN_POINT ( 'NONE',  ( 7.778174593052021635, 7.778174593052023411, 78.43750000000000000 ) ) ;
#36889=CARTESIAN_POINT ( 'NONE',  ( 4.220049686691941027, -10.18810118749999738, 89.50000000204836681 ) ) ;
#36890=CARTESIAN_POINT ( 'NONE',  ( 1.871523826299183495E-15, -10.18810118749999916, 111.5312500020483668 ) ) ;
#36904=CARTESIAN_POINT ( 'NONE',  ( -10.18810118749999916, 4.220049686691934809, 105.4375000020483810 ) ) ;
#36929=DIRECTION ( 'NONE',  ( -0.000000000000000000, -0.000000000000000000, -1.000000000000000000 ) ) ;
#36936=CIRCLE ( 'NONE', #9271, 10.49999999999998224 ) ;
#36940=ORIENTED_EDGE ( 'NONE', *, *, #55808, .F. ) ;
#36941=CARTESIAN_POINT ( 'NONE',  ( -4.220049686691937474, -10.18810118749999738, 79.93750000204838102 ) ) ;
#36944=CARTESIAN_POINT ( 'NONE',  ( 2.020667218593132706E-15, -11.00000000000000000, 94.37499999999998579 ) ) ;
#36958=LINE ( 'NONE', #35857, #20904 ) ;
#36973=CARTESIAN_POINT ( 'NONE',  ( 4.556349186104045934, 11.00000000000000000, 78.71875000409677625 ) ) ;
#36998=CARTESIAN_POINT ( 'NONE',  ( -7.204075437095965206, -7.204075437095968759, 83.21875000204836681 ) ) ;
#37005=CARTESIAN_POINT ( 'NONE',  ( 10.18810118750000093, -4.220049686691933921, 99.81250000204838102 ) ) ;
#37014=CARTESIAN_POINT ( 'NONE',  ( 4.220049686691941027, -10.18810118749999738, 97.00000000204836681 ) ) ;
#37029=EDGE_LOOP ( 'NONE', ( #21308, #42109, #16137, #12559 ) ) ;
#37030=CARTESIAN_POINT ( 'NONE',  ( 10.18810118750000093, -4.220049686691933033, 96.81250000204838102 ) ) ;
#37047=CARTESIAN_POINT ( 'NONE',  ( 11.00000000000000000, 1.347111479062088405E-15, 112.7499999999999858 ) ) ;
#37061=CARTESIAN_POINT ( 'NONE',  ( -10.99999999999999822, -4.556349186104052151, 106.2812500040967620 ) ) ;
#37085=CARTESIAN_POINT ( 'NONE',  ( 4.220049686691934809, 10.18810118749999916, 108.0625000020483810 ) ) ;
#37087=ADVANCED_FACE ( 'NONE', ( #23448 ), #58912, .T. ) ;
#37089=CARTESIAN_POINT ( 'NONE',  ( -4.556349186104048599, -10.99999999999999822, 109.4687500040967763 ) ) ;
#37092=CARTESIAN_POINT ( 'NONE',  ( 4.220049686691941027, -10.18810118749999738, 73.00000000204836681 ) ) ;
#37103=EDGE_CURVE ( 'NONE', #47406, #38757, #68018, .T. ) ;
#37106=CARTESIAN_POINT ( 'NONE',  ( -10.18810118749999916, 0.000000000000000000, 114.5312500020483810 ) ) ;
#37130=VERTEX_POINT ( 'NONE', #43010 ) ;
#37135=CARTESIAN_POINT ( 'NONE',  ( 11.00000000000000000, 1.347111479062088405E-15, 118.0000000000000000 ) ) ;
#37153=( BOUNDED_CURVE ( )  B_SPLINE_CURVE ( 2, ( #60152, #19786, #25810, #9224, #21278, #44301, #42794, #67317, #49583 ),
 .UNSPECIFIED., .F., .F. ) 
 B_SPLINE_CURVE_WITH_KNOTS ( ( 3, 2, 2, 2, 3 ),
 ( 0.7647058823529411242, 0.7683823529411765163, 0.7720588235294116863, 0.7757352941176469674, 0.7794117647058822484 ),
 .UNSPECIFIED. ) 
 CURVE ( )  GEOMETRIC_REPRESENTATION_ITEM ( )  RATIONAL_B_SPLINE_CURVE ( ( 1.000000000000000000, 0.9238795325112867385, 1.000000000000000000, 0.9238795325112867385, 1.000000000000000000, 0.9238795325112867385, 1.000000000000000000, 0.9238795325112890700, 0.9999999999999976685 ) ) 
 REPRESENTATION_ITEM ( '' )  );
#37162=CARTESIAN_POINT ( 'NONE',  ( 4.556349186104052151, -10.99999999999999822, 105.1562500040967763 ) ) ;
#37170=DIRECTION ( 'NONE',  ( -0.000000000000000000, -0.000000000000000000, -1.000000000000000000 ) ) ;
#37171=CARTESIAN_POINT ( 'NONE',  ( 7.204075437095966983, 7.204075437095967871, 94.09375000204838102 ) ) ;
#37172=CARTESIAN_POINT ( 'NONE',  ( -7.778174593052023411, 7.778174593052023411, 86.50000000409677625 ) ) ;
#37187=CARTESIAN_POINT ( 'NONE',  ( 10.18810118749999916, 1.247682550866122264E-15, 91.28125000204836681 ) ) ;
#37193=CARTESIAN_POINT ( 'NONE',  ( -10.18810118749999916, 4.220049686691934809, 73.93750000204838102 ) ) ;
#37200=CARTESIAN_POINT ( 'NONE',  ( 4.220049686691941027, -10.18810118749999738, 84.62500000204838102 ) ) ;
#37214=ORIENTED_EDGE ( 'NONE', *, *, #62081, .T. ) ;
#37225=VERTEX_POINT ( 'NONE', #49046 ) ;
#37236=CARTESIAN_POINT ( 'NONE',  ( -7.778174593052023411, 7.778174593052023411, 75.81249999999997158 ) ) ;
#37247=CARTESIAN_POINT ( 'NONE',  ( -11.00000000000000000, 4.556349186104045934, 115.0937500040967905 ) ) ;
#37250=CARTESIAN_POINT ( 'NONE',  ( -11.00000000000000000, 0.000000000000000000, 118.0000000000000000 ) ) ;
#37257=EDGE_LOOP ( 'NONE', ( #25437, #69385, #27254, #11406 ) ) ;
#37265=CARTESIAN_POINT ( 'NONE',  ( 10.18810118749999916, 4.220049686691935698, 86.87500000204836681 ) ) ;
#37267=CARTESIAN_POINT ( 'NONE',  ( -7.204075437095967871, 7.204075437095967871, 112.4687500020483810 ) ) ;
#37270=CARTESIAN_POINT ( 'NONE',  ( -11.00000000000000000, 0.000000000000000000, 118.0000000000000000 ) ) ;
#37280=CARTESIAN_POINT ( 'NONE',  ( 10.18810118750000093, -4.220049686691933033, 109.1875000020483810 ) ) ;
#37295=ORIENTED_EDGE ( 'NONE', *, *, #65929, .F. ) ;
#37302=CARTESIAN_POINT ( 'NONE',  ( -11.00000000000000000, 0.000000000000000000, 77.68750000409677625 ) ) ;
#37316=CARTESIAN_POINT ( 'NONE',  ( -10.18810118749999916, 4.220049686691934809, 82.56250000204836681 ) ) ;
#37319=CARTESIAN_POINT ( 'NONE',  ( 11.00000000000000000, 4.556349186104045934, 94.84374999999998579 ) ) ;
#37344=CARTESIAN_POINT ( 'NONE',  ( -11.00000000000000000, 0.000000000000000000, 70.18750000409676204 ) ) ;
#37346=CARTESIAN_POINT ( 'NONE',  ( 11.00000000000000000, 1.347111479062088405E-15, 82.93750000409677625 ) ) ;
#37357=EDGE_LOOP ( 'NONE', ( #14369, #45640, #52794, #67843 ) ) ;
#37363=CARTESIAN_POINT ( 'NONE',  ( 4.220049686691941027, -10.18810118749999738, 75.62500000204838102 ) ) ;
#37365=CARTESIAN_POINT ( 'NONE',  ( -4.556349186104045934, 11.00000000000000000, 92.40625000409677625 ) ) ;
#37371=CARTESIAN_POINT ( 'NONE',  ( -10.18810118749999916, 4.220049686691934809, 82.93750000204838102 ) ) ;
#37376=CARTESIAN_POINT ( 'NONE',  ( 10.18810118749999916, 4.220049686691935698, 103.0000000020483668 ) ) ;
#37385=CARTESIAN_POINT ( 'NONE',  ( -4.220049686691935698, 10.18810118749999916, 99.25000000204838102 ) ) ;
#37388=DIRECTION ( 'NONE',  ( -1.000000000000000000, 0.000000000000000000, 0.000000000000000000 ) ) ;
#37403=CARTESIAN_POINT ( 'NONE',  ( -7.204075437095967871, 7.204075437095967871, 95.96875000204838102 ) ) ;
#37411=AXIS2_PLACEMENT_3D ( 'NONE', #66117, #32176, #3502 ) ;
#37412=EDGE_CURVE ( 'NONE', #23833, #24773, #29033, .T. ) ;
#37425=CARTESIAN_POINT ( 'NONE',  ( 11.00000000000000000, 1.347111479062088405E-15, 111.2499999999999858 ) ) ;
#37431=DIRECTION ( 'NONE',  ( -0.000000000000000000, -0.000000000000000000, -1.000000000000000000 ) ) ;
#37436=CARTESIAN_POINT ( 'NONE',  ( 11.00000000000000000, 4.556349186104045934, 99.53125000409679046 ) ) ;
#37460=CARTESIAN_POINT ( 'NONE',  ( -4.220049686691937474, -10.18810118749999738, 104.3125000020483810 ) ) ;
#37465=CARTESIAN_POINT ( 'NONE',  ( -7.204075437095965206, -7.204075437095968759, 69.71875000204836681 ) ) ;
#37468=CARTESIAN_POINT ( 'NONE',  ( -6.238412754330611322E-16, 10.18810118749999916, 116.7812500020483810 ) ) ;
#37479=CARTESIAN_POINT ( 'NONE',  ( -7.204075437095967871, 7.204075437095967871, 114.3437500020483810 ) ) ;
#37495=( BOUNDED_CURVE ( )  B_SPLINE_CURVE ( 2, ( #57583, #68510, #51910, #250, #69259, #57961, #6269, #56832, #5152 ),
 .UNSPECIFIED., .F., .F. ) 
 B_SPLINE_CURVE_WITH_KNOTS ( ( 3, 2, 2, 2, 3 ),
 ( 0.6176470588235292158, 0.6213235294117644969, 0.6249999999999997780, 0.6286764705882351700, 0.6323529411764704511 ),
 .UNSPECIFIED. ) 
 CURVE ( )  GEOMETRIC_REPRESENTATION_ITEM ( )  RATIONAL_B_SPLINE_CURVE ( ( 1.000000000000004663, 0.9238795325112821866, 1.000000000000000000, 0.9238795325112867385, 1.000000000000000000, 0.9238795325112867385, 1.000000000000000000, 0.9238795325112890700, 0.9999999999999976685 ) ) 
 REPRESENTATION_ITEM ( '' )  );
#37497=CARTESIAN_POINT ( 'NONE',  ( -7.204075437095965206, -7.204075437095968759, 114.3437500020483810 ) ) ;
#37549=CARTESIAN_POINT ( 'NONE',  ( -7.204075437095967871, 7.204075437095967871, 97.46875000204838102 ) ) ;
#37554=CARTESIAN_POINT ( 'NONE',  ( 7.778174593052023411, -7.778174593052021635, 96.06250000000000000 ) ) ;
#37557=CARTESIAN_POINT ( 'NONE',  ( -11.00000000000000000, 0.000000000000000000, 118.0000000000000000 ) ) ;
#37563=CARTESIAN_POINT ( 'NONE',  ( 7.204075437095968759, -7.204075437095966983, 86.59375000204836681 ) ) ;
#37577=CARTESIAN_POINT ( 'NONE',  ( -6.238412754330611322E-16, 10.18810118749999916, 83.78125000204836681 ) ) ;
#37590=CARTESIAN_POINT ( 'NONE',  ( 7.778174593052023411, -7.778174593052021635, 76.56249999999997158 ) ) ;
#37612=CARTESIAN_POINT ( 'NONE',  ( -7.778174593052023411, 7.778174593052023411, 71.31249999999998579 ) ) ;
#37616=ORIENTED_EDGE ( 'NONE', *, *, #26003, .F. ) ;
#37619=CARTESIAN_POINT ( 'NONE',  ( 11.00000000000000000, 1.347111479062088405E-15, 114.4375000040967763 ) ) ;
#37642=CARTESIAN_POINT ( 'NONE',  ( 10.18810118749999916, 1.247682550866122264E-15, 88.28125000204836681 ) ) ;
#37643=CARTESIAN_POINT ( 'NONE',  ( 1.871523826299183495E-15, -10.18810118749999916, 114.5312500020483810 ) ) ;
#37652=DIRECTION ( 'NONE',  ( 1.000000000000000000, 0.000000000000000000, 0.000000000000000000 ) ) ;
#37656=CARTESIAN_POINT ( 'NONE',  ( 7.204075437095966983, 7.204075437095967871, 107.9687500020483810 ) ) ;
#37682=CARTESIAN_POINT ( 'NONE',  ( 4.556349186104052151, -10.99999999999999822, 78.15625000409677625 ) ) ;
#37695=CARTESIAN_POINT ( 'NONE',  ( -10.18810118749999916, 0.000000000000000000, 81.15625000204838102 ) ) ;
#37698=CARTESIAN_POINT ( 'NONE',  ( -6.735557395310442023E-16, 11.00000000000000000, 95.12499999999998579 ) ) ;
#37712=DIRECTION ( 'NONE',  ( -0.000000000000000000, -0.000000000000000000, -1.000000000000000000 ) ) ;
#37714=CARTESIAN_POINT ( 'NONE',  ( 4.556349186104052151, -10.99999999999999822, 112.6562500040967905 ) ) ;
#37727=CARTESIAN_POINT ( 'NONE',  ( -7.778174593052023411, 7.778174593052023411, 80.50000000409676204 ) ) ;
#37744=CARTESIAN_POINT ( 'NONE',  ( -7.204075437095967871, 7.204075437095967871, 77.96875000204836681 ) ) ;
#37752=CARTESIAN_POINT ( 'NONE',  ( -10.18810118749999916, 4.220049686691934809, 84.43750000204838102 ) ) ;
#37759=CARTESIAN_POINT ( 'NONE',  ( 10.18810118749999916, 1.247682550866122264E-15, 95.40625000204836681 ) ) ;
#37763=ORIENTED_EDGE ( 'NONE', *, *, #19184, .T. ) ;
#37768=CARTESIAN_POINT ( 'NONE',  ( -4.220049686691935698, 10.18810118749999916, 94.75000000204838102 ) ) ;
#37785=CARTESIAN_POINT ( 'NONE',  ( 1.871523826299183495E-15, -10.18810118749999916, 99.53125000204838102 ) ) ;
#37796=DIRECTION ( 'NONE',  ( -0.000000000000000000, -0.000000000000000000, -1.000000000000000000 ) ) ;
#37803=CARTESIAN_POINT ( 'NONE',  ( 2.020667218593132706E-15, -11.00000000000000000, 115.3749999999999858 ) ) ;
#37813=( BOUNDED_CURVE ( )  B_SPLINE_CURVE ( 2, ( #73168, #4146, #67877, #16168, #39209, #62578, #12754, #52394, #12391 ),
 .UNSPECIFIED., .F., .F. ) 
 B_SPLINE_CURVE_WITH_KNOTS ( ( 3, 2, 2, 2, 3 ),
 ( 0.6911764705882351700, 0.6948529411764704511, 0.6985294117647057321, 0.7022058823529410132, 0.7058823529411764053 ),
 .UNSPECIFIED. ) 
 CURVE ( )  GEOMETRIC_REPRESENTATION_ITEM ( )  RATIONAL_B_SPLINE_CURVE ( ( 1.000000000000002220, 0.9238795325112844070, 1.000000000000000000, 0.9238795325112867385, 1.000000000000000000, 0.9238795325112867385, 1.000000000000000000, 0.9238795325112890700, 0.9999999999999976685 ) ) 
 REPRESENTATION_ITEM ( '' )  );
#37817=CARTESIAN_POINT ( 'NONE',  ( 11.00000000000000355, -4.556349186104045046, 99.34375000409677625 ) ) ;
#37828=CARTESIAN_POINT ( 'NONE',  ( 11.00000000000000000, 1.347111479062088405E-15, 91.93750000409677625 ) ) ;
#37838=CARTESIAN_POINT ( 'NONE',  ( -7.778174593052020747, -7.778174593052023411, 70.37500000409677625 ) ) ;
#37839=CARTESIAN_POINT ( 'NONE',  ( 7.204075437095966983, 7.204075437095967871, 101.9687500020483668 ) ) ;
#37851=CARTESIAN_POINT ( 'NONE',  ( -6.238412754330611322E-16, 10.18810118749999916, 110.7812500020483668 ) ) ;
#37860=CARTESIAN_POINT ( 'NONE',  ( -10.18810118749999916, 4.220049686691934809, 67.56250000204836681 ) ) ;
#37861=VECTOR ( 'NONE', #4847, 1000.000000000000000 ) ;
#37884=ORIENTED_EDGE ( 'NONE', *, *, #70375, .T. ) ;
#37923=CARTESIAN_POINT ( 'NONE',  ( 4.220049686691934809, 10.18810118749999916, 94.18750000204836681 ) ) ;
#37937=CARTESIAN_POINT ( 'NONE',  ( 4.220049686691941027, -10.18810118749999738, 86.50000000204836681 ) ) ;
#37953=CARTESIAN_POINT ( 'NONE',  ( -10.18810118749999916, 0.000000000000000000, 81.15625000204838102 ) ) ;
#37956=CARTESIAN_POINT ( 'NONE',  ( 11.00000000000000000, 1.347111479062088405E-15, 100.9375000040967763 ) ) ;
#37958=ORIENTED_EDGE ( 'NONE', *, *, #67087, .T. ) ;
#37983=CARTESIAN_POINT ( 'NONE',  ( -10.99999999999999822, 0.000000000000000000, 114.9999999999999858 ) ) ;
#37987=CARTESIAN_POINT ( 'NONE',  ( -4.556349186104045934, 11.00000000000000000, 71.21875000000000000 ) ) ;
#37998=CARTESIAN_POINT ( 'NONE',  ( 0.000000000000000000, 0.000000000000000000, 118.0000000000000000 ) ) ;
#38006=CARTESIAN_POINT ( 'NONE',  ( 11.00000000000000000, 1.347111479062088405E-15, 87.43750000409677625 ) ) ;
#38012=CARTESIAN_POINT ( 'NONE',  ( -4.220049686691935698, 10.18810118749999916, 87.25000000204838102 ) ) ;
#38013=CARTESIAN_POINT ( 'NONE',  ( -10.18810118749999916, 0.000000000000000000, 114.1562500020483810 ) ) ;
#38027=CARTESIAN_POINT ( 'NONE',  ( -7.204075437095965206, -7.204075437095968759, 107.2187500020483810 ) ) ;
#38037=CARTESIAN_POINT ( 'NONE',  ( -4.556349186104048599, -10.99999999999999822, 71.96875000409677625 ) ) ;
#38054=ORIENTED_EDGE ( 'NONE', *, *, #69616, .F. ) ;
#38069=CARTESIAN_POINT ( 'NONE',  ( 4.220049686691941027, -10.18810118749999738, 80.12500000204836681 ) ) ;
#38072=CARTESIAN_POINT ( 'NONE',  ( -4.556349186104045934, 11.00000000000000000, 89.21874999999998579 ) ) ;
#38076=CARTESIAN_POINT ( 'NONE',  ( 11.00000000000000000, 1.347111479062088405E-15, 88.75000000000000000 ) ) ;
#38099=CARTESIAN_POINT ( 'NONE',  ( -11.00000000000000000, 4.556349186104045934, 82.09375000409676204 ) ) ;
#38115=CYLINDRICAL_SURFACE ( 'NONE', #63306, 11.00000000000000000 ) ;
#38116=CARTESIAN_POINT ( 'NONE',  ( 7.204075437095966983, 7.204075437095967871, 76.09375000204838102 ) ) ;
#38124=CARTESIAN_POINT ( 'NONE',  ( -10.18810118749999916, 4.220049686691934809, 85.93750000204839523 ) ) ;
#38127=CARTESIAN_POINT ( 'NONE',  ( -7.778174593052023411, 7.778174593052023411, 105.8124999999999858 ) ) ;
#38129=CARTESIAN_POINT ( 'NONE',  ( -7.204075437095967871, 7.204075437095967871, 95.96875000204838102 ) ) ;
#38136=CARTESIAN_POINT ( 'NONE',  ( 10.18810118750000093, -4.220049686691933921, 94.18750000204836681 ) ) ;
#38151=EDGE_LOOP ( 'NONE', ( #35368, #49975, #31810, #2780 ) ) ;
#38153=( BOUNDED_CURVE ( )  B_SPLINE_CURVE ( 2, ( #58242, #24242, #40119, #63499, #45776, #52932, #68788, #35222, #57864 ),
 .UNSPECIFIED., .F., .F. ) 
 B_SPLINE_CURVE_WITH_KNOTS ( ( 3, 2, 2, 2, 3 ),
 ( 0.3676470588235293824, 0.3713235294117646634, 0.3750000000000000000, 0.3786764705882352811, 0.3823529411764705621 ),
 .UNSPECIFIED. ) 
 CURVE ( )  GEOMETRIC_REPRESENTATION_ITEM ( )  RATIONAL_B_SPLINE_CURVE ( ( 1.000000000000001110, 0.9238795325112856283, 1.000000000000000000, 0.9238795325112867385, 1.000000000000000000, 0.9238795325112867385, 1.000000000000000000, 0.9238795325112867385, 1.000000000000000000 ) ) 
 REPRESENTATION_ITEM ( '' )  );
#38155=CARTESIAN_POINT ( 'NONE',  ( 7.204075437095968759, -7.204075437095966983, 99.71875000204838102 ) ) ;
#38158=CARTESIAN_POINT ( 'NONE',  ( 11.00000000000000355, -4.556349186104045046, 109.6562500000000000 ) ) ;
#38167=FACE_OUTER_BOUND ( 'NONE', #63302, .T. ) ;
#38172=CARTESIAN_POINT ( 'NONE',  ( -10.99999999999991829, 4.556349186104124982, 111.9062499999999858 ) ) ;
#38183=CARTESIAN_POINT ( 'NONE',  ( 0.000000000000000000, 0.000000000000000000, 118.0000000000000000 ) ) ;
#38184=CARTESIAN_POINT ( 'NONE',  ( 1.734723475976807489E-15, -16.00000000000000355, 38.34805510287551300 ) ) ;
#38185=ORIENTED_EDGE ( 'NONE', *, *, #8384, .F. ) ;
#38188=CARTESIAN_POINT ( 'NONE',  ( 11.00000000000000000, 1.347111479062088405E-15, 99.43750000409677625 ) ) ;
#38211=CARTESIAN_POINT ( 'NONE',  ( -10.18810118749999738, -4.220049686691941915, 105.6250000020483668 ) ) ;
#38212=ORIENTED_EDGE ( 'NONE', *, *, #25808, .F. ) ;
#38220=CARTESIAN_POINT ( 'NONE',  ( -7.204075437095965206, -7.204075437095968759, 115.8437500020483810 ) ) ;
#38223=VECTOR ( 'NONE', #21196, 1000.000000000000000 ) ;
#38229=CARTESIAN_POINT ( 'NONE',  ( -4.220049686691937474, -10.18810118749999738, 111.8125000020484094 ) ) ;
#38234=ORIENTED_EDGE ( 'NONE', *, *, #26499, .T. ) ;
#38242=EDGE_CURVE ( 'NONE', #10672, #3255, #32161, .T. ) ;
#38244=CARTESIAN_POINT ( 'NONE',  ( 4.220049686691941027, -10.18810118749999738, 114.6250000020483810 ) ) ;
#38255=EDGE_CURVE ( 'NONE', #20942, #48097, #36936, .T. ) ;
#38259=CARTESIAN_POINT ( 'NONE',  ( -4.556349186104048599, -10.99999999999999822, 77.78125000000001421 ) ) ;
#38260=CARTESIAN_POINT ( 'NONE',  ( 2.020667218593132706E-15, -11.00000000000000000, 94.37499999999998579 ) ) ;
#38271=CARTESIAN_POINT ( 'NONE',  ( -15.99999999999999645, 15.99999999999999645, 20.00000000000000000 ) ) ;
#38279=( BOUNDED_CURVE ( )  B_SPLINE_CURVE ( 2, ( #41882, #47534, #64893, #443, #58513, #35137, #69454, #70200, #12831 ),
 .UNSPECIFIED., .F., .F. ) 
 B_SPLINE_CURVE_WITH_KNOTS ( ( 3, 2, 2, 2, 3 ),
 ( 0.3529411764705882026, 0.3566176470588234837, 0.3602941176470587648, 0.3639705882352940458, 0.3676470588235293824 ),
 .UNSPECIFIED. ) 
 CURVE ( )  GEOMETRIC_REPRESENTATION_ITEM ( )  RATIONAL_B_SPLINE_CURVE ( ( 1.000000000000001110, 0.9238795325112856283, 1.000000000000000000, 0.9238795325112867385, 1.000000000000000000, 0.9238795325112867385, 1.000000000000000000, 0.9238795325112878487, 0.9999999999999988898 ) ) 
 REPRESENTATION_ITEM ( '' )  );
#38287=EDGE_LOOP ( 'NONE', ( #28814, #70137, #34070, #57884 ) ) ;
#38290=CARTESIAN_POINT ( 'NONE',  ( -7.778174593052020747, -7.778174593052023411, 82.18750000000000000 ) ) ;
#38295=CARTESIAN_POINT ( 'NONE',  ( -10.18810118749999916, 0.000000000000000000, 90.15625000204838102 ) ) ;
#38304=LINE ( 'NONE', #37557, #65984 ) ;
#38310=CARTESIAN_POINT ( 'NONE',  ( 4.220049686691941027, -10.18810118749999738, 85.00000000204838102 ) ) ;
#38315=CARTESIAN_POINT ( 'NONE',  ( -11.00000000000000533, 11.00000000000000000, 41.99999999999999289 ) ) ;
#38323=CARTESIAN_POINT ( 'NONE',  ( 10.18810118749999916, 4.220049686691935698, 77.50000000204839523 ) ) ;
#38355=CARTESIAN_POINT ( 'NONE',  ( 7.778174593052023411, -7.778174593052021635, 69.06249999999998579 ) ) ;
#38363=CARTESIAN_POINT ( 'NONE',  ( 10.99999999999998046, -4.556349186104063698, 114.3437500040967763 ) ) ;
#38376=ORIENTED_EDGE ( 'NONE', *, *, #56977, .T. ) ;
#38385=CARTESIAN_POINT ( 'NONE',  ( -6.238412754330611322E-16, 10.18810118749999916, 113.7812500020483810 ) ) ;
#38400=CARTESIAN_POINT ( 'NONE',  ( 10.18810118750000093, -4.220049686691933033, 103.1875000020483810 ) ) ;
#38412=ORIENTED_EDGE ( 'NONE', *, *, #44070, .T. ) ;
#38416=CARTESIAN_POINT ( 'NONE',  ( 11.00000000000000000, 1.347111479062088405E-15, 118.0000000000000000 ) ) ;
#38421=CARTESIAN_POINT ( 'NONE',  ( -4.220049686691937474, -10.18810118749999738, 78.81250000204838102 ) ) ;
#38441=CARTESIAN_POINT ( 'NONE',  ( 10.18810118750000093, -4.220049686691933033, 75.81250000204838102 ) ) ;
#38444=CARTESIAN_POINT ( 'NONE',  ( -6.735557395310442023E-16, 11.00000000000000000, 89.12499999999998579 ) ) ;
#38472=CARTESIAN_POINT ( 'NONE',  ( 7.778174593052023411, -7.778174593052021635, 82.75000000409676204 ) ) ;
#38488=CARTESIAN_POINT ( 'NONE',  ( 11.00000000000000000, 1.347111479062088405E-15, 102.2500000000000000 ) ) ;
#38489=CARTESIAN_POINT ( 'NONE',  ( 4.220049686691934809, 10.18810118749999916, 79.18750000204836681 ) ) ;
#38499=CARTESIAN_POINT ( 'NONE',  ( -7.204075437095967871, 7.204075437095967871, 87.34375000204836681 ) ) ;
#38502=EDGE_CURVE ( 'NONE', #23833, #9171, #72360, .T. ) ;
#38506=CARTESIAN_POINT ( 'NONE',  ( 4.220049686691941027, -10.18810118749999738, 95.12500000204836681 ) ) ;
#38514=CARTESIAN_POINT ( 'NONE',  ( 10.18810118750000093, -4.220049686691933921, 91.18750000204836681 ) ) ;
#38525=B_SPLINE_CURVE_WITH_KNOTS ( 'NONE', 1,
 ( #9006, #15394 ),
 .UNSPECIFIED., .F., .F.,
 ( 2, 2 ),
 ( 0.000000000000000000, 0.6095729009237784712 ),
 .UNSPECIFIED. ) ;
#38532=CARTESIAN_POINT ( 'NONE',  ( -4.220049686691935698, 10.18810118749999916, 100.3750000020483952 ) ) ;
#38535=CARTESIAN_POINT ( 'NONE',  ( 4.556349186104051263, -10.99999999999999822, 107.9687500000000142 ) ) ;
#38568=CARTESIAN_POINT ( 'NONE',  ( 2.020667218593132706E-15, -11.00000000000000000, 96.06250000409677625 ) ) ;
#38569=CARTESIAN_POINT ( 'NONE',  ( 0.000000000000000000, 0.000000000000000000, 128.5000000000001990 ) ) ;
#38588=CARTESIAN_POINT ( 'NONE',  ( -7.204075437095965206, -7.204075437095968759, 105.7187500020483810 ) ) ;
#38595=CARTESIAN_POINT ( 'NONE',  ( 5.499989586027935751, 9.526285454130809072, 66.68677389048282578 ) ) ;
#38598=CARTESIAN_POINT ( 'NONE',  ( 4.220049686691941027, -10.18810118749999738, 114.6250000020483810 ) ) ;
#38603=CARTESIAN_POINT ( 'NONE',  ( 0.000000000000000000, 0.000000000000000000, 118.0000000000000000 ) ) ;
#38605=CARTESIAN_POINT ( 'NONE',  ( -7.204075437095965206, -7.204075437095968759, 110.2187500020483810 ) ) ;
#38607=( BOUNDED_CURVE ( )  B_SPLINE_CURVE ( 2, ( #4177, #15093, #38127, #49810, #27164, #50181, #73201, #21508, #18084 ),
 .UNSPECIFIED., .F., .F. ) 
 B_SPLINE_CURVE_WITH_KNOTS ( ( 3, 2, 2, 2, 3 ),
 ( 0.2352941176470587092, 0.2389705882352940181, 0.2426470588235292991, 0.2463235294117646079, 0.2499999999999998890 ),
 .UNSPECIFIED. ) 
 CURVE ( )  GEOMETRIC_REPRESENTATION_ITEM ( )  RATIONAL_B_SPLINE_CURVE ( ( 1.000000000000002220, 0.9238795325112844070, 1.000000000000000000, 0.9238795325112867385, 1.000000000000000000, 0.9238795325112867385, 1.000000000000000000, 0.9238795325112890700, 0.9999999999999976685 ) ) 
 REPRESENTATION_ITEM ( '' )  );
#38613=ORIENTED_EDGE ( 'NONE', *, *, #67533, .F. ) ;
#38617=CARTESIAN_POINT ( 'NONE',  ( -6.238412754330611322E-16, 10.18810118749999916, 70.65625000204836681 ) ) ;
#38625=CARTESIAN_POINT ( 'NONE',  ( -7.204075437095967871, 7.204075437095967871, 113.9687500020483810 ) ) ;
#38636=CARTESIAN_POINT ( 'NONE',  ( -6.735557395310442023E-16, 11.00000000000000000, 87.81250000409676204 ) ) ;
#38638=CARTESIAN_POINT ( 'NONE',  ( -11.00000000000000000, 0.000000000000000000, 92.68750000409677625 ) ) ;
#38643=CARTESIAN_POINT ( 'NONE',  ( 7.778174593052023411, -7.778174593052021635, 111.0625000000000000 ) ) ;
#38648=CARTESIAN_POINT ( 'NONE',  ( 4.556349186104052151, -10.99999999999999822, 82.65625000409676204 ) ) ;
#38654=DIRECTION ( 'NONE',  ( -0.000000000000000000, -0.000000000000000000, -1.000000000000000000 ) ) ;
#38656=CARTESIAN_POINT ( 'NONE',  ( -7.778174593052020747, -7.778174593052023411, 79.18750000000000000 ) ) ;
#38674=CARTESIAN_POINT ( 'NONE',  ( -10.18810118749999738, -4.220049686691941915, 90.25000000204838102 ) ) ;
#38682=CARTESIAN_POINT ( 'NONE',  ( -4.556349186104045934, 11.00000000000000000, 77.21875000000000000 ) ) ;
#38687=CARTESIAN_POINT ( 'NONE',  ( 7.204075437095968759, -7.204075437095966983, 83.59375000204838102 ) ) ;
#38702=CARTESIAN_POINT ( 'NONE',  ( 10.18810118750000093, -4.220049686691933921, 78.81250000204838102 ) ) ;
#38715=ORIENTED_EDGE ( 'NONE', *, *, #42007, .F. ) ;
#38740=CARTESIAN_POINT ( 'NONE',  ( -7.778174593052023411, 7.778174593052023411, 72.81249999999998579 ) ) ;
#38750=CARTESIAN_POINT ( 'NONE',  ( -11.00000000000000000, 0.000000000000000000, 116.4999999999999858 ) ) ;
#38757=VERTEX_POINT ( 'NONE', #70974 ) ;
#38760=CARTESIAN_POINT ( 'NONE',  ( 11.00000000000000000, 1.347111479062088405E-15, 72.43750000409676204 ) ) ;
#38766=CARTESIAN_POINT ( 'NONE',  ( 1.871523826299183495E-15, -10.18810118749999916, 105.5312500020483810 ) ) ;
#38777=CARTESIAN_POINT ( 'NONE',  ( -10.18810118749999738, -4.220049686691941915, 101.1250000020483810 ) ) ;
#38785=CARTESIAN_POINT ( 'NONE',  ( 4.556349186104052151, -10.99999999999999822, 72.15625000409677625 ) ) ;
#38796=CARTESIAN_POINT ( 'NONE',  ( -4.220049686691937474, -10.18810118749999738, 83.31250000204836681 ) ) ;
#38811=ORIENTED_EDGE ( 'NONE', *, *, #20434, .F. ) ;
#38814=ORIENTED_EDGE ( 'NONE', *, *, #40236, .F. ) ;
#38815=( BOUNDED_CURVE ( )  B_SPLINE_CURVE ( 2, ( #47809, #36140, #59161, #55355, #46155, #40502, #57118, #9322, #9700 ),
 .UNSPECIFIED., .F., .F. ) 
 B_SPLINE_CURVE_WITH_KNOTS ( ( 3, 2, 2, 2, 3 ),
 ( 0.9264705882352941568, 0.9301470588235294379, 0.9338235294117648300, 0.9375000000000002220, 0.9411764705882355031 ),
 .UNSPECIFIED. ) 
 CURVE ( )  GEOMETRIC_REPRESENTATION_ITEM ( )  RATIONAL_B_SPLINE_CURVE ( ( 1.000000000000000000, 0.9238795325112867385, 1.000000000000000000, 0.9238795325112867385, 1.000000000000000000, 0.9238795325112867385, 1.000000000000000000, 0.9238795325112821866, 1.000000000000004663 ) ) 
 REPRESENTATION_ITEM ( '' )  );
#38817=CARTESIAN_POINT ( 'NONE',  ( -4.220049686691937474, -10.18810118749999738, 72.43750000204838102 ) ) ;
#38819=CARTESIAN_POINT ( 'NONE',  ( -11.00000000000000000, 4.556349186104045934, 90.90625000000000000 ) ) ;
#38822=CARTESIAN_POINT ( 'NONE',  ( -6.735557395310442023E-16, 11.00000000000000000, 89.12499999999998579 ) ) ;
#38845=CARTESIAN_POINT ( 'NONE',  ( -7.778174593052023411, 7.778174593052023411, 73.00000000409677625 ) ) ;
#38854=AXIS2_PLACEMENT_3D ( 'NONE', #58087, #71219, #42178 ) ;
#38859=ORIENTED_EDGE ( 'NONE', *, *, #6951, .T. ) ;
#38861=CARTESIAN_POINT ( 'NONE',  ( -10.18810118749999916, 4.220049686691934809, 79.56250000204836681 ) ) ;
#38866=CARTESIAN_POINT ( 'NONE',  ( 11.00000000000010836, -4.556349186103939353, 79.84375000409677625 ) ) ;
#38869=CARTESIAN_POINT ( 'NONE',  ( 4.220049686691934809, 10.18810118749999916, 82.56250000204836681 ) ) ;
#38881=CARTESIAN_POINT ( 'NONE',  ( -10.18810118749999916, 0.000000000000000000, 93.53125000204836681 ) ) ;
#38898=CARTESIAN_POINT ( 'NONE',  ( 10.18810118750000093, -4.220049686691933033, 90.81250000204838102 ) ) ;
#38901=CARTESIAN_POINT ( 'NONE',  ( -4.556349186104045934, 11.00000000000000000, 110.2187499999999858 ) ) ;
#38924=CARTESIAN_POINT ( 'NONE',  ( 0.000000000000000000, 0.000000000000000000, 118.0000000000000000 ) ) ;
#38925=CYLINDRICAL_SURFACE ( 'NONE', #29508, 11.00000000000000000 ) ;
#38926=CARTESIAN_POINT ( 'NONE',  ( 4.556349186104052151, -10.99999999999999822, 88.46874999999998579 ) ) ;
#38931=CARTESIAN_POINT ( 'NONE',  ( -4.556349186104045934, 11.00000000000000000, 90.90625000409677625 ) ) ;
#38952=CARTESIAN_POINT ( 'NONE',  ( -6.238412754330611322E-16, 10.18810118749999916, 105.1562500020483810 ) ) ;
#38961=CARTESIAN_POINT ( 'NONE',  ( 4.220049686691934809, 10.18810118749999916, 112.1875000020483810 ) ) ;
#38968=CARTESIAN_POINT ( 'NONE',  ( -4.556349186104048599, -10.99999999999999822, 103.4687500040967763 ) ) ;
#38969=CARTESIAN_POINT ( 'NONE',  ( 10.18810118749999916, 1.247682550866122264E-15, 109.2812500020483668 ) ) ;
#38977=CARTESIAN_POINT ( 'NONE',  ( -10.18810118749999916, 4.220049686691934809, 70.93750000204838102 ) ) ;
#38988=CARTESIAN_POINT ( 'NONE',  ( 4.220049686691934809, 10.18810118749999916, 109.1875000020483810 ) ) ;
#38989=CARTESIAN_POINT ( 'NONE',  ( 11.00000000000000000, 1.347111479062088405E-15, 103.7500000000000000 ) ) ;
#38998=EDGE_CURVE ( 'NONE', #39166, #72729, #31443, .T. ) ;
#39005=CARTESIAN_POINT ( 'NONE',  ( -6.735557395310442023E-16, 11.00000000000000000, 107.3125000040967905 ) ) ;
#39039=CARTESIAN_POINT ( 'NONE',  ( 7.204075437095968759, -7.204075437095966983, 87.71875000204836681 ) ) ;
#39051=CARTESIAN_POINT ( 'NONE',  ( -10.18810118749999916, 4.220049686691934809, 84.43750000204838102 ) ) ;
#39059=CYLINDRICAL_SURFACE ( 'NONE', #7159, 11.00000000000000000 ) ;
#39066=CARTESIAN_POINT ( 'NONE',  ( 7.204075437095966983, 7.204075437095967871, 79.09375000204838102 ) ) ;
#39101=CARTESIAN_POINT ( 'NONE',  ( 4.556349186104045934, 11.00000000000000000, 74.03125000000000000 ) ) ;
#39125=CARTESIAN_POINT ( 'NONE',  ( 1.871523826299183495E-15, -10.18810118749999916, 108.5312500020483810 ) ) ;
#39140=CARTESIAN_POINT ( 'NONE',  ( -7.204075437095967871, 7.204075437095967871, 99.34375000204836681 ) ) ;
#39151=ORIENTED_EDGE ( 'NONE', *, *, #14729, .T. ) ;
#39157=ORIENTED_EDGE ( 'NONE', *, *, #53175, .F. ) ;
#39161=CARTESIAN_POINT ( 'NONE',  ( 7.204075437095966983, 7.204075437095967871, 79.46875000204836681 ) ) ;
#39166=VERTEX_POINT ( 'NONE', #52072 ) ;
#39178=CARTESIAN_POINT ( 'NONE',  ( -10.18810118749999738, -4.220049686691941915, 75.25000000204836681 ) ) ;
#39181=CARTESIAN_POINT ( 'NONE',  ( 4.556349186104051263, -10.99999999999999822, 86.96874999999998579 ) ) ;
#39206=CARTESIAN_POINT ( 'NONE',  ( 11.00000000000000000, 1.347111479062088405E-15, 72.24999999999998579 ) ) ;
#39209=CARTESIAN_POINT ( 'NONE',  ( 2.020667218593132706E-15, -11.00000000000000000, 81.06250000409677625 ) ) ;
#39213=CARTESIAN_POINT ( 'NONE',  ( 4.556349186104051263, -10.99999999999999822, 75.15625000409677625 ) ) ;
#39229=CARTESIAN_POINT ( 'NONE',  ( 16.00000000000000711, 16.00000000000000355, 7.387219678533750056 ) ) ;
#39230=CARTESIAN_POINT ( 'NONE',  ( 1.871523826299183495E-15, -10.18810118749999916, 69.53125000204838102 ) ) ;
#39240=CARTESIAN_POINT ( 'NONE',  ( -10.18810118749999738, -4.220049686691941915, 80.12500000204835260 ) ) ;
#39251=CARTESIAN_POINT ( 'NONE',  ( -10.18810118749999916, 0.000000000000000000, 92.03125000204836681 ) ) ;
#39268=CARTESIAN_POINT ( 'NONE',  ( -6.238412754330611322E-16, 10.18810118749999916, 92.78125000204836681 ) ) ;
#39271=CARTESIAN_POINT ( 'NONE',  ( -11.00000000000000000, 0.000000000000000000, 106.0000000000000000 ) ) ;
#39278=CARTESIAN_POINT ( 'NONE',  ( 4.556349186104052151, -10.99999999999999822, 87.15625000409676204 ) ) ;
#39296=DIRECTION ( 'NONE',  ( -0.000000000000000000, -0.000000000000000000, -1.000000000000000000 ) ) ;
#39301=EDGE_CURVE ( 'NONE', #28981, #74545, #31296, .T. ) ;
#39304=CARTESIAN_POINT ( 'NONE',  ( 4.556349186104051263, -10.99999999999999822, 91.65625000409679046 ) ) ;
#39318=DIRECTION ( 'NONE',  ( -0.000000000000000000, -0.000000000000000000, -1.000000000000000000 ) ) ;
#39326=CARTESIAN_POINT ( 'NONE',  ( 1.871523826299183495E-15, -10.18810118749999916, 96.90625000204838102 ) ) ;
#39334=CARTESIAN_POINT ( 'NONE',  ( -10.18810118749999916, 0.000000000000000000, 111.1562500020483668 ) ) ;
#39339=CARTESIAN_POINT ( 'NONE',  ( -4.556349186104048599, -10.99999999999999822, 76.46875000409677625 ) ) ;
#39341=CARTESIAN_POINT ( 'NONE',  ( -6.238412754330611322E-16, 10.18810118749999916, 108.1562500020483668 ) ) ;
#39344=CARTESIAN_POINT ( 'NONE',  ( -11.00000000000000000, 0.000000000000000000, 117.3437500020483810 ) ) ;
#39349=LINE ( 'NONE', #68759, #68208 ) ;
#39356=CARTESIAN_POINT ( 'NONE',  ( 10.18810118750000093, -4.220049686691933033, 111.8125000020483810 ) ) ;
#39357=CARTESIAN_POINT ( 'NONE',  ( -7.778174593052023411, 7.778174593052023411, 97.00000000409677625 ) ) ;
#39374=CARTESIAN_POINT ( 'NONE',  ( 11.00000000000000000, 1.347111479062088405E-15, 73.93750000409676204 ) ) ;
#39385=CARTESIAN_POINT ( 'NONE',  ( 7.778174593052021635, 7.778174593052023411, 113.1250000040967763 ) ) ;
#39397=VERTEX_POINT ( 'NONE', #48239 ) ;
#39406=CARTESIAN_POINT ( 'NONE',  ( -7.204075437095967871, 7.204075437095967871, 86.96875000204836681 ) ) ;
#39413=CARTESIAN_POINT ( 'NONE',  ( -6.238412754330611322E-16, 10.18810118749999916, 115.6562500020483810 ) ) ;
#39421=CARTESIAN_POINT ( 'NONE',  ( -4.220049686691935698, 10.18810118749999916, 84.25000000204838102 ) ) ;
#39432=CARTESIAN_POINT ( 'NONE',  ( -4.220049686691937474, -10.18810118749999738, 75.43750000204836681 ) ) ;
#39446=CARTESIAN_POINT ( 'NONE',  ( -7.778174593052020747, -7.778174593052023411, 73.37500000409677625 ) ) ;
#39456=VECTOR ( 'NONE', #27762, 1000.000000000000000 ) ;
#39470=CARTESIAN_POINT ( 'NONE',  ( -7.778174593052023411, 7.778174593052023411, 107.3124999999999858 ) ) ;
#39478=VECTOR ( 'NONE', #2443, 1000.000000000000000 ) ;
#39499=CARTESIAN_POINT ( 'NONE',  ( -4.220049686691935698, 10.18810118749999916, 106.3750000020483668 ) ) ;
#39508=ORIENTED_EDGE ( 'NONE', *, *, #10691, .F. ) ;
#39516=CARTESIAN_POINT ( 'NONE',  ( -10.18810118749999738, -4.220049686691941915, 104.1250000020483810 ) ) ;
#39538=CARTESIAN_POINT ( 'NONE',  ( 4.220049686691941027, -10.18810118749999738, 79.00000000204838102 ) ) ;
#39557=CARTESIAN_POINT ( 'NONE',  ( -6.238412754330611322E-16, 10.18810118749999916, 73.28125000204838102 ) ) ;
#39560=CARTESIAN_POINT ( 'NONE',  ( -4.556349186104045934, 11.00000000000000000, 87.71874999999997158 ) ) ;
#39564=DIRECTION ( 'NONE',  ( 1.000000000000000000, 0.000000000000000000, -0.000000000000000000 ) ) ;
#39569=VECTOR ( 'NONE', #36595, 1000.000000000000000 ) ;
#39572=CARTESIAN_POINT ( 'NONE',  ( -10.99999999999994671, -4.556349186104105442, 98.78125000409679046 ) ) ;
#39582=CARTESIAN_POINT ( 'NONE',  ( 4.556349186104045934, 11.00000000000000000, 80.21875000409680467 ) ) ;
#39585=CARTESIAN_POINT ( 'NONE',  ( 7.778174593052023411, -7.778174593052021635, 75.25000000409676204 ) ) ;
#39602=CARTESIAN_POINT ( 'NONE',  ( 4.220049686691941027, -10.18810118749999738, 72.62500000204836681 ) ) ;
#39611=CARTESIAN_POINT ( 'NONE',  ( 10.18810118749999916, 4.220049686691935698, 79.37500000204838102 ) ) ;
#39617=ORIENTED_EDGE ( 'NONE', *, *, #36248, .F. ) ;
#39640=CARTESIAN_POINT ( 'NONE',  ( 4.220049686691941027, -10.18810118749999738, 93.62500000204838102 ) ) ;
#39643=CARTESIAN_POINT ( 'NONE',  ( -11.00000000000000000, 4.556349186104045934, 108.9062500000000000 ) ) ;
#39645=DIRECTION ( 'NONE',  ( -0.000000000000000000, -0.000000000000000000, -1.000000000000000000 ) ) ;
#39670=CARTESIAN_POINT ( 'NONE',  ( 4.556349186104051263, -10.99999999999999822, 90.15625000409677625 ) ) ;
#39690=CARTESIAN_POINT ( 'NONE',  ( -7.204075437095967871, 7.204075437095967871, 99.34375000204836681 ) ) ;
#39699=CARTESIAN_POINT ( 'NONE',  ( 7.204075437095966983, 7.204075437095967871, 106.0937500020483810 ) ) ;
#39707=CARTESIAN_POINT ( 'NONE',  ( 10.18810118749999916, 1.247682550866122264E-15, 110.7812500020483668 ) ) ;
#39724=CARTESIAN_POINT ( 'NONE',  ( -4.220049686691935698, 10.18810118749999916, 112.3750000020483810 ) ) ;
#39748=CARTESIAN_POINT ( 'NONE',  ( 4.556349186104051263, -10.99999999999999822, 111.1562500040967620 ) ) ;
#39750=DIRECTION ( 'NONE',  ( -1.000000000000000000, 0.000000000000000000, 0.000000000000000000 ) ) ;
#39761=ORIENTED_EDGE ( 'NONE', *, *, #36552, .T. ) ;
#39769=CARTESIAN_POINT ( 'NONE',  ( 1.871523826299183495E-15, -10.18810118749999916, 87.53125000204836681 ) ) ;
#39777=CARTESIAN_POINT ( 'NONE',  ( 11.00000000000000000, 1.347111479062088405E-15, 118.0000000000000000 ) ) ;
#39782=CARTESIAN_POINT ( 'NONE',  ( 1.871523826299183495E-15, -10.18810118749999916, 83.40625000204838102 ) ) ;
#39796=CARTESIAN_POINT ( 'NONE',  ( -7.204075437095967871, 7.204075437095967871, 76.46875000204836681 ) ) ;
#39803=AXIS2_PLACEMENT_3D ( 'NONE', #51330, #10976, #11344 ) ;
#39852=DIRECTION ( 'NONE',  ( -1.000000000000000000, 0.000000000000000000, 0.000000000000000000 ) ) ;
#39864=CARTESIAN_POINT ( 'NONE',  ( 7.204075437095966983, 7.204075437095967871, 107.5937500020483810 ) ) ;
#39873=VERTEX_POINT ( 'NONE', #1338 ) ;
#39880=CARTESIAN_POINT ( 'NONE',  ( -10.18810118749999916, 0.000000000000000000, 104.0312500020483810 ) ) ;
#39891=CARTESIAN_POINT ( 'NONE',  ( 1.871523826299183495E-15, -10.18810118749999916, 93.53125000204836681 ) ) ;
#39896=CIRCLE ( 'NONE', #59196, 11.00000000000000000 ) ;
#39902=CARTESIAN_POINT ( 'NONE',  ( -10.18810118749999916, 4.220049686691934809, 82.93750000204838102 ) ) ;
#39903=( BOUNDED_CURVE ( )  B_SPLINE_CURVE ( 2, ( #43564, #72995, #43190, #26204, #61677, #14511, #50346, #26962, #21302 ),
 .UNSPECIFIED., .F., .F. ) 
 B_SPLINE_CURVE_WITH_KNOTS ( ( 3, 2, 2, 2, 3 ),
 ( 0.4705882352941177516, 0.4742647058823530326, 0.4779411764705883692, 0.4816176470588236502, 0.4852941176470589313 ),
 .UNSPECIFIED. ) 
 CURVE ( )  GEOMETRIC_REPRESENTATION_ITEM ( )  RATIONAL_B_SPLINE_CURVE ( ( 0.9999999999999976685, 0.9238795325112890700, 1.000000000000000000, 0.9238795325112867385, 1.000000000000000000, 0.9238795325112867385, 1.000000000000000000, 0.9238795325112844070, 1.000000000000002220 ) ) 
 REPRESENTATION_ITEM ( '' )  );
#39907=AXIS2_PLACEMENT_3D ( 'NONE', #4316, #9604, #60525 ) ;
#39917=ORIENTED_EDGE ( 'NONE', *, *, #5392, .F. ) ;
#39925=CARTESIAN_POINT ( 'NONE',  ( -7.204075437095967871, 7.204075437095967871, 76.46875000204836681 ) ) ;
#39928=CARTESIAN_POINT ( 'NONE',  ( -7.778174593052020747, -7.778174593052023411, 85.18749999999998579 ) ) ;
#39940=FACE_OUTER_BOUND ( 'NONE', #63411, .T. ) ;
#39952=CARTESIAN_POINT ( 'NONE',  ( 2.020667218593132706E-15, -11.00000000000000000, 74.87499999999998579 ) ) ;
#39955=CARTESIAN_POINT ( 'NONE',  ( 4.556349186104051263, -10.99999999999999822, 73.65625000409676204 ) ) ;
#39973=CARTESIAN_POINT ( 'NONE',  ( 1.871523826299183495E-15, -10.18810118749999916, 71.03125000204838102 ) ) ;
#40010=EDGE_CURVE ( 'NONE', #30828, #70626, #40962, .T. ) ;
#40012=CARTESIAN_POINT ( 'NONE',  ( 10.18810118749999916, 4.220049686691935698, 91.00000000204836681 ) ) ;
#40014=CARTESIAN_POINT ( 'NONE',  ( -11.00000000000000000, 0.000000000000000000, 71.68750000409676204 ) ) ;
#40015=CARTESIAN_POINT ( 'NONE',  ( 11.00000000000000000, 4.556349186104045934, 103.8437499999999858 ) ) ;
#40043=CARTESIAN_POINT ( 'NONE',  ( -11.00000000000000000, 0.000000000000000000, 91.18750000409677625 ) ) ;
#40067=CARTESIAN_POINT ( 'NONE',  ( -10.18810118749999916, 0.000000000000000000, 96.53125000204838102 ) ) ;
#40074=CARTESIAN_POINT ( 'NONE',  ( 1.871523826299183495E-15, -10.18810118749999916, 108.5312500020483810 ) ) ;
#40083=CARTESIAN_POINT ( 'NONE',  ( -6.238412754330611322E-16, 10.18810118749999916, 105.1562500020483810 ) ) ;
#40099=CARTESIAN_POINT ( 'NONE',  ( 10.18810118749999916, 1.247682550866122264E-15, 108.9062500020483668 ) ) ;
#40100=CARTESIAN_POINT ( 'NONE',  ( 4.556349186104045934, 11.00000000000000000, 96.71875000409677625 ) ) ;
#40106=VERTEX_POINT ( 'NONE', #48082 ) ;
#40114=CARTESIAN_POINT ( 'NONE',  ( 10.18810118749999916, 1.247682550866122264E-15, 68.78125000204838102 ) ) ;
#40119=CARTESIAN_POINT ( 'NONE',  ( 7.778174593052023411, -7.778174593052021635, 97.75000000409677625 ) ) ;
#40125=CARTESIAN_POINT ( 'NONE',  ( -6.735557395310442023E-16, 11.00000000000000000, 108.8125000040967763 ) ) ;
#40142=( BOUNDED_CURVE ( )  B_SPLINE_CURVE ( 2, ( #3628, #20591, #37590, #31926, #54948, #26245, #32689, #43233, #25868 ),
 .UNSPECIFIED., .F., .F. ) 
 B_SPLINE_CURVE_WITH_KNOTS ( ( 3, 2, 2, 2, 3 ),
 ( 0.8088235294117647189, 0.8125000000000000000, 0.8161764705882352811, 0.8198529411764705621, 0.8235294117647058432 ),
 .UNSPECIFIED. ) 
 CURVE ( )  GEOMETRIC_REPRESENTATION_ITEM ( )  RATIONAL_B_SPLINE_CURVE ( ( 1.000000000000000000, 0.9238795325112867385, 1.000000000000000000, 0.9238795325112867385, 1.000000000000000000, 0.9238795325112867385, 1.000000000000000000, 0.9238795325112867385, 1.000000000000000000 ) ) 
 REPRESENTATION_ITEM ( '' )  );
#40151=CARTESIAN_POINT ( 'NONE',  ( 4.220049686691941027, -10.18810118749999738, 83.12500000204835260 ) ) ;
#40155=CARTESIAN_POINT ( 'NONE',  ( 10.18810118749999916, 1.247682550866122264E-15, 115.2812500020483810 ) ) ;
#40163=CARTESIAN_POINT ( 'NONE',  ( 10.18810118750000093, -4.220049686691933033, 76.18750000204838102 ) ) ;
#40176=CARTESIAN_POINT ( 'NONE',  ( -4.220049686691935698, 10.18810118749999916, 68.87500000204838102 ) ) ;
#40180=VERTEX_POINT ( 'NONE', #71454 ) ;
#40196=CARTESIAN_POINT ( 'NONE',  ( -6.735557395310442023E-16, 11.00000000000000000, 74.31250000409676204 ) ) ;
#40235=CARTESIAN_POINT ( 'NONE',  ( -3.205257545844395928, 10.40344923676435052, 117.6241125671348868 ) ) ;
#40236=EDGE_CURVE ( 'NONE', #40180, #41775, #31103, .T. ) ;
#40237=CARTESIAN_POINT ( 'NONE',  ( -7.204075437095965206, -7.204075437095968759, 103.8437500020483810 ) ) ;
#40247=EDGE_CURVE ( 'NONE', #74244, #72648, #59789, .T. ) ;
#40250=CARTESIAN_POINT ( 'NONE',  ( 7.778174593052021635, 7.778174593052023411, 99.62500000409677625 ) ) ;
#40254=CARTESIAN_POINT ( 'NONE',  ( -10.18810118749999916, 0.000000000000000000, 95.03125000204836681 ) ) ;
#40264=EDGE_LOOP ( 'NONE', ( #52862, #30164, #33501, #19662 ) ) ;
#40268=CARTESIAN_POINT ( 'NONE',  ( 7.204075437095968759, -7.204075437095966983, 96.71875000204838102 ) ) ;
#40275=VECTOR ( 'NONE', #36929, 1000.000000000000000 ) ;
#40277=CARTESIAN_POINT ( 'NONE',  ( 10.18810118750000093, -4.220049686691933921, 74.68750000204836681 ) ) ;
#40290=ORIENTED_EDGE ( 'NONE', *, *, #14729, .F. ) ;
#40294=CARTESIAN_POINT ( 'NONE',  ( -4.220049686691937474, -10.18810118749999738, 70.93750000204838102 ) ) ;
#40297=CARTESIAN_POINT ( 'NONE',  ( -4.556349186104047710, -10.99999999999999822, 85.28124999999998579 ) ) ;
#40305=DIRECTION ( 'NONE',  ( -0.000000000000000000, -0.000000000000000000, -1.000000000000000000 ) ) ;
#40322=CARTESIAN_POINT ( 'NONE',  ( 2.947432525776574330, 11.00000000000000178, 66.75185456451232824 ) ) ;
#40324=CARTESIAN_POINT ( 'NONE',  ( 11.00000000000000000, 4.556349186104045934, 77.03125000409677625 ) ) ;
#40338=CARTESIAN_POINT ( 'NONE',  ( 10.18810118749999916, 1.247682550866122264E-15, 113.7812500020483810 ) ) ;
#40342=CARTESIAN_POINT ( 'NONE',  ( -10.18810118749999916, 4.220049686691934809, 73.56250000204835260 ) ) ;
#40356=ADVANCED_FACE ( 'NONE', ( #28056 ), #56366, .F. ) ;
#40358=ORIENTED_EDGE ( 'NONE', *, *, #74582, .F. ) ;
#40383=CARTESIAN_POINT ( 'NONE',  ( -6.238412754330611322E-16, 10.18810118749999916, 89.78125000204836681 ) ) ;
#40386=CARTESIAN_POINT ( 'NONE',  ( 2.020667218593132706E-15, -11.00000000000000000, 98.87499999999998579 ) ) ;
#40392=CARTESIAN_POINT ( 'NONE',  ( 7.778174593052023411, -7.778174593052021635, 87.25000000409677625 ) ) ;
#40417=CARTESIAN_POINT ( 'NONE',  ( -6.735557395310442023E-16, 11.00000000000000000, 93.81250000409677625 ) ) ;
#40439=CARTESIAN_POINT ( 'NONE',  ( 10.18810118749999916, 4.220049686691935698, 95.87500000204838102 ) ) ;
#40447=CARTESIAN_POINT ( 'NONE',  ( 4.220049686691934809, 10.18810118749999916, 109.1875000020483810 ) ) ;
#40456=CARTESIAN_POINT ( 'NONE',  ( -10.18810118749999916, 4.220049686691934809, 105.4375000020483668 ) ) ;
#40457=CARTESIAN_POINT ( 'NONE',  ( -4.556349186104045934, 11.00000000000000000, 75.71874999999998579 ) ) ;
#40470=CARTESIAN_POINT ( 'NONE',  ( -10.18810118749999916, 4.220049686691934809, 108.0625000020483810 ) ) ;
#40488=CARTESIAN_POINT ( 'NONE',  ( -7.204075437095965206, -7.204075437095968759, 71.21875000204836681 ) ) ;
#40500=CARTESIAN_POINT ( 'NONE',  ( -6.735557395310442023E-16, 11.00000000000000000, 110.3125000040967763 ) ) ;
#40502=CARTESIAN_POINT ( 'NONE',  ( -4.556349186104048599, -10.99999999999999822, 70.28124999999998579 ) ) ;
#40521=CARTESIAN_POINT ( 'NONE',  ( -10.18810118749999916, 4.220049686691934809, 81.06250000204836681 ) ) ;
#40522=DIRECTION ( 'NONE',  ( -0.000000000000000000, -0.000000000000000000, -1.000000000000000000 ) ) ;
#40524=CARTESIAN_POINT ( 'NONE',  ( -4.220049686691937474, -10.18810118749999738, 114.8125000020483668 ) ) ;
#40531=CARTESIAN_POINT ( 'NONE',  ( -6.238412754330611322E-16, 10.18810118749999916, 76.65625000204836681 ) ) ;
#40534=CARTESIAN_POINT ( 'NONE',  ( 2.020667218593132706E-15, -11.00000000000000000, 94.56250000409677625 ) ) ;
#40545=CARTESIAN_POINT ( 'NONE',  ( -4.220049686691935698, 10.18810118749999916, 73.37500000204838102 ) ) ;
#40560=VERTEX_POINT ( 'NONE', #34859 ) ;
#40582=CARTESIAN_POINT ( 'NONE',  ( 0.000000000000000000, 0.000000000000000000, 118.0000000000000000 ) ) ;
#40611=CARTESIAN_POINT ( 'NONE',  ( -6.238412754330611322E-16, 10.18810118749999916, 98.78125000204838102 ) ) ;
#40624=CARTESIAN_POINT ( 'NONE',  ( -7.778174593052023411, 7.778174593052023411, 100.0000000040967763 ) ) ;
#40628=CARTESIAN_POINT ( 'NONE',  ( 4.220049686691941027, -10.18810118749999738, 94.00000000204838102 ) ) ;
#40638=CARTESIAN_POINT ( 'NONE',  ( -11.00000000000000000, 0.000000000000000000, 89.68750000409677625 ) ) ;
#40640=CARTESIAN_POINT ( 'NONE',  ( -7.204075437095965206, -7.204075437095968759, 91.84375000204838102 ) ) ;
#40650=CARTESIAN_POINT ( 'NONE',  ( 4.220049686691941027, -10.18810118749999738, 76.00000000204838102 ) ) ;
#40653=LINE ( 'NONE', #1055, #18550 ) ;
#40667=CARTESIAN_POINT ( 'NONE',  ( 7.204075437095966983, 7.204075437095967871, 70.09375000204836681 ) ) ;
#40670=CARTESIAN_POINT ( 'NONE',  ( -11.00000000000000000, 0.000000000000000000, 83.49999999999998579 ) ) ;
#40674=( BOUNDED_CURVE ( )  B_SPLINE_CURVE ( 2, ( #31685, #14684, #10910, #50892, #10537, #39582, #57318, #11284, #16929 ),
 .UNSPECIFIED., .F., .F. ) 
 B_SPLINE_CURVE_WITH_KNOTS ( ( 3, 2, 2, 2, 3 ),
 ( 0.7058823529411764053, 0.7095588235294116863, 0.7132352941176469674, 0.7169117647058822484, 0.7205882352941175295 ),
 .UNSPECIFIED. ) 
 CURVE ( )  GEOMETRIC_REPRESENTATION_ITEM ( )  RATIONAL_B_SPLINE_CURVE ( ( 1.000000000000002220, 0.9238795325112844070, 1.000000000000000000, 0.9238795325112867385, 1.000000000000000000, 0.9238795325112867385, 1.000000000000000000, 0.9238795325112890700, 0.9999999999999976685 ) ) 
 REPRESENTATION_ITEM ( '' )  );
#40675=ORIENTED_EDGE ( 'NONE', *, *, #56073, .T. ) ;
#40697=CARTESIAN_POINT ( 'NONE',  ( 7.778174593052021635, 7.778174593052023411, 69.62500000409677625 ) ) ;
#40707=CARTESIAN_POINT ( 'NONE',  ( 5.471491410962281421, 9.542682104092435225, 117.5000000000000568 ) ) ;
#40709=CARTESIAN_POINT ( 'NONE',  ( 10.18810118749999916, 1.247682550866122264E-15, 115.2812500020483810 ) ) ;
#40713=CARTESIAN_POINT ( 'NONE',  ( -10.18810118749999916, 0.000000000000000000, 73.65625000204836681 ) ) ;
#40739=VECTOR ( 'NONE', #54500, 1000.000000000000000 ) ;
#40747=CARTESIAN_POINT ( 'NONE',  ( -10.18810118749999916, 0.000000000000000000, 88.65625000204838102 ) ) ;
#40748=CARTESIAN_POINT ( 'NONE',  ( -7.778174593052023411, 7.778174593052023411, 92.31249999999998579 ) ) ;
#40750=CARTESIAN_POINT ( 'NONE',  ( -6.735557395310442023E-16, 11.00000000000000000, 104.1250000000000000 ) ) ;
#40757=CARTESIAN_POINT ( 'NONE',  ( -11.00000000000000000, 0.000000000000000000, 86.68750000409677625 ) ) ;
#40759=ADVANCED_FACE ( 'NONE', ( #60055 ), #9131, .T. ) ;
#40780=EDGE_CURVE ( 'NONE', #49272, #31332, #23811, .T. ) ;
#40783=CARTESIAN_POINT ( 'NONE',  ( -11.00000000000000000, 0.000000000000000000, 86.68750000409677625 ) ) ;
#40806=CARTESIAN_POINT ( 'NONE',  ( 7.204075437095968759, -7.204075437095966983, 89.59375000204838102 ) ) ;
#40807=ORIENTED_EDGE ( 'NONE', *, *, #40010, .T. ) ;
#40810=DIRECTION ( 'NONE',  ( -0.000000000000000000, -0.000000000000000000, -1.000000000000000000 ) ) ;
#40811=CARTESIAN_POINT ( 'NONE',  ( -7.778174593052020747, -7.778174593052023411, 100.3750000040967763 ) ) ;
#40815=CARTESIAN_POINT ( 'NONE',  ( 1.871523826299183495E-15, -10.18810118749999916, 105.5312500020483810 ) ) ;
#40822=CARTESIAN_POINT ( 'NONE',  ( 2.020667218593132706E-15, -11.00000000000000000, 76.56250000409677625 ) ) ;
#40826=CARTESIAN_POINT ( 'NONE',  ( -10.18810118749999916, 0.000000000000000000, 105.5312500020483810 ) ) ;
#40841=CARTESIAN_POINT ( 'NONE',  ( -10.18810118749999916, 0.000000000000000000, 105.1562500020483810 ) ) ;
#40861=CARTESIAN_POINT ( 'NONE',  ( 7.778174593052023411, -7.778174593052021635, 117.0625000000000000 ) ) ;
#40874=CARTESIAN_POINT ( 'NONE',  ( -11.00000000000000000, 0.000000000000000000, 107.6875000040967763 ) ) ;
#40888=EDGE_CURVE ( 'NONE', #32560, #72571, #8009, .T. ) ;
#40890=FACE_OUTER_BOUND ( 'NONE', #42444, .T. ) ;
#40894=CARTESIAN_POINT ( 'NONE',  ( -6.238412754330611322E-16, 10.18810118749999916, 82.28125000204838102 ) ) ;
#40898=CARTESIAN_POINT ( 'NONE',  ( -10.18810118749999916, 0.000000000000000000, 113.0312500020483810 ) ) ;
#40905=CARTESIAN_POINT ( 'NONE',  ( -7.204075437095965206, -7.204075437095968759, 77.21875000204836681 ) ) ;
#40919=CARTESIAN_POINT ( 'NONE',  ( 10.18810118749999916, 1.247682550866122264E-15, 72.90625000204836681 ) ) ;
#40924=CARTESIAN_POINT ( 'NONE',  ( -6.735557395310442023E-16, 11.00000000000000000, 110.1249999999999858 ) ) ;
#40937=VERTEX_POINT ( 'NONE', #9883 ) ;
#40948=PRODUCT_DEFINITION_SHAPE ( 'NONE', 'NONE',  #50979 ) ;
#40962=LINE ( 'NONE', #53396, #69525 ) ;
#40985=CARTESIAN_POINT ( 'NONE',  ( -10.68940375632318052, 0.4758252052427544010, 117.8105962436767697 ) ) ;
#40987=CARTESIAN_POINT ( 'NONE',  ( -7.204075437095967871, 7.204075437095967871, 101.9687500020483668 ) ) ;
#40999=CARTESIAN_POINT ( 'NONE',  ( 2.020667218593132706E-15, -11.00000000000000000, 73.37500000000000000 ) ) ;
#41004=CARTESIAN_POINT ( 'NONE',  ( 7.204075437095968759, -7.204075437095966983, 92.59375000204838102 ) ) ;
#41009=CARTESIAN_POINT ( 'NONE',  ( 7.204075437095968759, -7.204075437095966983, 77.59375000204838102 ) ) ;
#41018=CARTESIAN_POINT ( 'NONE',  ( 10.18810118749999916, 1.247682550866122264E-15, 92.40625000204836681 ) ) ;
#41027=CARTESIAN_POINT ( 'NONE',  ( -10.18810118749999738, -4.220049686691941915, 75.62500000204838102 ) ) ;
#41031=( BOUNDED_CURVE ( )  B_SPLINE_CURVE ( 1, ( #3191, #26177 ),
 .UNSPECIFIED., .F., .F. ) 
 B_SPLINE_CURVE_WITH_KNOTS ( ( 2, 2 ),
 ( 0.000000000000000000, 1.000000000000000000 ),
 .UNSPECIFIED. ) 
 CURVE ( )  GEOMETRIC_REPRESENTATION_ITEM ( )  RATIONAL_B_SPLINE_CURVE ( ( 0.9660721378631347278, 0.9660721378631347278 ) ) 
 REPRESENTATION_ITEM ( '' )  );
#41039=CARTESIAN_POINT ( 'NONE',  ( 11.00000000000010836, -4.556349186103939353, 88.84375000409677625 ) ) ;
#41044=CARTESIAN_POINT ( 'NONE',  ( 4.220049686691934809, 10.18810118749999916, 70.18750000204838102 ) ) ;
#41047=CARTESIAN_POINT ( 'NONE',  ( 4.556349186104045934, 11.00000000000000000, 84.53125000000000000 ) ) ;
#41051=EDGE_CURVE ( 'NONE', #16043, #13039, #20860, .T. ) ;
#41073=CARTESIAN_POINT ( 'NONE',  ( 7.204075437095966983, 7.204075437095967871, 116.5937500020483810 ) ) ;
#41074=DIRECTION ( 'NONE',  ( -0.000000000000000000, -0.000000000000000000, -1.000000000000000000 ) ) ;
#41083=CARTESIAN_POINT ( 'NONE',  ( -10.99999999999989342, 4.556349186104152515, 108.9062500000000000 ) ) ;
#41085=CARTESIAN_POINT ( 'NONE',  ( 7.204075437095968759, -7.204075437095966983, 110.5937500020483810 ) ) ;
#41125=CARTESIAN_POINT ( 'NONE',  ( -7.204075437095965206, -7.204075437095968759, 87.34375000204836681 ) ) ;
#41128=CARTESIAN_POINT ( 'NONE',  ( 4.556349186104045934, 11.00000000000000000, 104.0312499999999858 ) ) ;
#41135=AXIS2_PLACEMENT_3D ( 'NONE', #23904, #69562, #29939 ) ;
#41137=PLANE ( 'NONE',  #9678 ) ;
#41160=CARTESIAN_POINT ( 'NONE',  ( 11.00000000000000355, -4.556349186104045046, 88.84375000409677625 ) ) ;
#41162=CARTESIAN_POINT ( 'NONE',  ( -11.00000000000006395, -4.556349186103986426, 110.7812500040967620 ) ) ;
#41175=ORIENTED_EDGE ( 'NONE', *, *, #54378, .T. ) ;
#41176=CARTESIAN_POINT ( 'NONE',  ( 11.00000000000005329, -4.556349186103991755, 100.6562500000000000 ) ) ;
#41184=CARTESIAN_POINT ( 'NONE',  ( 4.220049686691934809, 10.18810118749999916, 91.56250000204836681 ) ) ;
#41191=CARTESIAN_POINT ( 'NONE',  ( -7.204075437095967871, 7.204075437095967871, 107.9687500020483810 ) ) ;
#41199=CARTESIAN_POINT ( 'NONE',  ( -6.735557395310442023E-16, 11.00000000000000000, 96.62499999999998579 ) ) ;
#41200=CARTESIAN_POINT ( 'NONE',  ( 10.18810118749999916, 4.220049686691935698, 104.8750000020483668 ) ) ;
#41215=CARTESIAN_POINT ( 'NONE',  ( -10.18810118749999916, 4.220049686691934809, 105.0625000020483810 ) ) ;
#41216=CARTESIAN_POINT ( 'NONE',  ( 11.00000000000005329, -4.556349186103991755, 103.6562499999999716 ) ) ;
#41233=CARTESIAN_POINT ( 'NONE',  ( -11.00000000000000000, 0.000000000000000000, 73.18750000409676204 ) ) ;
#41234=CARTESIAN_POINT ( 'NONE',  ( -11.00000000000000000, 0.000000000000000000, 118.0000000000000000 ) ) ;
#41246=CARTESIAN_POINT ( 'NONE',  ( 11.00000000000000000, 1.347111479062088405E-15, 103.9375000040967763 ) ) ;
#41262=DIRECTION ( 'NONE',  ( -0.000000000000000000, -0.000000000000000000, -1.000000000000000000 ) ) ;
#41265=CARTESIAN_POINT ( 'NONE',  ( -4.220049686691935698, 10.18810118749999916, 80.87500000204836681 ) ) ;
#41269=CARTESIAN_POINT ( 'NONE',  ( 4.220049686691934809, 10.18810118749999916, 112.5625000020483810 ) ) ;
#41277=CARTESIAN_POINT ( 'NONE',  ( 4.220049686691941027, -10.18810118749999738, 79.00000000204838102 ) ) ;
#41290=CARTESIAN_POINT ( 'NONE',  ( 10.18810118749999916, 4.220049686691935698, 71.50000000204839523 ) ) ;
#41293=EDGE_CURVE ( 'NONE', #1009, #56815, #18875, .T. ) ;
#41316=ORIENTED_EDGE ( 'NONE', *, *, #58065, .T. ) ;
#41331=EDGE_CURVE ( 'NONE', #69053, #28981, #38279, .T. ) ;
#41333=AXIS2_PLACEMENT_3D ( 'NONE', #12133, #40810, #474 ) ;
#41335=EDGE_CURVE ( 'NONE', #7250, #68586, #35866, .T. ) ;
#41354=CARTESIAN_POINT ( 'NONE',  ( -6.164216839359130340, 8.915442299230837975, 117.6714253161478183 ) ) ;
#41355=CARTESIAN_POINT ( 'NONE',  ( 7.204075437095966983, 7.204075437095967871, 98.59375000204836681 ) ) ;
#41358=CARTESIAN_POINT ( 'NONE',  ( -11.00000000000020783, -4.556349186103842541, 68.59374999999997158 ) ) ;
#41369=CARTESIAN_POINT ( 'NONE',  ( 11.00000000000000000, 1.347111479062088405E-15, 99.43750000409677625 ) ) ;
#41373=CARTESIAN_POINT ( 'NONE',  ( 4.220049686691934809, 10.18810118749999916, 94.56250000204838102 ) ) ;
#41379=CARTESIAN_POINT ( 'NONE',  ( 4.220049686691941027, -10.18810118749999738, 82.00000000204836681 ) ) ;
#41387=CARTESIAN_POINT ( 'NONE',  ( 4.220049686691941027, -10.18810118749999738, 89.12500000204836681 ) ) ;
#41396=CARTESIAN_POINT ( 'NONE',  ( 4.220049686691941027, -10.18810118749999738, 73.00000000204836681 ) ) ;
#41414=CARTESIAN_POINT ( 'NONE',  ( -10.18810118749999738, -4.220049686691941915, 69.25000000204836681 ) ) ;
#41417=CARTESIAN_POINT ( 'NONE',  ( 7.778174593052021635, 7.778174593052023411, 82.93750000000000000 ) ) ;
#41420=CARTESIAN_POINT ( 'NONE',  ( 4.556349186104052151, -10.99999999999999822, 113.9687500000000142 ) ) ;
#41444=CARTESIAN_POINT ( 'NONE',  ( 7.778174593052023411, -7.778174593052021635, 67.75000000409677625 ) ) ;
#41456=CARTESIAN_POINT ( 'NONE',  ( -4.220049686691935698, 10.18810118749999916, 112.7500000020483810 ) ) ;
#41460=CYLINDRICAL_SURFACE ( 'NONE', #38854, 11.00000000000000000 ) ;
#41492=CARTESIAN_POINT ( 'NONE',  ( -4.220049686691935698, 10.18810118749999916, 85.37500000204838102 ) ) ;
#41494=CARTESIAN_POINT ( 'NONE',  ( -10.99999999999999822, -4.556349186104052151, 103.0937500000000000 ) ) ;
#41499=CARTESIAN_POINT ( 'NONE',  ( 7.778174593052021635, 7.778174593052023411, 105.6250000040967763 ) ) ;
#41503=AXIS2_PLACEMENT_3D ( 'NONE', #53071, #1406, #70421 ) ;
#41518=DIRECTION ( 'NONE',  ( 1.000000000000000000, 0.000000000000000000, 0.000000000000000000 ) ) ;
#41522=CARTESIAN_POINT ( 'NONE',  ( 4.556349186104051263, -10.99999999999999822, 85.65625000409679046 ) ) ;
#41544=VECTOR ( 'NONE', #70996, 1000.000000000000000 ) ;
#41547=CARTESIAN_POINT ( 'NONE',  ( -7.204075437095965206, -7.204075437095968759, 90.71875000204838102 ) ) ;
#41552=CARTESIAN_POINT ( 'NONE',  ( -6.238412754330611322E-16, 10.18810118749999916, 98.78125000204838102 ) ) ;
#41564=CARTESIAN_POINT ( 'NONE',  ( -7.204075437095967871, 7.204075437095967871, 102.3437500020483668 ) ) ;
#41579=VERTEX_POINT ( 'NONE', #50054 ) ;
#41581=CARTESIAN_POINT ( 'NONE',  ( 10.18810118749999916, 1.247682550866122264E-15, 102.9062500020483810 ) ) ;
#41600=CARTESIAN_POINT ( 'NONE',  ( -11.00000000000000000, 4.556349186104045934, 116.4062500000000142 ) ) ;
#41612=CARTESIAN_POINT ( 'NONE',  ( -4.556349186104047710, -10.99999999999999822, 101.9687500040967620 ) ) ;
#41624=DIRECTION ( 'NONE',  ( -0.000000000000000000, -0.000000000000000000, -1.000000000000000000 ) ) ;
#41630=DIRECTION ( 'NONE',  ( -1.000000000000000000, 0.000000000000000000, 0.000000000000000000 ) ) ;
#41633=CARTESIAN_POINT ( 'NONE',  ( 4.220049686691941027, -10.18810118749999738, 84.62500000204838102 ) ) ;
#41637=CARTESIAN_POINT ( 'NONE',  ( 10.18810118749999916, 1.247682550866122264E-15, 110.7812500020483668 ) ) ;
#41644=CARTESIAN_POINT ( 'NONE',  ( 4.220049686691941027, -10.18810118749999738, 71.50000000204838102 ) ) ;
#41655=CARTESIAN_POINT ( 'NONE',  ( 10.18810118750000093, -4.220049686691933921, 71.31250000204836681 ) ) ;
#41659=ORIENTED_EDGE ( 'NONE', *, *, #40247, .F. ) ;
#41674=CARTESIAN_POINT ( 'NONE',  ( -10.18810118749999916, 0.000000000000000000, 117.1562500020483810 ) ) ;
#41681=LINE ( 'NONE', #64691, #68731 ) ;
#41703=CARTESIAN_POINT ( 'NONE',  ( -11.00000000000000533, -11.00000000000000355, 41.99999999999999289 ) ) ;
#41715=ADVANCED_FACE ( 'NONE', ( #11928 ), #46624, .F. ) ;
#41720=CARTESIAN_POINT ( 'NONE',  ( -4.220049686691935698, 10.18810118749999916, 103.3750000020484094 ) ) ;
#41733=CARTESIAN_POINT ( 'NONE',  ( 7.778174593052021635, 7.778174593052023411, 83.12500000409676204 ) ) ;
#41737=CARTESIAN_POINT ( 'NONE',  ( -10.18810118749999916, 4.220049686691934809, 97.93750000204836681 ) ) ;
#41743=CARTESIAN_POINT ( 'NONE',  ( 10.18810118749999916, 4.220049686691935698, 73.37500000204838102 ) ) ;
#41751=CARTESIAN_POINT ( 'NONE',  ( -4.220049686691935698, 10.18810118749999916, 89.87500000204836681 ) ) ;
#41760=CARTESIAN_POINT ( 'NONE',  ( 10.18810118749999916, 1.247682550866122264E-15, 77.78125000204836681 ) ) ;
#41762=EDGE_CURVE ( 'NONE', #39397, #63637, #33895, .T. ) ;
#41775=VERTEX_POINT ( 'NONE', #36425 ) ;
#41779=CARTESIAN_POINT ( 'NONE',  ( -6.735557395310442023E-16, 11.00000000000000000, 78.62499999999998579 ) ) ;
#41783=ORIENTED_EDGE ( 'NONE', *, *, #51466, .F. ) ;
#41806=CARTESIAN_POINT ( 'NONE',  ( 10.18810118750000093, -4.220049686691933921, 116.3125000020483668 ) ) ;
#41817=CARTESIAN_POINT ( 'NONE',  ( -7.204075437095965206, -7.204075437095968759, 111.7187500020483810 ) ) ;
#41821=CARTESIAN_POINT ( 'NONE',  ( -10.18810118749999738, -4.220049686691941915, 67.75000000204836681 ) ) ;
#41844=EDGE_LOOP ( 'NONE', ( #27101, #10627, #10081, #10051 ) ) ;
#41856=CARTESIAN_POINT ( 'NONE',  ( 10.18810118750000093, -4.220049686691933033, 86.31250000204838102 ) ) ;
#41858=CARTESIAN_POINT ( 'NONE',  ( -4.556349186104045934, 11.00000000000000000, 98.21875000000000000 ) ) ;
#41859=CARTESIAN_POINT ( 'NONE',  ( -7.778174593052020747, -7.778174593052023411, 104.6874999999999858 ) ) ;
#41863=CARTESIAN_POINT ( 'NONE',  ( -11.00000000000000000, 0.000000000000000000, 106.1875000040967620 ) ) ;
#41864=CARTESIAN_POINT ( 'NONE',  ( -6.735557395310442023E-16, 11.00000000000000000, 78.62499999999998579 ) ) ;
#41877=( BOUNDED_CURVE ( )  B_SPLINE_CURVE ( 2, ( #44219, #48740, #67232, #71747, #14405, #43079, #54796, #14778, #9137 ),
 .UNSPECIFIED., .F., .F. ) 
 B_SPLINE_CURVE_WITH_KNOTS ( ( 3, 2, 2, 2, 3 ),
 ( 0.1911764705882353921, 0.1948529411764707009, 0.1985294117647060097, 0.2022058823529413185, 0.2058823529411765996 ),
 .UNSPECIFIED. ) 
 CURVE ( )  GEOMETRIC_REPRESENTATION_ITEM ( )  RATIONAL_B_SPLINE_CURVE ( ( 0.9999999999999976685, 0.9238795325112890700, 1.000000000000000000, 0.9238795325112867385, 1.000000000000000000, 0.9238795325112867385, 1.000000000000000000, 0.9238795325112838519, 1.000000000000002887 ) ) 
 REPRESENTATION_ITEM ( '' )  );
#41882=CARTESIAN_POINT ( 'NONE',  ( -11.00000000000000000, 0.000000000000000000, 99.99999999999998579 ) ) ;
#41887=CARTESIAN_POINT ( 'NONE',  ( -4.556349186104045934, 11.00000000000000000, 89.40625000409676204 ) ) ;
#41911=CARTESIAN_POINT ( 'NONE',  ( -10.18810118749999916, 0.000000000000000000, 92.03125000204836681 ) ) ;
#41916=CARTESIAN_POINT ( 'NONE',  ( 10.18810118750000093, -4.220049686691933921, 104.3125000020483810 ) ) ;
#41923=CARTESIAN_POINT ( 'NONE',  ( -11.00000000000000000, 4.556349186104045934, 96.90624999999998579 ) ) ;
#41924=EDGE_CURVE ( 'NONE', #39166, #18528, #66566, .T. ) ;
#41925=CARTESIAN_POINT ( 'NONE',  ( 4.220049686691934809, 10.18810118749999916, 97.56250000204836681 ) ) ;
#41926=ADVANCED_FACE ( 'NONE', ( #32256 ), #42803, .T. ) ;
#41942=CARTESIAN_POINT ( 'NONE',  ( 1.871523826299183495E-15, -10.18810118749999916, 105.5312500020483810 ) ) ;
#41958=CARTESIAN_POINT ( 'NONE',  ( -6.735557395310442023E-16, 11.00000000000000000, 113.1249999999999858 ) ) ;
#41969=CARTESIAN_POINT ( 'NONE',  ( 7.778174593052023411, -7.778174593052021635, 103.7500000040967763 ) ) ;
#41992=CARTESIAN_POINT ( 'NONE',  ( -6.238412754330611322E-16, 10.18810118749999916, 111.1562500020483668 ) ) ;
#41994=( BOUNDED_CURVE ( )  B_SPLINE_CURVE ( 2, ( #70537, #48621, #71628, #14282, #18852, #12810, #41859, #64870, #61072 ),
 .UNSPECIFIED., .F., .F. ) 
 B_SPLINE_CURVE_WITH_KNOTS ( ( 3, 2, 2, 2, 3 ),
 ( 0.2499999999999998890, 0.2536764705882351700, 0.2573529411764704511, 0.2610294117647057877, 0.2647058823529410687 ),
 .UNSPECIFIED. ) 
 CURVE ( )  GEOMETRIC_REPRESENTATION_ITEM ( )  RATIONAL_B_SPLINE_CURVE ( ( 1.000000000000002220, 0.9238795325112844070, 1.000000000000000000, 0.9238795325112867385, 1.000000000000000000, 0.9238795325112867385, 1.000000000000000000, 0.9238795325112890700, 0.9999999999999976685 ) ) 
 REPRESENTATION_ITEM ( '' )  );
#41997=CARTESIAN_POINT ( 'NONE',  ( 4.556349186104052151, -10.99999999999999822, 109.6562500040967905 ) ) ;
#42001=CARTESIAN_POINT ( 'NONE',  ( -10.18810118749999916, 4.220049686691934809, 73.93750000204838102 ) ) ;
#42007=EDGE_CURVE ( 'NONE', #24549, #68202, #72223, .T. ) ;
#42014=CARTESIAN_POINT ( 'NONE',  ( 7.204075437095966983, 7.204075437095967871, 115.4687500020483810 ) ) ;
#42043=CARTESIAN_POINT ( 'NONE',  ( 11.00000000000000000, 1.347111479062088405E-15, 94.74999999999998579 ) ) ;
#42045=CARTESIAN_POINT ( 'NONE',  ( 7.778174593052021635, 7.778174593052023411, 116.1250000040967905 ) ) ;
#42050=CARTESIAN_POINT ( 'NONE',  ( -6.735557395310442023E-16, 11.00000000000000000, 75.81250000409677625 ) ) ;
#42058=CARTESIAN_POINT ( 'NONE',  ( 4.556349186104045934, 11.00000000000000000, 68.21875000409676204 ) ) ;
#42064=FACE_OUTER_BOUND ( 'NONE', #73873, .T. ) ;
#42075=CYLINDRICAL_SURFACE ( 'NONE', #57255, 11.00000000000000000 ) ;
#42076=CARTESIAN_POINT ( 'NONE',  ( -10.18810118749999916, 0.000000000000000000, 97.65625000204838102 ) ) ;
#42079=CARTESIAN_POINT ( 'NONE',  ( -11.00000000000000533, 11.00000000000000000, 41.99999999999999289 ) ) ;
#42090=CARTESIAN_POINT ( 'NONE',  ( 10.18810118750000093, -4.220049686691933033, 91.18750000204836681 ) ) ;
#42095=CARTESIAN_POINT ( 'NONE',  ( -7.778174593052020747, -7.778174593052023411, 101.8750000040967763 ) ) ;
#42096=CARTESIAN_POINT ( 'NONE',  ( 7.204075437095966983, 7.204075437095967871, 74.96875000204836681 ) ) ;
#42104=CARTESIAN_POINT ( 'NONE',  ( 7.204075437095968759, -7.204075437095966983, 89.21875000204838102 ) ) ;
#42109=ORIENTED_EDGE ( 'NONE', *, *, #54172, .T. ) ;
#42116=CARTESIAN_POINT ( 'NONE',  ( 4.220049686691941027, -10.18810118749999738, 70.00000000204836681 ) ) ;
#42135=CARTESIAN_POINT ( 'NONE',  ( -4.556349186104047710, -10.99999999999999822, 74.78125000000001421 ) ) ;
#42148=LINE ( 'NONE', #13472, #8274 ) ;
#42161=CARTESIAN_POINT ( 'NONE',  ( -6.238412754330611322E-16, 10.18810118749999916, 84.15625000204838102 ) ) ;
#42162=CARTESIAN_POINT ( 'NONE',  ( -10.99999999999999822, -4.556349186104052151, 70.28125000409677625 ) ) ;
#42174=CARTESIAN_POINT ( 'NONE',  ( 1.871523826299183495E-15, -10.18810118749999916, 105.9062500020483810 ) ) ;
#42178=DIRECTION ( 'NONE',  ( -1.000000000000000000, 0.000000000000000000, 0.000000000000000000 ) ) ;
#42201=ORIENTED_EDGE ( 'NONE', *, *, #28984, .F. ) ;
#42214=VERTEX_POINT ( 'NONE', #35576 ) ;
#42217=CARTESIAN_POINT ( 'NONE',  ( -10.18810118749999738, -4.220049686691941915, 85.75000000204838102 ) ) ;
#42219=CARTESIAN_POINT ( 'NONE',  ( -4.556349186104047710, -10.99999999999999822, 95.78124999999998579 ) ) ;
#42250=CARTESIAN_POINT ( 'NONE',  ( -4.556349186104045934, 11.00000000000000000, 84.90625000409676204 ) ) ;
#42268=EDGE_LOOP ( 'NONE', ( #6907, #32837, #33170, #15626 ) ) ;
#42275=CARTESIAN_POINT ( 'NONE',  ( 11.00000000000010658, 4.556349186103942017, 90.53125000409677625 ) ) ;
#42277=CARTESIAN_POINT ( 'NONE',  ( -6.238412754330611322E-16, 10.18810118749999916, 91.65625000204836681 ) ) ;
#42282=CARTESIAN_POINT ( 'NONE',  ( 4.220049686691941027, -10.18810118749999738, 102.6250000020483810 ) ) ;
#42290=CARTESIAN_POINT ( 'NONE',  ( 7.204075437095966983, 7.204075437095967871, 98.96875000204838102 ) ) ;
#42295=ORIENTED_EDGE ( 'NONE', *, *, #21146, .T. ) ;
#42305=ORIENTED_EDGE ( 'NONE', *, *, #64472, .T. ) ;
#42306=CARTESIAN_POINT ( 'NONE',  ( -7.204075437095965206, -7.204075437095968759, 103.8437500020483810 ) ) ;
#42307=CARTESIAN_POINT ( 'NONE',  ( 4.556349186104045934, 11.00000000000000000, 114.7187500040967763 ) ) ;
#42308=CIRCLE ( 'NONE', #9818, 34.85072926314708752 ) ;
#42316=ORIENTED_EDGE ( 'NONE', *, *, #5266, .T. ) ;
#42324=CARTESIAN_POINT ( 'NONE',  ( 7.778174593052021635, 7.778174593052023411, 111.4375000000000000 ) ) ;
#42338=CARTESIAN_POINT ( 'NONE',  ( -11.00000000000000000, 4.556349186104045934, 104.5937500040967763 ) ) ;
#42341=CARTESIAN_POINT ( 'NONE',  ( 11.00000000000000000, 1.347111479062088405E-15, 94.93750000409677625 ) ) ;
#42344=FACE_OUTER_BOUND ( 'NONE', #64363, .T. ) ;
#42362=CARTESIAN_POINT ( 'NONE',  ( 10.18810118749999916, 4.220049686691935698, 112.3750000020483810 ) ) ;
#42364=LINE ( 'NONE', #64650, #62385 ) ;
#42370=CARTESIAN_POINT ( 'NONE',  ( 1.871523826299183495E-15, -10.18810118749999916, 68.40625000204836681 ) ) ;
#42382=CARTESIAN_POINT ( 'NONE',  ( -7.204075437095967871, 7.204075437095967871, 115.8437500020483810 ) ) ;
#42385=VERTEX_POINT ( 'NONE', #71730 ) ;
#42386=VECTOR ( 'NONE', #62398, 1000.000000000000000 ) ;
#42414=CARTESIAN_POINT ( 'NONE',  ( -11.00000000000000000, 0.000000000000000000, 118.0000000000000000 ) ) ;
#42426=PLANE ( 'NONE',  #4083 ) ;
#42431=VECTOR ( 'NONE', #14097, 1000.000000000000000 ) ;
#42435=CYLINDRICAL_SURFACE ( 'NONE', #1204, 11.00000000000000000 ) ;
#42440=CARTESIAN_POINT ( 'NONE',  ( 11.00000000000000000, 1.347111479062088405E-15, 115.7499999999999858 ) ) ;
#42444=EDGE_LOOP ( 'NONE', ( #13946, #52813, #4113, #42820 ) ) ;
#42446=CARTESIAN_POINT ( 'NONE',  ( -10.18810118749999916, 4.220049686691934809, 96.06250000204836681 ) ) ;
#42458=CARTESIAN_POINT ( 'NONE',  ( 7.778174593052023411, -7.778174593052021635, 73.56249999999998579 ) ) ;
#42464=CARTESIAN_POINT ( 'NONE',  ( 7.204075437095968759, -7.204075437095966983, 91.09375000204838102 ) ) ;
#42470=CARTESIAN_POINT ( 'NONE',  ( -4.220049686691937474, -10.18810118749999738, 75.81250000204838102 ) ) ;
#42478=CARTESIAN_POINT ( 'NONE',  ( 7.204075437095966983, 7.204075437095967871, 83.59375000204836681 ) ) ;
#42489=CARTESIAN_POINT ( 'NONE',  ( -10.18810118749999916, 4.220049686691934809, 67.93750000204838102 ) ) ;
#42511=CARTESIAN_POINT ( 'NONE',  ( 7.778174593052021635, 7.778174593052023411, 79.93750000000000000 ) ) ;
#42516=EDGE_CURVE ( 'NONE', #68675, #17249, #15140, .T. ) ;
#42517=EDGE_CURVE ( 'NONE', #41775, #8028, #46421, .T. ) ;
#42524=CARTESIAN_POINT ( 'NONE',  ( 4.556349186104045934, 11.00000000000000000, 116.2187500040967763 ) ) ;
#42534=DIRECTION ( 'NONE',  ( -1.084202172485504434E-16, 1.000000000000000000, 0.000000000000000000 ) ) ;
#42539=CARTESIAN_POINT ( 'NONE',  ( 7.204075437095968759, -7.204075437095966983, 89.59375000204838102 ) ) ;
#42540=CARTESIAN_POINT ( 'NONE',  ( 10.18810118750000093, -4.220049686691933921, 111.8125000020483952 ) ) ;
#42553=CARTESIAN_POINT ( 'NONE',  ( 7.204075437095966983, 7.204075437095967871, 104.9687500020483810 ) ) ;
#42576=CARTESIAN_POINT ( 'NONE',  ( -7.778174593052020747, -7.778174593052023411, 77.87500000409677625 ) ) ;
#42589=CARTESIAN_POINT ( 'NONE',  ( -7.204075437095965206, -7.204075437095968759, 81.34375000204838102 ) ) ;
#42591=CARTESIAN_POINT ( 'NONE',  ( 4.556349186104045934, 11.00000000000000000, 95.03124999999998579 ) ) ;
#42621=CARTESIAN_POINT ( 'NONE',  ( -10.99999999999999822, -4.556349186104052151, 79.28125000409677625 ) ) ;
#42647=CARTESIAN_POINT ( 'NONE',  ( 7.204075437095966983, 7.204075437095967871, 88.46875000204838102 ) ) ;
#42653=CARTESIAN_POINT ( 'NONE',  ( 10.18810118749999916, 1.247682550866122264E-15, 101.4062500020483810 ) ) ;
#42662=CARTESIAN_POINT ( 'NONE',  ( -6.238412754330611322E-16, 10.18810118749999916, 99.15625000204838102 ) ) ;
#42677=CARTESIAN_POINT ( 'NONE',  ( 7.204075437095968759, -7.204075437095966983, 96.71875000204838102 ) ) ;
#42694=CARTESIAN_POINT ( 'NONE',  ( -4.556349186104045934, 11.00000000000000000, 114.7187500000000000 ) ) ;
#42708=CARTESIAN_POINT ( 'NONE',  ( -6.735557395310442023E-16, 11.00000000000000000, 104.3125000040967763 ) ) ;
#42714=CARTESIAN_POINT ( 'NONE',  ( 11.00000000000000000, 1.347111479062088405E-15, 118.0000000000000000 ) ) ;
#42721=CARTESIAN_POINT ( 'NONE',  ( -7.778174593052020747, -7.778174593052023411, 67.37500000409676204 ) ) ;
#42732=CARTESIAN_POINT ( 'NONE',  ( 7.204075437095968759, -7.204075437095966983, 109.0937500020483810 ) ) ;
#42738=CARTESIAN_POINT ( 'NONE',  ( 10.18810118749999916, 4.220049686691935698, 71.87500000204836681 ) ) ;
#42750=CARTESIAN_POINT ( 'NONE',  ( -6.238412754330611322E-16, 10.18810118749999916, 114.1562500020483810 ) ) ;
#42760=CARTESIAN_POINT ( 'NONE',  ( -11.00000000000000000, 0.000000000000000000, 118.0000000000000000 ) ) ;
#42762=ORIENTED_EDGE ( 'NONE', *, *, #1104, .F. ) ;
#42765=( BOUNDED_CURVE ( )  B_SPLINE_CURVE ( 2, ( #48009, #30671, #47639, #13667, #19339, #64993, #42721, #70661, #14037 ),
 .UNSPECIFIED., .F., .F. ) 
 B_SPLINE_CURVE_WITH_KNOTS ( ( 3, 2, 2, 2, 3 ),
 ( 0.9558823529411765163, 0.9595588235294117974, 0.9632352941176471894, 0.9669117647058824705, 0.9705882352941177516 ),
 .UNSPECIFIED. ) 
 CURVE ( )  GEOMETRIC_REPRESENTATION_ITEM ( )  RATIONAL_B_SPLINE_CURVE ( ( 1.000000000000000000, 0.9238795325112867385, 1.000000000000000000, 0.9238795325112867385, 1.000000000000000000, 0.9238795325112867385, 1.000000000000000000, 0.9238795325112844070, 1.000000000000002220 ) ) 
 REPRESENTATION_ITEM ( '' )  );
#42794=CARTESIAN_POINT ( 'NONE',  ( 7.778174593052021635, 7.778174593052023411, 77.12500000409677625 ) ) ;
#42803=CYLINDRICAL_SURFACE ( 'NONE', #4581, 11.00000000000000000 ) ;
#42804=CARTESIAN_POINT ( 'NONE',  ( 11.00000000000013323, -4.556349186103911819, 105.3437500040967905 ) ) ;
#42807=CARTESIAN_POINT ( 'NONE',  ( 7.778174593052023411, -7.778174593052021635, 82.56249999999998579 ) ) ;
#42812=CARTESIAN_POINT ( 'NONE',  ( 10.18810118749999916, 4.220049686691935698, 95.50000000204838102 ) ) ;
#42820=ORIENTED_EDGE ( 'NONE', *, *, #62904, .F. ) ;
#42826=CARTESIAN_POINT ( 'NONE',  ( -7.204075437095965206, -7.204075437095968759, 87.71875000204836681 ) ) ;
#42831=CARTESIAN_POINT ( 'NONE',  ( 4.220049686691941027, -10.18810118749999738, 73.00000000204836681 ) ) ;
#42840=CARTESIAN_POINT ( 'NONE',  ( -10.18810118749999916, 0.000000000000000000, 82.65625000204838102 ) ) ;
#42846=ORIENTED_EDGE ( 'NONE', *, *, #25899, .T. ) ;
#42852=CARTESIAN_POINT ( 'NONE',  ( -4.220049686691935698, 10.18810118749999916, 67.75000000204836681 ) ) ;
#42874=CARTESIAN_POINT ( 'NONE',  ( 4.556349186104045934, 11.00000000000000000, 80.03124999999998579 ) ) ;
#42883=CARTESIAN_POINT ( 'NONE',  ( -11.00000000000000000, 4.556349186104045934, 116.5937500040967620 ) ) ;
#42900=CARTESIAN_POINT ( 'NONE',  ( 4.220049686691941027, -10.18810118749999738, 88.00000000204836681 ) ) ;
#42901=CARTESIAN_POINT ( 'NONE',  ( 10.18810118750000093, -4.220049686691933921, 110.3125000020483810 ) ) ;
#42913=DIRECTION ( 'NONE',  ( -1.000000000000000000, 0.000000000000000000, 0.000000000000000000 ) ) ;
#42916=CARTESIAN_POINT ( 'NONE',  ( -7.204075437095967871, 7.204075437095967871, 106.8437500020483810 ) ) ;
#42940=CARTESIAN_POINT ( 'NONE',  ( 11.00000000000000000, 1.347111479062088405E-15, 93.24999999999998579 ) ) ;
#42948=EDGE_LOOP ( 'NONE', ( #24447, #63518, #66336, #52019 ) ) ;
#42950=CARTESIAN_POINT ( 'NONE',  ( 11.00000000000000000, 4.556349186104045934, 82.84375000000000000 ) ) ;
#42955=CARTESIAN_POINT ( 'NONE',  ( 4.220049686691934809, 10.18810118749999916, 77.68750000204838102 ) ) ;
#42958=CARTESIAN_POINT ( 'NONE',  ( 11.00000000000000000, 1.347111479062088405E-15, 93.24999999999998579 ) ) ;
#42986=CARTESIAN_POINT ( 'NONE',  ( -4.556349186104047710, -10.99999999999999822, 79.46875000409677625 ) ) ;
#43003=CARTESIAN_POINT ( 'NONE',  ( 10.18810118749999916, 1.247682550866122264E-15, 75.90625000204836681 ) ) ;
#43005=CARTESIAN_POINT ( 'NONE',  ( -11.00000000000000000, 0.000000000000000000, 92.68750000409677625 ) ) ;
#43007=CARTESIAN_POINT ( 'NONE',  ( -11.00000000000000000, 0.000000000000000000, 74.49999999999998579 ) ) ;
#43010=CARTESIAN_POINT ( 'NONE',  ( -11.00000000000000000, 0.000000000000000000, 116.6875000040967763 ) ) ;
#43012=CARTESIAN_POINT ( 'NONE',  ( -7.204075437095965206, -7.204075437095968759, 84.71875000204836681 ) ) ;
#43017=CARTESIAN_POINT ( 'NONE',  ( 10.18810118749999916, 1.247682550866122264E-15, 104.4062500020483810 ) ) ;
#43025=CARTESIAN_POINT ( 'NONE',  ( -7.204075437095967871, 7.204075437095967871, 100.8437500020483668 ) ) ;
#43034=EDGE_CURVE ( 'NONE', #11931, #8408, #71272, .T. ) ;
#43042=EDGE_LOOP ( 'NONE', ( #26617, #70672, #68665, #31321 ) ) ;
#43044=CARTESIAN_POINT ( 'NONE',  ( -4.220049686691937474, -10.18810118749999738, 99.43750000204836681 ) ) ;
#43055=ORIENTED_EDGE ( 'NONE', *, *, #56439, .T. ) ;
#43065=CARTESIAN_POINT ( 'NONE',  ( -7.778174593052023411, 7.778174593052023411, 113.3125000000000000 ) ) ;
#43073=LINE ( 'NONE', #14399, #35089 ) ;
#43078=CARTESIAN_POINT ( 'NONE',  ( 4.556349186104045934, 11.00000000000000000, 98.21875000409679046 ) ) ;
#43079=CARTESIAN_POINT ( 'NONE',  ( -4.556349186104048599, -10.99999999999999822, 106.4687500040967763 ) ) ;
#43100=CARTESIAN_POINT ( 'NONE',  ( -6.735557395310442023E-16, 11.00000000000000000, 69.62499999999998579 ) ) ;
#43101=CARTESIAN_POINT ( 'NONE',  ( -10.18810118749999916, 4.220049686691934809, 103.9375000020483810 ) ) ;
#43107=CARTESIAN_POINT ( 'NONE',  ( 1.871523826299183495E-15, -10.18810118749999916, 71.40625000204836681 ) ) ;
#43108=EDGE_CURVE ( 'NONE', #69954, #55449, #21463, .T. ) ;
#43111=CARTESIAN_POINT ( 'NONE',  ( -7.204075437095967871, 7.204075437095967871, 116.9687500020483810 ) ) ;
#43114=ORIENTED_EDGE ( 'NONE', *, *, #19940, .F. ) ;
#43121=VECTOR ( 'NONE', #20162, 1000.000000000000000 ) ;
#43122=CARTESIAN_POINT ( 'NONE',  ( -10.18810118749999916, 4.220049686691934809, 117.4375000020483810 ) ) ;
#43136=ORIENTED_EDGE ( 'NONE', *, *, #65198, .T. ) ;
#43139=ORIENTED_EDGE ( 'NONE', *, *, #16525, .T. ) ;
#43140=CARTESIAN_POINT ( 'NONE',  ( 10.18810118750000093, -4.220049686691933033, 114.8125000020483668 ) ) ;
#43152=CARTESIAN_POINT ( 'NONE',  ( -4.556349186104045934, 11.00000000000000000, 87.90625000409677625 ) ) ;
#43179=DIRECTION ( 'NONE',  ( -1.000000000000000000, 0.000000000000000000, 0.000000000000000000 ) ) ;
#43183=CARTESIAN_POINT ( 'NONE',  ( -10.99999999999989164, -4.556349186104158733, 82.09375000000000000 ) ) ;
#43189=CARTESIAN_POINT ( 'NONE',  ( -7.204075437095965206, -7.204075437095968759, 96.34375000204836681 ) ) ;
#43190=CARTESIAN_POINT ( 'NONE',  ( -7.778174593052023411, 7.778174593052023411, 93.81250000000000000 ) ) ;
#43203=CARTESIAN_POINT ( 'NONE',  ( 10.18810118750000093, -4.220049686691933033, 86.68750000204838102 ) ) ;
#43206=ORIENTED_EDGE ( 'NONE', *, *, #36094, .F. ) ;
#43215=ORIENTED_EDGE ( 'NONE', *, *, #59179, .F. ) ;
#43217=CARTESIAN_POINT ( 'NONE',  ( 7.204075437095968759, -7.204075437095966983, 81.71875000204836681 ) ) ;
#43225=VECTOR ( 'NONE', #58272, 1000.000000000000000 ) ;
#43233=CARTESIAN_POINT ( 'NONE',  ( -10.99999999999999822, -4.556349186104053040, 76.09375000000000000 ) ) ;
#43253=CARTESIAN_POINT ( 'NONE',  ( 4.556349186104051263, -10.99999999999999822, 79.46874999999998579 ) ) ;
#43262=CIRCLE ( 'NONE', #20376, 38.34805510287551300 ) ;
#43280=CARTESIAN_POINT ( 'NONE',  ( 10.18810118750000093, -4.220049686691933921, 85.18750000204838102 ) ) ;
#43282=CARTESIAN_POINT ( 'NONE',  ( -4.220049686691935698, 10.18810118749999916, 113.8750000020483668 ) ) ;
#43296=CARTESIAN_POINT ( 'NONE',  ( -7.204075437095965206, -7.204075437095968759, 105.7187500020483810 ) ) ;
#43299=ORIENTED_EDGE ( 'NONE', *, *, #43607, .T. ) ;
#43311=EDGE_LOOP ( 'NONE', ( #70748, #47875, #63369, #9388, #67026 ) ) ;
#43331=CARTESIAN_POINT ( 'NONE',  ( 7.204075437095968759, -7.204075437095966983, 78.71875000204836681 ) ) ;
#43333=CARTESIAN_POINT ( 'NONE',  ( 11.00000000000000355, -4.556349186104045046, 97.65624999999998579 ) ) ;
#43351=CARTESIAN_POINT ( 'NONE',  ( 10.99999999999996270, -4.556349186104084126, 112.8437500040967620 ) ) ;
#43363=CARTESIAN_POINT ( 'NONE',  ( -4.556349186104045934, 11.00000000000000000, 81.90625000409676204 ) ) ;
#43380=CARTESIAN_POINT ( 'NONE',  ( 0.000000000000000000, 0.000000000000000000, 118.0000000000000000 ) ) ;
#43381=CARTESIAN_POINT ( 'NONE',  ( 10.18810118750000093, -4.220049686691933921, 74.31250000204836681 ) ) ;
#43385=CARTESIAN_POINT ( 'NONE',  ( 10.99999999999999467, 11.00000000000000355, 20.00000000000000000 ) ) ;
#43391=CARTESIAN_POINT ( 'NONE',  ( 10.18810118749999916, 1.247682550866122264E-15, 88.28125000204836681 ) ) ;
#43396=CARTESIAN_POINT ( 'NONE',  ( 4.220049686691941027, -10.18810118749999738, 93.62500000204838102 ) ) ;
#43398=ORIENTED_EDGE ( 'NONE', *, *, #41293, .T. ) ;
#43404=CARTESIAN_POINT ( 'NONE',  ( 1.871523826299183495E-15, -10.18810118749999916, 99.90625000204838102 ) ) ;
#43420=( BOUNDED_CURVE ( )  B_SPLINE_CURVE ( 2, ( #43722, #26354, #61075, #66736, #38822, #2990, #56177, #25612, #38076 ),
 .UNSPECIFIED., .F., .F. ) 
 B_SPLINE_CURVE_WITH_KNOTS ( ( 3, 2, 2, 2, 3 ),
 ( 0.5588235294117646079, 0.5624999999999998890, 0.5661764705882351700, 0.5698529411764704511, 0.5735294117647057321 ),
 .UNSPECIFIED. ) 
 CURVE ( )  GEOMETRIC_REPRESENTATION_ITEM ( )  RATIONAL_B_SPLINE_CURVE ( ( 1.000000000000002220, 0.9238795325112844070, 1.000000000000000000, 0.9238795325112867385, 1.000000000000000000, 0.9238795325112867385, 1.000000000000000000, 0.9238795325112890700, 0.9999999999999976685 ) ) 
 REPRESENTATION_ITEM ( '' )  );
#43422=CARTESIAN_POINT ( 'NONE',  ( 7.204075437095966983, 7.204075437095967871, 100.0937500020483668 ) ) ;
#43440=LINE ( 'NONE', #24603, #41544 ) ;
#43441=CARTESIAN_POINT ( 'NONE',  ( -7.778174593052023411, 7.778174593052023411, 110.3125000000000000 ) ) ;
#43445=CARTESIAN_POINT ( 'NONE',  ( -7.778174593052020747, -7.778174593052023411, 101.6874999999999858 ) ) ;
#43454=CARTESIAN_POINT ( 'NONE',  ( 11.00000000000000355, -4.556349186104045046, 97.84375000409676204 ) ) ;
#43478=CARTESIAN_POINT ( 'NONE',  ( -7.204075437095967871, 7.204075437095967871, 105.3437500020483810 ) ) ;
#43487=CARTESIAN_POINT ( 'NONE',  ( 4.220049686691941027, -10.18810118749999738, 113.1250000020483810 ) ) ;
#43496=CARTESIAN_POINT ( 'NONE',  ( 10.18810118750000093, -4.220049686691933921, 115.1875000020483668 ) ) ;
#43508=ORIENTED_EDGE ( 'NONE', *, *, #7424, .F. ) ;
#43538=VERTEX_POINT ( 'NONE', #1088 ) ;
#43563=CARTESIAN_POINT ( 'NONE',  ( -4.220049686691935698, 10.18810118749999916, 97.37500000204839523 ) ) ;
#43564=CARTESIAN_POINT ( 'NONE',  ( -11.00000000000000000, 0.000000000000000000, 93.99999999999998579 ) ) ;
#43569=CARTESIAN_POINT ( 'NONE',  ( 10.99999999999995026, -4.556349186104096560, 96.15625000000000000 ) ) ;
#43578=CARTESIAN_POINT ( 'NONE',  ( -7.204075437095965206, -7.204075437095968759, 89.21875000204838102 ) ) ;
#43592=CARTESIAN_POINT ( 'NONE',  ( 1.871523826299183495E-15, -10.18810118749999916, 81.53125000204838102 ) ) ;
#43602=VECTOR ( 'NONE', #50512, 1000.000000000000000 ) ;
#43607=EDGE_CURVE ( 'NONE', #38757, #50500, #42148, .T. ) ;
#43613=ADVANCED_FACE ( 'NONE', ( #53859 ), #26185, .T. ) ;
#43625=EDGE_CURVE ( 'NONE', #37130, #53484, #32306, .T. ) ;
#43626=ORIENTED_EDGE ( 'NONE', *, *, #40780, .F. ) ;
#43631=CARTESIAN_POINT ( 'NONE',  ( 7.778174593052023411, -7.778174593052021635, 73.56249999999998579 ) ) ;
#43637=CARTESIAN_POINT ( 'NONE',  ( -11.00000000000000000, 0.000000000000000000, 107.6875000040967763 ) ) ;
#43644=DIRECTION ( 'NONE',  ( -0.000000000000000000, -0.000000000000000000, -1.000000000000000000 ) ) ;
#43658=CARTESIAN_POINT ( 'NONE',  ( -10.18810118749999916, 0.000000000000000000, 86.03125000204836681 ) ) ;
#43659=CARTESIAN_POINT ( 'NONE',  ( 10.18810118749999916, 1.247682550866122264E-15, 110.4062500020483668 ) ) ;
#43674=CARTESIAN_POINT ( 'NONE',  ( -4.220049686691935698, 10.18810118749999916, 108.2500000020483810 ) ) ;
#43715=CARTESIAN_POINT ( 'NONE',  ( -4.220049686691937474, -10.18810118749999738, 82.93750000204838102 ) ) ;
#43718=CARTESIAN_POINT ( 'NONE',  ( 4.556349186104045934, 11.00000000000000000, 89.03124999999998579 ) ) ;
#43722=CARTESIAN_POINT ( 'NONE',  ( -11.00000000000000000, 0.000000000000000000, 89.50000000000000000 ) ) ;
#43746=CARTESIAN_POINT ( 'NONE',  ( -11.00000000000000000, 4.556349186104045934, 83.59375000409677625 ) ) ;
#43763=CARTESIAN_POINT ( 'NONE',  ( -10.18810118749999916, 4.220049686691934809, 76.56250000204836681 ) ) ;
#43771=CARTESIAN_POINT ( 'NONE',  ( 1.871523826299183495E-15, -10.18810118749999916, 86.40625000204838102 ) ) ;
#43778=CARTESIAN_POINT ( 'NONE',  ( 10.18810118749999916, 1.247682550866122264E-15, 93.90625000204836681 ) ) ;
#43781=ORIENTED_EDGE ( 'NONE', *, *, #60214, .F. ) ;
#43786=CARTESIAN_POINT ( 'NONE',  ( -7.204075437095967871, 7.204075437095967871, 94.84375000204838102 ) ) ;
#43806=CARTESIAN_POINT ( 'NONE',  ( 10.18810118749999916, 4.220049686691935698, 97.00000000204838102 ) ) ;
#43809=CARTESIAN_POINT ( 'NONE',  ( -7.778174593052020747, -7.778174593052023411, 106.1874999999999858 ) ) ;
#43823=CARTESIAN_POINT ( 'NONE',  ( 7.778174593052021635, 7.778174593052023411, 111.4375000000000000 ) ) ;
#43838=CARTESIAN_POINT ( 'NONE',  ( 4.556349186104051263, -10.99999999999999822, 96.15625000409677625 ) ) ;
#43841=CARTESIAN_POINT ( 'NONE',  ( 11.00000000000000000, 1.347111479062088405E-15, 117.2500000000000000 ) ) ;
#43860=CARTESIAN_POINT ( 'NONE',  ( 7.204075437095968759, -7.204075437095966983, 106.0937500020483810 ) ) ;
#43870=CARTESIAN_POINT ( 'NONE',  ( 4.220049686691941027, -10.18810118749999738, 116.1250000020483810 ) ) ;
#43878=CARTESIAN_POINT ( 'NONE',  ( -4.220049686691937474, -10.18810118749999738, 107.3125000020483668 ) ) ;
#43897=CARTESIAN_POINT ( 'NONE',  ( -10.18810118749999916, 0.000000000000000000, 115.6562500020483810 ) ) ;
#43910=DIRECTION ( 'NONE',  ( -0.000000000000000000, -0.000000000000000000, -1.000000000000000000 ) ) ;
#43912=CARTESIAN_POINT ( 'NONE',  ( 7.778174593052023411, -7.778174593052021635, 78.06249999999998579 ) ) ;
#43915=CARTESIAN_POINT ( 'NONE',  ( 11.00000000000000000, 1.347111479062088405E-15, 106.9375000040967763 ) ) ;
#43917=CARTESIAN_POINT ( 'NONE',  ( -4.556349186104048599, -10.99999999999999822, 110.7812500000000000 ) ) ;
#43948=CARTESIAN_POINT ( 'NONE',  ( 10.18810118749999916, 4.220049686691935698, 89.50000000204836681 ) ) ;
#43961=CARTESIAN_POINT ( 'NONE',  ( -6.238412754330611322E-16, 10.18810118749999916, 81.15625000204838102 ) ) ;
#43963=VERTEX_POINT ( 'NONE', #11093 ) ;
#43975=CARTESIAN_POINT ( 'NONE',  ( -6.238412754330611322E-16, 10.18810118749999916, 80.78125000204838102 ) ) ;
#43983=( BOUNDED_CURVE ( )  B_SPLINE_CURVE ( 2, ( #28116, #52623, #23571, #17916, #12251, #58299, #29610, #69978, #33806 ),
 .UNSPECIFIED., .F., .F. ) 
 B_SPLINE_CURVE_WITH_KNOTS ( ( 3, 2, 2, 2, 3 ),
 ( 0.4411764705882352811, 0.4448529411764705621, 0.4485294117647058987, 0.4522058823529411797, 0.4558823529411764608 ),
 .UNSPECIFIED. ) 
 CURVE ( )  GEOMETRIC_REPRESENTATION_ITEM ( )  RATIONAL_B_SPLINE_CURVE ( ( 1.000000000000000000, 0.9238795325112867385, 1.000000000000000000, 0.9238795325112867385, 1.000000000000000000, 0.9238795325112867385, 1.000000000000000000, 0.9238795325112867385, 1.000000000000000000 ) ) 
 REPRESENTATION_ITEM ( '' )  );
#43988=ORIENTED_EDGE ( 'NONE', *, *, #21242, .F. ) ;
#44012=CARTESIAN_POINT ( 'NONE',  ( 11.00000000000000000, 1.347111479062088405E-15, 69.24999999999997158 ) ) ;
#44022=CARTESIAN_POINT ( 'NONE',  ( -4.556349186104045934, 11.00000000000000000, 111.9062500040967763 ) ) ;
#44041=CARTESIAN_POINT ( 'NONE',  ( 7.204075437095968759, -7.204075437095966983, 116.2187500020483810 ) ) ;
#44044=DIRECTION ( 'NONE',  ( -0.000000000000000000, -1.000000000000000000, -0.000000000000000000 ) ) ;
#44045=CARTESIAN_POINT ( 'NONE',  ( -7.778174593052020747, -7.778174593052023411, 106.1874999999999858 ) ) ;
#44055=CARTESIAN_POINT ( 'NONE',  ( -4.220049686691935698, 10.18810118749999916, 100.7500000020483810 ) ) ;
#44065=CARTESIAN_POINT ( 'NONE',  ( -7.778174593052020747, -7.778174593052023411, 71.87500000409677625 ) ) ;
#44070=EDGE_CURVE ( 'NONE', #53323, #40937, #2135, .T. ) ;
#44076=EDGE_CURVE ( 'NONE', #8408, #43538, #30552, .T. ) ;
#44098=CARTESIAN_POINT ( 'NONE',  ( -4.220049686691935698, 10.18810118749999916, 80.87500000204836681 ) ) ;
#44100=PLANE ( 'NONE',  #27606 ) ;
#44101=CARTESIAN_POINT ( 'NONE',  ( 7.778174593052023411, -7.778174593052021635, 90.06249999999998579 ) ) ;
#44125=CARTESIAN_POINT ( 'NONE',  ( 11.00000000000006573, 4.556349186103981097, 111.5312500040967620 ) ) ;
#44130=CARTESIAN_POINT ( 'NONE',  ( -6.735557395310442023E-16, 11.00000000000000000, 83.31250000409676204 ) ) ;
#44137=CARTESIAN_POINT ( 'NONE',  ( -11.00000000000005151, 4.556349186103993532, 98.59375000409677625 ) ) ;
#44145=CARTESIAN_POINT ( 'NONE',  ( -10.18810118749999916, 4.220049686691934809, 75.06250000204836681 ) ) ;
#44152=CARTESIAN_POINT ( 'NONE',  ( 10.18810118749999916, 4.220049686691935698, 83.87500000204835260 ) ) ;
#44158=CARTESIAN_POINT ( 'NONE',  ( 10.18810118750000093, -4.220049686691933921, 93.81250000204839523 ) ) ;
#44166=CARTESIAN_POINT ( 'NONE',  ( -4.220049686691937474, -10.18810118749999738, 90.81250000204838102 ) ) ;
#44183=CARTESIAN_POINT ( 'NONE',  ( 7.204075437095966983, 7.204075437095967871, 98.59375000204836681 ) ) ;
#44186=CARTESIAN_POINT ( 'NONE',  ( -7.778174593052020747, -7.778174593052023411, 109.1875000000000000 ) ) ;
#44218=CARTESIAN_POINT ( 'NONE',  ( -4.556349186104047710, -10.99999999999999822, 100.4687500040967763 ) ) ;
#44219=CARTESIAN_POINT ( 'NONE',  ( 11.00000000000000000, 1.347111479062088405E-15, 106.9375000040967763 ) ) ;
#44241=CARTESIAN_POINT ( 'NONE',  ( 11.00000000000000355, -4.556349186104044158, 70.84375000409676204 ) ) ;
#44242=CARTESIAN_POINT ( 'NONE',  ( -7.204075437095965206, -7.204075437095968759, 101.2187500020483668 ) ) ;
#44252=CARTESIAN_POINT ( 'NONE',  ( 10.18810118750000093, -4.220049686691933921, 113.3125000020483668 ) ) ;
#44261=CARTESIAN_POINT ( 'NONE',  ( -10.18810118749999916, 4.220049686691934809, 111.4375000020483810 ) ) ;
#44268=CARTESIAN_POINT ( 'NONE',  ( -10.18810118749999916, 0.000000000000000000, 71.03125000204838102 ) ) ;
#44272=ORIENTED_EDGE ( 'NONE', *, *, #8899, .F. ) ;
#44273=CARTESIAN_POINT ( 'NONE',  ( -6.735557395310442023E-16, 11.00000000000000000, 90.62499999999998579 ) ) ;
#44275=CARTESIAN_POINT ( 'NONE',  ( 1.871523826299183495E-15, -10.18810118749999916, 114.5312500020483810 ) ) ;
#44287=LINE ( 'NONE', #54871, #56319 ) ;
#44288=LINE ( 'NONE', #26543, #58012 ) ;
#44301=CARTESIAN_POINT ( 'NONE',  ( 4.556349186104045934, 11.00000000000000000, 77.21875000409679046 ) ) ;
#44302=VECTOR ( 'NONE', #27714, 1000.000000000000000 ) ;
#44305=CARTESIAN_POINT ( 'NONE',  ( 4.556349186104052151, -10.99999999999999822, 79.46874999999998579 ) ) ;
#44320=CARTESIAN_POINT ( 'NONE',  ( 7.778174593052021635, 7.778174593052023411, 94.93750000000000000 ) ) ;
#44324=CARTESIAN_POINT ( 'NONE',  ( -10.18810118749999916, 4.220049686691934809, 90.06250000204838102 ) ) ;
#44337=CARTESIAN_POINT ( 'NONE',  ( -7.204075437095967871, 7.204075437095967871, 85.84375000204836681 ) ) ;
#44344=CARTESIAN_POINT ( 'NONE',  ( 4.556349186104052151, -10.99999999999999822, 85.65625000409679046 ) ) ;
#44352=CARTESIAN_POINT ( 'NONE',  ( -6.238412754330611322E-16, 10.18810118749999916, 79.28125000204836681 ) ) ;
#44385=CARTESIAN_POINT ( 'NONE',  ( 11.00000000000000000, 4.556349186104045934, 72.34374999999998579 ) ) ;
#44390=EDGE_CURVE ( 'NONE', #54736, #13039, #3309, .T. ) ;
#44392=CARTESIAN_POINT ( 'NONE',  ( -11.00000000000002842, -4.556349186104018401, 113.7812500040967478 ) ) ;
#44404=CARTESIAN_POINT ( 'NONE',  ( 11.00000000000000000, 4.556349186104045934, 81.34374999999997158 ) ) ;
#44412=CARTESIAN_POINT ( 'NONE',  ( 7.204075437095968759, -7.204075437095966983, 105.7187500020483810 ) ) ;
#44425=CARTESIAN_POINT ( 'NONE',  ( -10.18810118749999738, -4.220049686691941915, 99.62500000204838102 ) ) ;
#44440=VECTOR ( 'NONE', #49384, 1000.000000000000000 ) ;
#44449=CARTESIAN_POINT ( 'NONE',  ( 4.220049686691934809, 10.18810118749999916, 82.56250000204836681 ) ) ;
#44467=CARTESIAN_POINT ( 'NONE',  ( 7.204075437095968759, -7.204075437095966983, 72.71875000204838102 ) ) ;
#44470=CARTESIAN_POINT ( 'NONE',  ( 7.778174593052021635, 7.778174593052023411, 90.43749999999998579 ) ) ;
#44494=VERTEX_POINT ( 'NONE', #8966 ) ;
#44498=CARTESIAN_POINT ( 'NONE',  ( 7.778174593052021635, 7.778174593052023411, 74.12500000409677625 ) ) ;
#44504=EDGE_CURVE ( 'NONE', #58573, #3255, #67430, .T. ) ;
#44506=CARTESIAN_POINT ( 'NONE',  ( 11.00000000000000000, 1.347111479062088405E-15, 69.24999999999997158 ) ) ;
#44515=CARTESIAN_POINT ( 'NONE',  ( -7.204075437095967871, 7.204075437095967871, 74.96875000204836681 ) ) ;
#44517=DIRECTION ( 'NONE',  ( -1.000000000000000000, 0.000000000000000000, 0.000000000000000000 ) ) ;
#44523=CARTESIAN_POINT ( 'NONE',  ( -7.204075437095967871, 7.204075437095967871, 81.34375000204838102 ) ) ;
#44530=EDGE_CURVE ( 'NONE', #56060, #45292, #74409, .T. ) ;
#44538=CARTESIAN_POINT ( 'NONE',  ( -4.220049686691935698, 10.18810118749999916, 91.75000000204836681 ) ) ;
#44542=( BOUNDED_CURVE ( )  B_SPLINE_CURVE ( 2, ( #64541, #30205, #6094, #59258, #47177, #7570, #58521, #47912, #24895 ),
 .UNSPECIFIED., .F., .F. ) 
 B_SPLINE_CURVE_WITH_KNOTS ( ( 3, 2, 2, 2, 3 ),
 ( 0.3235294117647058432, 0.3272058823529411242, 0.3308823529411764053, 0.3345588235294116863, 0.3382352941176470229 ),
 .UNSPECIFIED. ) 
 CURVE ( )  GEOMETRIC_REPRESENTATION_ITEM ( )  RATIONAL_B_SPLINE_CURVE ( ( 1.000000000000001110, 0.9238795325112856283, 1.000000000000000000, 0.9238795325112867385, 1.000000000000000000, 0.9238795325112867385, 1.000000000000000000, 0.9238795325112878487, 0.9999999999999988898 ) ) 
 REPRESENTATION_ITEM ( '' )  );
#44556=CARTESIAN_POINT ( 'NONE',  ( -10.18810118749999738, -4.220049686691941915, 91.75000000204836681 ) ) ;
#44559=CARTESIAN_POINT ( 'NONE',  ( 2.020667218593132706E-15, -11.00000000000000000, 109.3750000000000000 ) ) ;
#44575=CARTESIAN_POINT ( 'NONE',  ( 10.99999999999999467, 11.00000000000000355, 20.00000000000000000 ) ) ;
#44578=CARTESIAN_POINT ( 'NONE',  ( -10.18810118749999916, 0.000000000000000000, 117.5312500020483810 ) ) ;
#44581=EDGE_CURVE ( 'NONE', #69418, #40106, #15117, .T. ) ;
#44591=CARTESIAN_POINT ( 'NONE',  ( -11.00000000000000000, 0.000000000000000000, 100.1875000040967763 ) ) ;
#44611=CARTESIAN_POINT ( 'NONE',  ( -10.18810118749999916, 4.220049686691934809, 105.4375000020483668 ) ) ;
#44621=CARTESIAN_POINT ( 'NONE',  ( -7.204075437095967871, 7.204075437095967871, 112.4687500020483810 ) ) ;
#44629=CARTESIAN_POINT ( 'NONE',  ( 4.220049686691941027, -10.18810118749999738, 110.5000000020483810 ) ) ;
#44638=CARTESIAN_POINT ( 'NONE',  ( 2.729893485599593106, 10.18810118750000093, 67.59560438569886287 ) ) ;
#44643=CARTESIAN_POINT ( 'NONE',  ( -7.778174593052023411, 7.778174593052023411, 90.81249999999998579 ) ) ;
#44645=CARTESIAN_POINT ( 'NONE',  ( -10.18810118749999916, 0.000000000000000000, 111.1562500020483668 ) ) ;
#44663=CARTESIAN_POINT ( 'NONE',  ( -10.99999999999991829, 4.556349186104124982, 107.5937500040967336 ) ) ;
#44695=CARTESIAN_POINT ( 'NONE',  ( 10.18810118749999916, 1.247682550866122264E-15, 89.40625000204838102 ) ) ;
#44701=CARTESIAN_POINT ( 'NONE',  ( -4.556349186104048599, -10.99999999999999822, 95.78124999999998579 ) ) ;
#44708=CARTESIAN_POINT ( 'NONE',  ( 7.204075437095968759, -7.204075437095966983, 82.09375000204838102 ) ) ;
#44714=VECTOR ( 'NONE', #22379, 1000.000000000000000 ) ;
#44715=CARTESIAN_POINT ( 'NONE',  ( 11.00000000000010836, -4.556349186103939353, 85.84375000409677625 ) ) ;
#44722=CARTESIAN_POINT ( 'NONE',  ( -7.204075437095965206, -7.204075437095968759, 76.84375000204838102 ) ) ;
#44755=CARTESIAN_POINT ( 'NONE',  ( -11.00000000000000000, 0.000000000000000000, 115.1875000040967763 ) ) ;
#44760=CARTESIAN_POINT ( 'NONE',  ( 11.00000000000000355, -4.556349186104045046, 72.15624999999997158 ) ) ;
#44782=VECTOR ( 'NONE', #12928, 1000.000000000000000 ) ;
#44784=ORIENTED_EDGE ( 'NONE', *, *, #18185, .T. ) ;
#44786=CARTESIAN_POINT ( 'NONE',  ( 4.220049686691941027, -10.18810118749999738, 105.6250000020483668 ) ) ;
#44799=CARTESIAN_POINT ( 'NONE',  ( -4.220049686691937474, -10.18810118749999738, 101.3125000020483810 ) ) ;
#44801=ORIENTED_EDGE ( 'NONE', *, *, #64767, .T. ) ;
#44819=CARTESIAN_POINT ( 'NONE',  ( -10.18810118749999916, 0.000000000000000000, 80.03125000204836681 ) ) ;
#44820=ORIENTED_EDGE ( 'NONE', *, *, #56766, .F. ) ;
#44834=VECTOR ( 'NONE', #29665, 1000.000000000000000 ) ;
#44836=EDGE_CURVE ( 'NONE', #9385, #17249, #30768, .T. ) ;
#44841=CARTESIAN_POINT ( 'NONE',  ( 7.204075437095966983, 7.204075437095967871, 74.59375000204838102 ) ) ;
#44844=CARTESIAN_POINT ( 'NONE',  ( 4.556349186104051263, -10.99999999999999822, 89.96875000000000000 ) ) ;
#44873=CARTESIAN_POINT ( 'NONE',  ( 11.00000000000000355, -4.556349186104045046, 72.34375000409679046 ) ) ;
#44880=CARTESIAN_POINT ( 'NONE',  ( 11.00000000000000000, 1.347111479062088405E-15, 97.93750000409677625 ) ) ;
#44888=CARTESIAN_POINT ( 'NONE',  ( 7.204075437095968759, -7.204075437095966983, 116.5937500020483810 ) ) ;
#44892=CARTESIAN_POINT ( 'NONE',  ( 4.220049686691934809, 10.18810118749999916, 70.18750000204838102 ) ) ;
#44900=CARTESIAN_POINT ( 'NONE',  ( 4.220049686691934809, 10.18810118749999916, 79.56250000204836681 ) ) ;
#44913=CARTESIAN_POINT ( 'NONE',  ( -7.204075437095967871, 7.204075437095967871, 90.34375000204838102 ) ) ;
#44930=CARTESIAN_POINT ( 'NONE',  ( -4.220049686691935698, 10.18810118749999916, 91.37500000204838102 ) ) ;
#44933=CARTESIAN_POINT ( 'NONE',  ( -10.99999999999999822, -4.556349186104052151, 107.5937499999999858 ) ) ;
#44937=AXIS2_PLACEMENT_3D ( 'NONE', #38603, #60476, #32575 ) ;
#44963=CARTESIAN_POINT ( 'NONE',  ( 7.778174593052023411, -7.778174593052021635, 90.25000000409677625 ) ) ;
#44984=CARTESIAN_POINT ( 'NONE',  ( -4.220049686691935698, 10.18810118749999916, 99.25000000204838102 ) ) ;
#44985=ORIENTED_EDGE ( 'NONE', *, *, #46321, .T. ) ;
#44994=CARTESIAN_POINT ( 'NONE',  ( -4.220049686691937474, -10.18810118749999738, 114.4375000020483668 ) ) ;
#45004=CARTESIAN_POINT ( 'NONE',  ( -4.220049686691935698, 10.18810118749999916, 111.2500000020483952 ) ) ;
#45015=CARTESIAN_POINT ( 'NONE',  ( 10.99999999999999645, -10.99999999999999645, 20.00000000000000000 ) ) ;
#45021=CARTESIAN_POINT ( 'NONE',  ( -6.238412754330611322E-16, 10.18810118749999916, 107.7812500020483810 ) ) ;
#45058=ORIENTED_EDGE ( 'NONE', *, *, #19001, .F. ) ;
#45067=CARTESIAN_POINT ( 'NONE',  ( -10.18810118749999738, -4.220049686691941915, 88.75000000204836681 ) ) ;
#45071=CARTESIAN_POINT ( 'NONE',  ( 11.00000000000000000, 1.347111479062088405E-15, 117.4999999999999716 ) ) ;
#45079=CARTESIAN_POINT ( 'NONE',  ( -4.220049686691937474, -10.18810118749999738, 81.81250000204838102 ) ) ;
#45091=CARTESIAN_POINT ( 'NONE',  ( -10.18810118749999738, -4.220049686691941915, 79.75000000204838102 ) ) ;
#45106=CARTESIAN_POINT ( 'NONE',  ( 11.00000000000000000, 1.347111479062088405E-15, 73.93750000409676204 ) ) ;
#45112=CARTESIAN_POINT ( 'NONE',  ( -7.778174593052023411, 7.778174593052023411, 74.50000000409676204 ) ) ;
#45117=AXIS2_PLACEMENT_3D ( 'NONE', #46397, #47496, #70519 ) ;
#45144=ORIENTED_EDGE ( 'NONE', *, *, #20434, .T. ) ;
#45153=CARTESIAN_POINT ( 'NONE',  ( -6.238412754330611322E-16, 10.18810118749999916, 104.7812500020483810 ) ) ;
#45171=CARTESIAN_POINT ( 'NONE',  ( -4.220049686691935698, 10.18810118749999916, 102.2500000020483810 ) ) ;
#45190=CARTESIAN_POINT ( 'NONE',  ( 10.18810118750000093, -4.220049686691933921, 79.18750000204836681 ) ) ;
#45196=CARTESIAN_POINT ( 'NONE',  ( 0.000000000000000000, 0.000000000000000000, 118.0000000000000000 ) ) ;
#45209=CARTESIAN_POINT ( 'NONE',  ( -7.204075437095965206, -7.204075437095968759, 73.84375000204838102 ) ) ;
#45212=CARTESIAN_POINT ( 'NONE',  ( -7.778174593052023411, 7.778174593052023411, 86.31249999999998579 ) ) ;
#45221=ORIENTED_EDGE ( 'NONE', *, *, #3523, .T. ) ;
#45240=CARTESIAN_POINT ( 'NONE',  ( -4.556349186104045934, 11.00000000000000000, 74.40625000409676204 ) ) ;
#45257=CARTESIAN_POINT ( 'NONE',  ( 10.18810118749999916, 4.220049686691935698, 68.50000000204838102 ) ) ;
#45268=CARTESIAN_POINT ( 'NONE',  ( 10.18810118750000093, -4.220049686691933921, 77.68750000204838102 ) ) ;
#45287=CARTESIAN_POINT ( 'NONE',  ( 4.556349186104045934, 11.00000000000000000, 78.71875000409676204 ) ) ;
#45292=VERTEX_POINT ( 'NONE', #33030 ) ;
#45293=CARTESIAN_POINT ( 'NONE',  ( 1.871523826299183495E-15, -10.18810118749999916, 95.03125000204836681 ) ) ;
#45295=CARTESIAN_POINT ( 'NONE',  ( 11.00000000000000000, 4.556349186104045934, 108.3437499999999858 ) ) ;
#45297=DIRECTION ( 'NONE',  ( -1.000000000000000000, 0.000000000000000000, 0.000000000000000000 ) ) ;
#45324=CARTESIAN_POINT ( 'NONE',  ( -7.778174593052023411, 7.778174593052023411, 94.00000000409677625 ) ) ;
#45337=CARTESIAN_POINT ( 'NONE',  ( 11.00000000000000000, 1.347111479062088405E-15, 79.74999999999998579 ) ) ;
#45338=ORIENTED_EDGE ( 'NONE', *, *, #24483, .F. ) ;
#45345=EDGE_CURVE ( 'NONE', #22788, #30828, #1705, .T. ) ;
#45347=CARTESIAN_POINT ( 'NONE',  ( -10.18810118749999916, 4.220049686691934809, 97.93750000204836681 ) ) ;
#45356=CARTESIAN_POINT ( 'NONE',  ( 4.220049686691934809, 10.18810118749999916, 104.6875000020483810 ) ) ;
#45364=CARTESIAN_POINT ( 'NONE',  ( 7.204075437095968759, -7.204075437095966983, 107.5937500020483810 ) ) ;
#45379=CARTESIAN_POINT ( 'NONE',  ( -4.220049686691937474, -10.18810118749999738, 111.4375000020483810 ) ) ;
#45390=CARTESIAN_POINT ( 'NONE',  ( -11.00000000000000000, 0.000000000000000000, 91.00000000000000000 ) ) ;
#45401=VERTEX_POINT ( 'NONE', #67529 ) ;
#45404=CARTESIAN_POINT ( 'NONE',  ( 7.778174593052021635, 7.778174593052023411, 110.1250000040967763 ) ) ;
#45427=CARTESIAN_POINT ( 'NONE',  ( -7.204075437095967871, 7.204075437095967871, 89.96875000204838102 ) ) ;
#45431=ORIENTED_EDGE ( 'NONE', *, *, #30340, .T. ) ;
#45433=CARTESIAN_POINT ( 'NONE',  ( 10.18810118749999916, 4.220049686691935698, 113.8750000020483668 ) ) ;
#45435=ADVANCED_FACE ( 'NONE', ( #61117 ), #15083, .T. ) ;
#45441=CARTESIAN_POINT ( 'NONE',  ( 10.18810118749999916, 4.220049686691935698, 85.37500000204838102 ) ) ;
#45452=CARTESIAN_POINT ( 'NONE',  ( 7.204075437095966983, 7.204075437095967871, 76.09375000204838102 ) ) ;
#45494=ADVANCED_FACE ( 'NONE', ( #55471 ), #32841, .T. ) ;
#45508=ADVANCED_FACE ( 'NONE', ( #50540 ), #54729, .T. ) ;
#45517=CARTESIAN_POINT ( 'NONE',  ( 10.18810118750000093, -4.220049686691933921, 108.8125000020484094 ) ) ;
#45534=CARTESIAN_POINT ( 'NONE',  ( 7.204075437095968759, -7.204075437095966983, 98.59375000204836681 ) ) ;
#45547=CARTESIAN_POINT ( 'NONE',  ( 7.204075437095966983, 7.204075437095967871, 95.59375000204836681 ) ) ;
#45560=CARTESIAN_POINT ( 'NONE',  ( 10.18810118750000093, -4.220049686691933921, 83.68750000204836681 ) ) ;
#45571=SHAPE_DEFINITION_REPRESENTATION ( #40948, #20419 ) ;
#45578=CARTESIAN_POINT ( 'NONE',  ( 10.18810118749999916, 1.247682550866122264E-15, 75.90625000204836681 ) ) ;
#45581=CARTESIAN_POINT ( 'NONE',  ( -6.735557395310442023E-16, 11.00000000000000000, 86.12499999999998579 ) ) ;
#45608=CARTESIAN_POINT ( 'NONE',  ( 11.00000000000000000, 4.556349186104045934, 75.53125000409676204 ) ) ;
#45624=ORIENTED_EDGE ( 'NONE', *, *, #16283, .F. ) ;
#45626=CARTESIAN_POINT ( 'NONE',  ( 1.871523826299183495E-15, -10.18810118749999916, 74.03125000204836681 ) ) ;
#45640=ORIENTED_EDGE ( 'NONE', *, *, #16441, .T. ) ;
#45661=CARTESIAN_POINT ( 'NONE',  ( 10.18810118749999916, 1.247682550866122264E-15, 95.40625000204836681 ) ) ;
#45664=CARTESIAN_POINT ( 'NONE',  ( -11.00000000000000000, 4.556349186104045934, 99.90624999999998579 ) ) ;
#45667=CARTESIAN_POINT ( 'NONE',  ( 11.00000000000000000, 1.347111479062088405E-15, 112.9375000040967763 ) ) ;
#45671=CARTESIAN_POINT ( 'NONE',  ( 11.00000000000010836, -4.556349186103939353, 87.34375000409679046 ) ) ;
#45693=CARTESIAN_POINT ( 'NONE',  ( -6.735557395310442023E-16, 11.00000000000000000, 95.31250000409677625 ) ) ;
#45718=CARTESIAN_POINT ( 'NONE',  ( 7.204075437095968759, -7.204075437095966983, 100.0937500020483668 ) ) ;
#45725=CARTESIAN_POINT ( 'NONE',  ( -7.204075437095965206, -7.204075437095968759, 109.8437500020483810 ) ) ;
#45733=CARTESIAN_POINT ( 'NONE',  ( 7.204075437095966983, 7.204075437095967871, 106.4687500020483810 ) ) ;
#45753=CARTESIAN_POINT ( 'NONE',  ( 10.18810118750000093, -4.220049686691933033, 110.3125000020483810 ) ) ;
#45770=CARTESIAN_POINT ( 'NONE',  ( 11.00000000000000000, 1.347111479062088405E-15, 91.93750000409677625 ) ) ;
#45771=CARTESIAN_POINT ( 'NONE',  ( -10.18810118749999916, 4.220049686691934809, 69.43750000204838102 ) ) ;
#45776=CARTESIAN_POINT ( 'NONE',  ( 2.020667218593132706E-15, -11.00000000000000000, 97.56250000409677625 ) ) ;
#45782=CARTESIAN_POINT ( 'NONE',  ( -11.00000000000000000, 4.556349186104045934, 112.0937500040967905 ) ) ;
#45788=LINE ( 'NONE', #33373, #2464 ) ;
#45803=CARTESIAN_POINT ( 'NONE',  ( -10.18810118749999916, 4.220049686691934809, 85.56250000204838102 ) ) ;
#45807=CARTESIAN_POINT ( 'NONE',  ( 10.18810118750000093, -4.220049686691933921, 116.6875000020483952 ) ) ;
#45815=CARTESIAN_POINT ( 'NONE',  ( 10.18810118750000093, -4.220049686691933033, 74.68750000204838102 ) ) ;
#45817=ORIENTED_EDGE ( 'NONE', *, *, #59303, .F. ) ;
#45818=CARTESIAN_POINT ( 'NONE',  ( 3.469446951953614189E-15, -11.00000000000000000, 41.99999999999999289 ) ) ;
#45826=LINE ( 'NONE', #68837, #6402 ) ;
#45829=CARTESIAN_POINT ( 'NONE',  ( 1.871523826299183495E-15, -10.18810118749999916, 72.53125000204838102 ) ) ;
#45838=CARTESIAN_POINT ( 'NONE',  ( -10.99999999999989164, -4.556349186104158733, 74.78125000409679046 ) ) ;
#45850=AXIS2_PLACEMENT_3D ( 'NONE', #52437, #58111, #23387 ) ;
#45865=CARTESIAN_POINT ( 'NONE',  ( -10.99999999999984368, 4.556349186104204030, 107.4062500000000000 ) ) ;
#45893=CARTESIAN_POINT ( 'NONE',  ( -6.238412754330611322E-16, 10.18810118749999916, 109.2812500020483668 ) ) ;
#45897=CARTESIAN_POINT ( 'NONE',  ( 11.00000000000000355, -4.556349186104044158, 97.65624999999998579 ) ) ;
#45910=CARTESIAN_POINT ( 'NONE',  ( 10.18810118749999916, 1.247682550866122264E-15, 94.28125000204836681 ) ) ;
#45920=ORIENTED_EDGE ( 'NONE', *, *, #44581, .F. ) ;
#45923=CARTESIAN_POINT ( 'NONE',  ( 10.18810118749999916, 4.220049686691935698, 95.50000000204838102 ) ) ;
#45934=CARTESIAN_POINT ( 'NONE',  ( 4.220049686691941027, -10.18810118749999738, 80.50000000204839523 ) ) ;
#45954=CARTESIAN_POINT ( 'NONE',  ( -7.778174593052020747, -7.778174593052023411, 80.68750000000000000 ) ) ;
#45969=CARTESIAN_POINT ( 'NONE',  ( 0.000000000000000000, 0.000000000000000000, 118.0000000000000000 ) ) ;
#45982=CARTESIAN_POINT ( 'NONE',  ( -11.00000000000000000, 4.556349186104045934, 76.09375000409676204 ) ) ;
#45995=CARTESIAN_POINT ( 'NONE',  ( -4.220049686691937474, -10.18810118749999738, 116.3125000020483810 ) ) ;
#45999=CARTESIAN_POINT ( 'NONE',  ( 10.18810118749999916, 4.220049686691935698, 71.50000000204839523 ) ) ;
#46035=CARTESIAN_POINT ( 'NONE',  ( 1.871523826299183495E-15, -10.18810118749999916, 92.03125000204836681 ) ) ;
#46038=CARTESIAN_POINT ( 'NONE',  ( 11.00000000000000355, -4.556349186104045046, 102.1562499999999858 ) ) ;
#46063=VERTEX_POINT ( 'NONE', #21037 ) ;
#46066=CARTESIAN_POINT ( 'NONE',  ( 4.556349186104045934, 11.00000000000000000, 92.21875000409677625 ) ) ;
#46089=CARTESIAN_POINT ( 'NONE',  ( 10.18810118749999916, 1.247682550866122264E-15, 95.78125000204836681 ) ) ;
#46098=CARTESIAN_POINT ( 'NONE',  ( 10.18810118749999916, 1.247682550866122264E-15, 108.9062500020483668 ) ) ;
#46107=CARTESIAN_POINT ( 'NONE',  ( 11.00000000000000000, 1.347111479062088405E-15, 96.24999999999998579 ) ) ;
#46108=CARTESIAN_POINT ( 'NONE',  ( 7.204075437095968759, -7.204075437095966983, 103.0937500020483668 ) ) ;
#46124=CARTESIAN_POINT ( 'NONE',  ( -10.18810118749999916, 0.000000000000000000, 108.1562500020483668 ) ) ;
#46125=CARTESIAN_POINT ( 'NONE',  ( 2.020667218593132706E-15, -11.00000000000000000, 103.3750000000000000 ) ) ;
#46141=CARTESIAN_POINT ( 'NONE',  ( 4.556349186104045934, 11.00000000000000000, 72.71875000409677625 ) ) ;
#46142=CARTESIAN_POINT ( 'NONE',  ( 10.18810118750000093, -4.220049686691933921, 68.68750000204836681 ) ) ;
#46148=DIRECTION ( 'NONE',  ( 0.000000000000000000, -0.000000000000000000, -1.000000000000000000 ) ) ;
#46149=CARTESIAN_POINT ( 'NONE',  ( 0.000000000000000000, 0.000000000000000000, 118.0000000000000000 ) ) ;
#46153=CARTESIAN_POINT ( 'NONE',  ( 11.00000000000000000, 1.347111479062088405E-15, 111.4375000040967763 ) ) ;
#46155=CARTESIAN_POINT ( 'NONE',  ( 2.020667218593132706E-15, -11.00000000000000000, 70.37500000000000000 ) ) ;
#46175=CARTESIAN_POINT ( 'NONE',  ( -7.204075437095967871, 7.204075437095967871, 82.46875000204836681 ) ) ;
#46178=CARTESIAN_POINT ( 'NONE',  ( -10.99999999999994849, 4.556349186104097448, 113.4062500000000000 ) ) ;
#46179=CARTESIAN_POINT ( 'NONE',  ( 10.18810118749999916, 1.247682550866122264E-15, 116.7812500020483810 ) ) ;
#46186=CARTESIAN_POINT ( 'NONE',  ( -4.220049686691935698, 10.18810118749999916, 79.75000000204838102 ) ) ;
#46189=CARTESIAN_POINT ( 'NONE',  ( -7.778174593052020747, -7.778174593052023411, 94.37500000409677625 ) ) ;
#46203=CARTESIAN_POINT ( 'NONE',  ( -10.18810118749999916, 0.000000000000000000, 70.65625000204836681 ) ) ;
#46217=ORIENTED_EDGE ( 'NONE', *, *, #29166, .T. ) ;
#46238=CARTESIAN_POINT ( 'NONE',  ( -4.556349186104045934, 11.00000000000000000, 68.21875000000000000 ) ) ;
#46264=CARTESIAN_POINT ( 'NONE',  ( 1.871523826299183495E-15, -10.18810118749999916, 104.0312500020483810 ) ) ;
#46280=CARTESIAN_POINT ( 'NONE',  ( -10.18810118749999916, 4.220049686691934809, 96.43750000204836681 ) ) ;
#46282=VERTEX_POINT ( 'NONE', #7725 ) ;
#46293=CARTESIAN_POINT ( 'NONE',  ( 7.204075437095968759, -7.204075437095966983, 87.71875000204836681 ) ) ;
#46304=CARTESIAN_POINT ( 'NONE',  ( 1.871523826299183495E-15, -10.18810118749999916, 72.90625000204836681 ) ) ;
#46317=CARTESIAN_POINT ( 'NONE',  ( -11.00000000000000000, 0.000000000000000000, 88.18750000409677625 ) ) ;
#46321=EDGE_CURVE ( 'NONE', #2485, #56146, #68671, .T. ) ;
#46324=CARTESIAN_POINT ( 'NONE',  ( 10.18810118749999916, 1.247682550866122264E-15, 68.40625000204836681 ) ) ;
#46327=CARTESIAN_POINT ( 'NONE',  ( 4.556349186104051263, -10.99999999999999822, 83.96874999999997158 ) ) ;
#46353=CARTESIAN_POINT ( 'NONE',  ( 11.00000000000000355, -4.556349186104045046, 67.84375000409677625 ) ) ;
#46358=VECTOR ( 'NONE', #37431, 1000.000000000000000 ) ;
#46365=CARTESIAN_POINT ( 'NONE',  ( -6.735557395310442023E-16, 11.00000000000000000, 108.6250000000000000 ) ) ;
#46368=CARTESIAN_POINT ( 'NONE',  ( 7.204075437095968759, -7.204075437095966983, 115.0937500020483810 ) ) ;
#46372=CARTESIAN_POINT ( 'NONE',  ( -4.220049686691935698, 10.18810118749999916, 73.37500000204838102 ) ) ;
#46389=EDGE_CURVE ( 'NONE', #42214, #20382, #55619, .T. ) ;
#46397=CARTESIAN_POINT ( 'NONE',  ( 0.000000000000000000, 0.000000000000000000, 118.0000000000000000 ) ) ;
#46400=( BOUNDED_CURVE ( )  B_SPLINE_CURVE ( 2, ( #32680, #55311, #3619, #55688, #40924, #5116, #28484, #10760, #17906 ),
 .UNSPECIFIED., .F., .F. ) 
 B_SPLINE_CURVE_WITH_KNOTS ( ( 3, 2, 2, 2, 3 ),
 ( 0.1470588235294118806, 0.1507352941176471617, 0.1544117647058824705, 0.1580882352941177238, 0.1617647058823530326 ),
 .UNSPECIFIED. ) 
 CURVE ( )  GEOMETRIC_REPRESENTATION_ITEM ( )  RATIONAL_B_SPLINE_CURVE ( ( 0.9999999999999976685, 0.9238795325112890700, 1.000000000000000000, 0.9238795325112867385, 1.000000000000000000, 0.9238795325112867385, 1.000000000000000000, 0.9238795325112849621, 1.000000000000001776 ) ) 
 REPRESENTATION_ITEM ( '' )  );
#46401=CARTESIAN_POINT ( 'NONE',  ( 11.00000000000000000, 1.347111479062088405E-15, 78.43750000409677625 ) ) ;
#46408=ORIENTED_EDGE ( 'NONE', *, *, #47285, .F. ) ;
#46409=CARTESIAN_POINT ( 'NONE',  ( -10.18810118749999916, 4.220049686691934809, 85.56250000204838102 ) ) ;
#46412=CARTESIAN_POINT ( 'NONE',  ( -10.99999999999999822, -4.556349186104052151, 98.59375000000000000 ) ) ;
#46421=( BOUNDED_CURVE ( )  B_SPLINE_CURVE ( 2, ( #26451, #38172, #72495, #67588, #61175, #15884, #43823, #4588, #11356 ),
 .UNSPECIFIED., .F., .F. ) 
 B_SPLINE_CURVE_WITH_KNOTS ( ( 3, 2, 2, 2, 3 ),
 ( 0.1176470588235294934, 0.1213235294117648022, 0.1250000000000001110, 0.1286764705882353921, 0.1323529411764707009 ),
 .UNSPECIFIED. ) 
 CURVE ( )  GEOMETRIC_REPRESENTATION_ITEM ( )  RATIONAL_B_SPLINE_CURVE ( ( 0.9999999999999982236, 0.9238795325112885148, 1.000000000000000000, 0.9238795325112867385, 1.000000000000000000, 0.9238795325112867385, 1.000000000000000000, 0.9238795325112844070, 1.000000000000002220 ) ) 
 REPRESENTATION_ITEM ( '' )  );
#46441=CARTESIAN_POINT ( 'NONE',  ( 7.778174593052021635, 7.778174593052023411, 90.62500000409677625 ) ) ;
#46453=CYLINDRICAL_SURFACE ( 'NONE', #65499, 11.00000000000000000 ) ;
#46463=CARTESIAN_POINT ( 'NONE',  ( 10.18810118749999916, 1.247682550866122264E-15, 98.78125000204838102 ) ) ;
#46471=CARTESIAN_POINT ( 'NONE',  ( 4.220049686691941027, -10.18810118749999738, 107.1250000020483810 ) ) ;
#46480=CARTESIAN_POINT ( 'NONE',  ( -4.220049686691937474, -10.18810118749999738, 105.8125000020483952 ) ) ;
#46494=CARTESIAN_POINT ( 'NONE',  ( 10.18810118750000093, -4.220049686691933033, 107.3125000020483810 ) ) ;
#46514=CARTESIAN_POINT ( 'NONE',  ( -4.556349186104045934, 11.00000000000000000, 117.7187499999999858 ) ) ;
#46519=FACE_OUTER_BOUND ( 'NONE', #18848, .T. ) ;
#46520=CARTESIAN_POINT ( 'NONE',  ( 0.000000000000000000, 0.000000000000000000, 118.0000000000000000 ) ) ;
#46526=CARTESIAN_POINT ( 'NONE',  ( -10.99999999999999822, -4.556349186104052151, 107.7812500040967763 ) ) ;
#46540=ORIENTED_EDGE ( 'NONE', *, *, #63309, .F. ) ;
#46547=CARTESIAN_POINT ( 'NONE',  ( -6.238412754330611322E-16, 10.18810118749999916, 83.78125000204836681 ) ) ;
#46551=CARTESIAN_POINT ( 'NONE',  ( -7.204075437095965206, -7.204075437095968759, 113.2187500020483810 ) ) ;
#46552=EDGE_LOOP ( 'NONE', ( #59094, #34081, #28023, #5288, #29416 ) ) ;
#46558=CARTESIAN_POINT ( 'NONE',  ( -4.220049686691935698, 10.18810118749999916, 76.75000000204838102 ) ) ;
#46570=CARTESIAN_POINT ( 'NONE',  ( 10.18810118749999916, 4.220049686691935698, 70.00000000204836681 ) ) ;
#46613=EDGE_CURVE ( 'NONE', #10820, #34245, #44288, .T. ) ;
#46616=CARTESIAN_POINT ( 'NONE',  ( -11.00000000000000000, 0.000000000000000000, 68.68750000409676204 ) ) ;
#46624=PLANE ( 'NONE',  #73238 ) ;
#46635=CARTESIAN_POINT ( 'NONE',  ( 10.18810118749999916, 4.220049686691935698, 100.0000000020483668 ) ) ;
#46653=CARTESIAN_POINT ( 'NONE',  ( 7.204075437095966983, 7.204075437095967871, 94.46875000204838102 ) ) ;
#46659=CARTESIAN_POINT ( 'NONE',  ( 10.18810118750000093, -4.220049686691933921, 79.18750000204836681 ) ) ;
#46666=CARTESIAN_POINT ( 'NONE',  ( 7.204075437095966983, 7.204075437095967871, 88.09375000204836681 ) ) ;
#46675=CARTESIAN_POINT ( 'NONE',  ( -10.18810118749999738, -4.220049686691941915, 74.12500000204836681 ) ) ;
#46690=CARTESIAN_POINT ( 'NONE',  ( -7.204075437095965206, -7.204075437095968759, 67.84375000204836681 ) ) ;
#46693=CARTESIAN_POINT ( 'NONE',  ( 11.00000000000000000, 1.347111479062088405E-15, 81.24999999999998579 ) ) ;
#46699=CARTESIAN_POINT ( 'NONE',  ( 0.000000000000000000, 0.000000000000000000, 118.0000000000000000 ) ) ;
#46718=CARTESIAN_POINT ( 'NONE',  ( -7.204075437095967871, 7.204075437095967871, 116.9687500020483810 ) ) ;
#46732=CARTESIAN_POINT ( 'NONE',  ( -7.204075437095965206, -7.204075437095968759, 113.2187500020483810 ) ) ;
#46736=DIRECTION ( 'NONE',  ( 1.000000000000000000, 0.000000000000000000, 0.000000000000000000 ) ) ;
#46764=CARTESIAN_POINT ( 'NONE',  ( 11.00000000000000000, 1.347111479062088405E-15, 99.24999999999998579 ) ) ;
#46771=CARTESIAN_POINT ( 'NONE',  ( -10.18810118749999738, -4.220049686691941915, 87.25000000204838102 ) ) ;
#46774=CARTESIAN_POINT ( 'NONE',  ( -4.556349186104047710, -10.99999999999999822, 103.2812499999999858 ) ) ;
#46782=CARTESIAN_POINT ( 'NONE',  ( -11.00000000000000000, 4.556349186104045934, 78.90624999999998579 ) ) ;
#46803=ORIENTED_EDGE ( 'NONE', *, *, #1503, .F. ) ;
#46806=CARTESIAN_POINT ( 'NONE',  ( -11.00000000000000000, 4.556349186104045934, 89.59375000409677625 ) ) ;
#46808=CARTESIAN_POINT ( 'NONE',  ( -4.556349186104048599, -10.99999999999999822, 110.9687500040967905 ) ) ;
#46819=ORIENTED_EDGE ( 'NONE', *, *, #27549, .T. ) ;
#46829=CARTESIAN_POINT ( 'NONE',  ( 0.000000000000000000, 0.000000000000000000, 118.0000000000000000 ) ) ;
#46831=CARTESIAN_POINT ( 'NONE',  ( -10.18810118749999916, 4.220049686691934809, 90.43750000204836681 ) ) ;
#46832=ORIENTED_EDGE ( 'NONE', *, *, #52675, .F. ) ;
#46836=CARTESIAN_POINT ( 'NONE',  ( -10.49999999999998224, 0.000000000000000000, 118.0000000000000000 ) ) ;
#46839=ORIENTED_EDGE ( 'NONE', *, *, #64300, .F. ) ;
#46840=CARTESIAN_POINT ( 'NONE',  ( 4.220049686691934809, 10.18810118749999916, 107.6875000020483810 ) ) ;
#46843=VERTEX_POINT ( 'NONE', #9683 ) ;
#46850=CARTESIAN_POINT ( 'NONE',  ( -10.18810118749999916, 4.220049686691934809, 102.4375000020483810 ) ) ;
#46856=CARTESIAN_POINT ( 'NONE',  ( -7.778174593052020747, -7.778174593052023411, 80.68750000000000000 ) ) ;
#46864=VERTEX_POINT ( 'NONE', #23589 ) ;
#46868=CARTESIAN_POINT ( 'NONE',  ( -7.204075437095965206, -7.204075437095968759, 106.8437500020483810 ) ) ;
#46886=CARTESIAN_POINT ( 'NONE',  ( -7.204075437095967871, 7.204075437095967871, 70.84375000204836681 ) ) ;
#46897=CARTESIAN_POINT ( 'NONE',  ( -11.00000000000000000, 0.000000000000000000, 101.6875000040967763 ) ) ;
#46913=FACE_OUTER_BOUND ( 'NONE', #4568, .T. ) ;
#46916=CARTESIAN_POINT ( 'NONE',  ( 4.220049686691934809, 10.18810118749999916, 85.18750000204838102 ) ) ;
#46920=CARTESIAN_POINT ( 'NONE',  ( -4.220049686691935698, 10.18810118749999916, 109.7500000020483810 ) ) ;
#46923=CARTESIAN_POINT ( 'NONE',  ( 7.778174593052023411, -7.778174593052021635, 109.7500000040967763 ) ) ;
#46927=CARTESIAN_POINT ( 'NONE',  ( -6.238412754330611322E-16, 10.18810118749999916, 78.15625000204836681 ) ) ;
#46938=CARTESIAN_POINT ( 'NONE',  ( 10.18810118749999916, 1.247682550866122264E-15, 74.40625000204836681 ) ) ;
#46940=DIRECTION ( 'NONE',  ( -1.000000000000000000, 0.000000000000000000, 0.000000000000000000 ) ) ;
#46971=CARTESIAN_POINT ( 'NONE',  ( -11.00000000000000000, 0.000000000000000000, 76.18750000409677625 ) ) ;
#46981=CARTESIAN_POINT ( 'NONE',  ( -7.778174593052023411, 7.778174593052023411, 68.50000000409677625 ) ) ;
#46995=CARTESIAN_POINT ( 'NONE',  ( 11.00000000000000000, 1.347111479062088405E-15, 88.75000000000000000 ) ) ;
#46999=CARTESIAN_POINT ( 'NONE',  ( -8.259994644541624353, 7.006214462904858387, 117.7099183163968092 ) ) ;
#47001=CARTESIAN_POINT ( 'NONE',  ( -4.220049686691937474, -10.18810118749999738, 103.9375000020483810 ) ) ;
#47013=DIRECTION ( 'NONE',  ( -1.000000000000000000, 0.000000000000000000, 0.000000000000000000 ) ) ;
#47017=CARTESIAN_POINT ( 'NONE',  ( -4.220049686691937474, -10.18810118749999738, 96.81250000204838102 ) ) ;
#47020=LINE ( 'NONE', #70415, #65720 ) ;
#47021=CARTESIAN_POINT ( 'NONE',  ( 0.000000000000000000, 0.000000000000000000, 118.0000000000000000 ) ) ;
#47023=CARTESIAN_POINT ( 'NONE',  ( 4.220049686691934809, 10.18810118749999916, 78.06250000204838102 ) ) ;
#47031=CARTESIAN_POINT ( 'NONE',  ( -10.18810118749999738, -4.220049686691941915, 91.75000000204836681 ) ) ;
#47041=CARTESIAN_POINT ( 'NONE',  ( -10.18810118749999916, 4.220049686691934809, 76.93750000204839523 ) ) ;
#47059=CARTESIAN_POINT ( 'NONE',  ( 4.556349186104045934, 11.00000000000000000, 86.03124999999998579 ) ) ;
#47085=CARTESIAN_POINT ( 'NONE',  ( 4.556349186104051263, -10.99999999999999822, 70.65625000409676204 ) ) ;
#47097=CARTESIAN_POINT ( 'NONE',  ( -4.220049686691937474, -10.18810118749999738, 114.8125000020483668 ) ) ;
#47131=EDGE_CURVE ( 'NONE', #32492, #40180, #35433, .T. ) ;
#47139=ORIENTED_EDGE ( 'NONE', *, *, #47131, .T. ) ;
#47141=CARTESIAN_POINT ( 'NONE',  ( -7.204075437095965206, -7.204075437095968759, 85.84375000204836681 ) ) ;
#47144=CARTESIAN_POINT ( 'NONE',  ( 11.00000000000000355, -4.556349186104045046, 99.15624999999998579 ) ) ;
#47168=DIRECTION ( 'NONE',  ( -0.000000000000000000, -0.000000000000000000, -1.000000000000000000 ) ) ;
#47174=CARTESIAN_POINT ( 'NONE',  ( 7.778174593052023411, -7.778174593052021635, 85.75000000409677625 ) ) ;
#47177=CARTESIAN_POINT ( 'NONE',  ( -6.735557395310442023E-16, 11.00000000000000000, 101.1249999999999858 ) ) ;
#47196=VECTOR ( 'NONE', #26364, 1000.000000000000000 ) ;
#47200=CARTESIAN_POINT ( 'NONE',  ( -7.204075437095965206, -7.204075437095968759, 92.21875000204838102 ) ) ;
#47205=CARTESIAN_POINT ( 'NONE',  ( -7.204075437095967871, 7.204075437095967871, 100.4687500020483668 ) ) ;
#47212=CARTESIAN_POINT ( 'NONE',  ( -6.238412754330611322E-16, 10.18810118749999916, 106.6562500020483810 ) ) ;
#47217=VERTEX_POINT ( 'NONE', #51163 ) ;
#47218=CARTESIAN_POINT ( 'NONE',  ( -10.99999999999989164, -4.556349186104158733, 80.59374999999998579 ) ) ;
#47227=CARTESIAN_POINT ( 'NONE',  ( 7.778174593052021635, 7.778174593052023411, 84.43749999999998579 ) ) ;
#47229=ORIENTED_EDGE ( 'NONE', *, *, #47538, .T. ) ;
#47231=CARTESIAN_POINT ( 'NONE',  ( 10.18810118749999916, 1.247682550866122264E-15, 105.9062500020483810 ) ) ;
#47250=CARTESIAN_POINT ( 'NONE',  ( 7.204075437095968759, -7.204075437095966983, 71.59375000204836681 ) ) ;
#47255=CYLINDRICAL_SURFACE ( 'NONE', #24794, 11.00000000000000000 ) ;
#47261=CARTESIAN_POINT ( 'NONE',  ( -7.778174593052023411, 7.778174593052023411, 106.0000000040967763 ) ) ;
#47281=CARTESIAN_POINT ( 'NONE',  ( -10.18810118749999916, 0.000000000000000000, 81.15625000204838102 ) ) ;
#47285=EDGE_CURVE ( 'NONE', #62397, #56611, #55068, .T. ) ;
#47286=CARTESIAN_POINT ( 'NONE',  ( 1.871523826299183495E-15, -10.18810118749999916, 108.9062500020483668 ) ) ;
#47289=DIRECTION ( 'NONE',  ( -7.885106708985487801E-17, 1.000000000000000000, -0.000000000000000000 ) ) ;
#47294=CARTESIAN_POINT ( 'NONE',  ( 10.18810118749999916, 1.247682550866122264E-15, 74.78125000204836681 ) ) ;
#47308=CARTESIAN_POINT ( 'NONE',  ( -10.18810118749999916, 0.000000000000000000, 69.15625000204836681 ) ) ;
#47371=CARTESIAN_POINT ( 'NONE',  ( 10.18810118750000093, -4.220049686691933921, 101.3125000020483810 ) ) ;
#47372=CARTESIAN_POINT ( 'NONE',  ( 7.778174593052021635, 7.778174593052023411, 86.12500000409677625 ) ) ;
#47383=CARTESIAN_POINT ( 'NONE',  ( -11.00000000000010303, -4.556349186103947346, 73.09375000000000000 ) ) ;
#47389=CARTESIAN_POINT ( 'NONE',  ( -6.238412754330611322E-16, 10.18810118749999916, 93.15625000204836681 ) ) ;
#47394=FACE_OUTER_BOUND ( 'NONE', #63381, .T. ) ;
#47395=CARTESIAN_POINT ( 'NONE',  ( 11.00000000000000000, 1.347111479062088405E-15, 102.2500000000000000 ) ) ;
#47396=CARTESIAN_POINT ( 'NONE',  ( -10.18810118749999916, 4.220049686691934809, 75.43750000204836681 ) ) ;
#47400=CARTESIAN_POINT ( 'NONE',  ( -4.556349186104045934, 11.00000000000000000, 89.40625000409677625 ) ) ;
#47402=CARTESIAN_POINT ( 'NONE',  ( 7.204075437095966983, 7.204075437095967871, 86.59375000204836681 ) ) ;
#47406=VERTEX_POINT ( 'NONE', #53028 ) ;
#47412=CARTESIAN_POINT ( 'NONE',  ( 10.18810118749999916, 1.247682550866122264E-15, 73.28125000204838102 ) ) ;
#47416=CARTESIAN_POINT ( 'NONE',  ( 11.00000000000000000, 1.347111479062088405E-15, 93.43750000409677625 ) ) ;
#47429=CARTESIAN_POINT ( 'NONE',  ( -6.238412754330611322E-16, 10.18810118749999916, 70.28125000204838102 ) ) ;
#47432=CARTESIAN_POINT ( 'NONE',  ( 11.00000000000000000, 1.347111479062088405E-15, 78.24999999999998579 ) ) ;
#47436=EDGE_LOOP ( 'NONE', ( #57084, #59288, #65172, #37295 ) ) ;
#47443=EDGE_CURVE ( 'NONE', #64267, #42385, #71016, .T. ) ;
#47458=CARTESIAN_POINT ( 'NONE',  ( 2.020667218593132706E-15, -11.00000000000000000, 116.8749999999999858 ) ) ;
#47460=CARTESIAN_POINT ( 'NONE',  ( -10.18810118749999916, 0.000000000000000000, 117.1562500020483810 ) ) ;
#47472=CARTESIAN_POINT ( 'NONE',  ( -10.18810118749999916, 4.220049686691934809, 112.9375000020483810 ) ) ;
#47482=ORIENTED_EDGE ( 'NONE', *, *, #81, .T. ) ;
#47496=DIRECTION ( 'NONE',  ( -0.000000000000000000, -0.000000000000000000, -1.000000000000000000 ) ) ;
#47504=ADVANCED_FACE ( 'NONE', ( #42344 ), #65361, .T. ) ;
#47508=CARTESIAN_POINT ( 'NONE',  ( 10.18810118749999916, 4.220049686691935698, 85.00000000204838102 ) ) ;
#47510=CARTESIAN_POINT ( 'NONE',  ( -11.00000000000000000, 0.000000000000000000, 96.99999999999998579 ) ) ;
#47534=CARTESIAN_POINT ( 'NONE',  ( -11.00000000000005151, 4.556349186103993532, 99.90624999999997158 ) ) ;
#47536=CARTESIAN_POINT ( 'NONE',  ( -7.778174593052023411, 7.778174593052023411, 104.5000000040967763 ) ) ;
#47538=EDGE_CURVE ( 'NONE', #13039, #30692, #4126, .T. ) ;
#47541=CARTESIAN_POINT ( 'NONE',  ( 2.020667218593132706E-15, -11.00000000000000000, 87.06250000409676204 ) ) ;
#47557=CARTESIAN_POINT ( 'NONE',  ( -6.735557395310442023E-16, 11.00000000000000000, 92.31250000409677625 ) ) ;
#47565=CARTESIAN_POINT ( 'NONE',  ( 10.18810118750000093, -4.220049686691933921, 91.18750000204836681 ) ) ;
#47568=CARTESIAN_POINT ( 'NONE',  ( 11.00000000000000000, 1.347111479062088405E-15, 100.9375000040967763 ) ) ;
#47570=CARTESIAN_POINT ( 'NONE',  ( 10.18810118750000093, -4.220049686691933921, 101.3125000020483810 ) ) ;
#47578=CARTESIAN_POINT ( 'NONE',  ( 7.204075437095966983, 7.204075437095967871, 97.46875000204838102 ) ) ;
#47589=CARTESIAN_POINT ( 'NONE',  ( 5.499987861550171608, 9.526286449755788865, 67.99927393035380874 ) ) ;
#47593=ORIENTED_EDGE ( 'NONE', *, *, #49514, .F. ) ;
#47594=CARTESIAN_POINT ( 'NONE',  ( 7.204075437095966983, 7.204075437095967871, 101.5937500020483668 ) ) ;
#47611=CARTESIAN_POINT ( 'NONE',  ( 2.020667218593132706E-15, -11.00000000000000000, 110.8749999999999858 ) ) ;
#47624=CARTESIAN_POINT ( 'NONE',  ( 11.00000000000000000, 4.556349186104045934, 104.0312500040967763 ) ) ;
#47628=CARTESIAN_POINT ( 'NONE',  ( 11.00000000000000000, 1.347111479062088405E-15, 79.93750000409677625 ) ) ;
#47631=CARTESIAN_POINT ( 'NONE',  ( -11.00000000000010658, 4.556349186103942017, 87.90625000000000000 ) ) ;
#47639=CARTESIAN_POINT ( 'NONE',  ( 7.778174593052023411, -7.778174593052021635, 67.75000000409677625 ) ) ;
#47646=CARTESIAN_POINT ( 'NONE',  ( 5.094045771088254959, 8.823157229062946527, 67.15552375567561683 ) ) ;
#47650=CARTESIAN_POINT ( 'NONE',  ( 10.18810118749999916, 1.247682550866122264E-15, 107.7812500020483810 ) ) ;
#47653=CARTESIAN_POINT ( 'NONE',  ( 10.99999999999992006, -4.556349186104122317, 109.8437500040967620 ) ) ;
#47657=CARTESIAN_POINT ( 'NONE',  ( -4.220049686691935698, 10.18810118749999916, 73.75000000204836681 ) ) ;
#47668=CARTESIAN_POINT ( 'NONE',  ( -10.18810118749999916, 0.000000000000000000, 117.5312500020483810 ) ) ;
#47679=VECTOR ( 'NONE', #31739, 1000.000000000000000 ) ;
#47693=VECTOR ( 'NONE', #24998, 1000.000000000000000 ) ;
#47700=CARTESIAN_POINT ( 'NONE',  ( -7.778174593052023411, 7.778174593052023411, 116.5000000040967905 ) ) ;
#47705=CARTESIAN_POINT ( 'NONE',  ( 11.00000000000010836, -4.556349186103939353, 69.34375000409676204 ) ) ;
#47719=ADVANCED_FACE ( 'NONE', ( #65167 ), #19516, .F. ) ;
#47723=CARTESIAN_POINT ( 'NONE',  ( 7.778174593052023411, -7.778174593052021635, 85.56249999999998579 ) ) ;
#47725=CARTESIAN_POINT ( 'NONE',  ( -4.556349186104045934, 11.00000000000000000, 101.4062500040967763 ) ) ;
#47731=CARTESIAN_POINT ( 'NONE',  ( 5.471491410962281421, 9.542682104092435225, 117.5000000000000568 ) ) ;
#47732=CARTESIAN_POINT ( 'NONE',  ( 7.204075437095966983, 7.204075437095967871, 101.5937500020483668 ) ) ;
#47749=CARTESIAN_POINT ( 'NONE',  ( -10.18810118749999916, 0.000000000000000000, 89.03125000204836681 ) ) ;
#47756=CARTESIAN_POINT ( 'NONE',  ( 10.18810118750000093, -4.220049686691933921, 71.68750000204836681 ) ) ;
#47763=CARTESIAN_POINT ( 'NONE',  ( -10.18810118749999916, 0.000000000000000000, 90.15625000204838102 ) ) ;
#47774=CARTESIAN_POINT ( 'NONE',  ( 4.220049686691941027, -10.18810118749999738, 68.50000000204838102 ) ) ;
#47796=CARTESIAN_POINT ( 'NONE',  ( 7.778174593052023411, -7.778174593052021635, 79.56249999999998579 ) ) ;
#47809=CARTESIAN_POINT ( 'NONE',  ( 11.00000000000000000, 1.347111479062088405E-15, 70.74999999999998579 ) ) ;
#47825=CARTESIAN_POINT ( 'NONE',  ( -4.220049686691935698, 10.18810118749999916, 84.25000000204838102 ) ) ;
#47826=CARTESIAN_POINT ( 'NONE',  ( -10.99999999999999822, -4.556349186104052151, 67.28125000409676204 ) ) ;
#47838=CARTESIAN_POINT ( 'NONE',  ( -10.18810118749999916, 0.000000000000000000, 114.5312500020483810 ) ) ;
#47840=ORIENTED_EDGE ( 'NONE', *, *, #41051, .T. ) ;
#47864=VERTEX_POINT ( 'NONE', #38006 ) ;
#47875=ORIENTED_EDGE ( 'NONE', *, *, #49514, .T. ) ;
#47878=CARTESIAN_POINT ( 'NONE',  ( -6.238412754330611322E-16, 10.18810118749999916, 88.28125000204836681 ) ) ;
#47880=CARTESIAN_POINT ( 'NONE',  ( -4.556349186104045934, 11.00000000000000000, 95.21874999999998579 ) ) ;
#47885=CARTESIAN_POINT ( 'NONE',  ( -11.00000000000000000, 0.000000000000000000, 84.99999999999998579 ) ) ;
#47909=CARTESIAN_POINT ( 'NONE',  ( -7.778174593052023411, 7.778174593052023411, 85.00000000409677625 ) ) ;
#47912=CARTESIAN_POINT ( 'NONE',  ( 10.99999999999994849, 4.556349186104097448, 100.8437500000000142 ) ) ;
#47932=CARTESIAN_POINT ( 'NONE',  ( -4.220049686691937474, -10.18810118749999738, 92.31250000204838102 ) ) ;
#47937=CARTESIAN_POINT ( 'NONE',  ( 7.204075437095968759, -7.204075437095966983, 102.7187500020483668 ) ) ;
#47947=CARTESIAN_POINT ( 'NONE',  ( 10.18810118750000093, -4.220049686691933921, 100.1875000020483668 ) ) ;
#47962=CARTESIAN_POINT ( 'NONE',  ( -7.778174593052023411, 7.778174593052023411, 84.81249999999998579 ) ) ;
#47966=CARTESIAN_POINT ( 'NONE',  ( 4.220049686691934809, 10.18810118749999916, 106.1875000020483810 ) ) ;
#47983=CARTESIAN_POINT ( 'NONE',  ( 2.020667218593132706E-15, -11.00000000000000000, 91.56250000409677625 ) ) ;
#47984=CARTESIAN_POINT ( 'NONE',  ( -7.778174593052020747, -7.778174593052023411, 112.1875000000000000 ) ) ;
#47990=LINE ( 'NONE', #14397, #46358 ) ;
#47996=CARTESIAN_POINT ( 'NONE',  ( -6.735557395310442023E-16, 11.00000000000000000, 105.8125000040967763 ) ) ;
#48000=CARTESIAN_POINT ( 'NONE',  ( -11.00000000000000000, 0.000000000000000000, 107.4999999999999858 ) ) ;
#48009=CARTESIAN_POINT ( 'NONE',  ( 11.00000000000000000, 1.347111479062088405E-15, 67.93750000409676204 ) ) ;
#48019=CARTESIAN_POINT ( 'NONE',  ( -7.204075437095967871, 7.204075437095967871, 111.3437500020483810 ) ) ;
#48020=ORIENTED_EDGE ( 'NONE', *, *, #18919, .T. ) ;
#48023=DIRECTION ( 'NONE',  ( -0.000000000000000000, -0.000000000000000000, -1.000000000000000000 ) ) ;
#48027=CARTESIAN_POINT ( 'NONE',  ( 1.871523826299183495E-15, -10.18810118749999916, 69.90625000204836681 ) ) ;
#48039=CARTESIAN_POINT ( 'NONE',  ( 4.220049686691941027, -10.18810118749999738, 116.5000000020483810 ) ) ;
#48044=EDGE_CURVE ( 'NONE', #55449, #72546, #11834, .T. ) ;
#48067=ORIENTED_EDGE ( 'NONE', *, *, #74133, .T. ) ;
#48082=CARTESIAN_POINT ( 'NONE',  ( -11.00000000000000000, 0.000000000000000000, 96.99999999999998579 ) ) ;
#48089=LINE ( 'NONE', #41703, #59470 ) ;
#48097=VERTEX_POINT ( 'NONE', #34219 ) ;
#48104=CARTESIAN_POINT ( 'NONE',  ( -10.18810118749999916, 0.000000000000000000, 93.15625000204836681 ) ) ;
#48117=CARTESIAN_POINT ( 'NONE',  ( 11.00000000000000000, 1.347111479062088405E-15, 73.74999999999998579 ) ) ;
#48118=CARTESIAN_POINT ( 'NONE',  ( 10.99999999999978861, 4.556349186104256432, 83.03125000409679046 ) ) ;
#48122=CARTESIAN_POINT ( 'NONE',  ( 7.204075437095966983, 7.204075437095967871, 91.46875000204838102 ) ) ;
#48128=CARTESIAN_POINT ( 'NONE',  ( -4.220049686691935698, 10.18810118749999916, 75.25000000204836681 ) ) ;
#48135=CARTESIAN_POINT ( 'NONE',  ( 10.18810118749999916, 4.220049686691935698, 80.50000000204839523 ) ) ;
#48141=DIRECTION ( 'NONE',  ( -0.000000000000000000, -0.000000000000000000, -1.000000000000000000 ) ) ;
#48146=CARTESIAN_POINT ( 'NONE',  ( 7.204075437095966983, 7.204075437095967871, 70.46875000204836681 ) ) ;
#48147=ORIENTED_EDGE ( 'NONE', *, *, #52790, .T. ) ;
#48169=CARTESIAN_POINT ( 'NONE',  ( 7.778174593052023411, -7.778174593052021635, 75.06249999999997158 ) ) ;
#48179=CARTESIAN_POINT ( 'NONE',  ( -10.99999999999999822, -4.556349186104052151, 115.2812500040967763 ) ) ;
#48194=CARTESIAN_POINT ( 'NONE',  ( 1.871523826299183495E-15, -10.18810118749999916, 86.40625000204838102 ) ) ;
#48195=CARTESIAN_POINT ( 'NONE',  ( -7.204075437095965206, -7.204075437095968759, 112.8437500020483810 ) ) ;
#48202=AXIS2_PLACEMENT_3D ( 'NONE', #3173, #73970, #20885 ) ;
#48207=CARTESIAN_POINT ( 'NONE',  ( 7.204075437095968759, -7.204075437095966983, 106.0937500020483810 ) ) ;
#48209=ORIENTED_EDGE ( 'NONE', *, *, #54476, .F. ) ;
#48236=CARTESIAN_POINT ( 'NONE',  ( -6.735557395310442023E-16, 11.00000000000000000, 72.62500000000000000 ) ) ;
#48239=CARTESIAN_POINT ( 'NONE',  ( -11.00000000000000000, 0.000000000000000000, 101.6875000040967763 ) ) ;
#48248=CARTESIAN_POINT ( 'NONE',  ( 10.18810118749999916, 1.247682550866122264E-15, 78.90625000204836681 ) ) ;
#48250=CARTESIAN_POINT ( 'NONE',  ( 11.00000000000000355, -4.556349186104045046, 93.15625000000000000 ) ) ;
#48257=FACE_OUTER_BOUND ( 'NONE', #21413, .T. ) ;
#48282=CARTESIAN_POINT ( 'NONE',  ( 4.556349186104051263, -10.99999999999999822, 88.65625000409679046 ) ) ;
#48297=DIRECTION ( 'NONE',  ( -0.000000000000000000, -0.000000000000000000, -1.000000000000000000 ) ) ;
#48299=CARTESIAN_POINT ( 'NONE',  ( 11.00000000000005151, 4.556349186103993532, 92.03125000409677625 ) ) ;
#48305=CARTESIAN_POINT ( 'NONE',  ( -4.220049686691935698, 10.18810118749999916, 88.75000000204836681 ) ) ;
#48306=ORIENTED_EDGE ( 'NONE', *, *, #60667, .F. ) ;
#48311=CARTESIAN_POINT ( 'NONE',  ( 7.204075437095968759, -7.204075437095966983, 99.71875000204838102 ) ) ;
#48316=VECTOR ( 'NONE', #67674, 1000.000000000000000 ) ;
#48321=CARTESIAN_POINT ( 'NONE',  ( -4.220049686691935698, 10.18810118749999916, 100.7500000020483526 ) ) ;
#48331=CARTESIAN_POINT ( 'NONE',  ( 4.556349186104045934, 11.00000000000000000, 84.53125000000000000 ) ) ;
#48335=CARTESIAN_POINT ( 'NONE',  ( -10.18810118749999916, 4.220049686691934809, 97.56250000204836681 ) ) ;
#48336=CARTESIAN_POINT ( 'NONE',  ( 11.00000000000002132, 4.556349186104026394, 114.5312500040967620 ) ) ;
#48346=DIRECTION ( 'NONE',  ( -0.000000000000000000, 0.000000000000000000, 1.000000000000000000 ) ) ;
#48353=CARTESIAN_POINT ( 'NONE',  ( 11.00000000000000000, 4.556349186104045934, 115.8437500000000000 ) ) ;
#48367=CARTESIAN_POINT ( 'NONE',  ( 4.556349186104045934, 11.00000000000000000, 105.7187500040967763 ) ) ;
#48391=CARTESIAN_POINT ( 'NONE',  ( -6.238412754330611322E-16, 10.18810118749999916, 108.1562500020483668 ) ) ;
#48395=DIRECTION ( 'NONE',  ( -0.000000000000000000, -0.000000000000000000, -1.000000000000000000 ) ) ;
#48399=CARTESIAN_POINT ( 'NONE',  ( 7.204075437095966983, 7.204075437095967871, 73.46875000204838102 ) ) ;
#48411=CARTESIAN_POINT ( 'NONE',  ( -7.204075437095967871, 7.204075437095967871, 67.46875000204836681 ) ) ;
#48443=CARTESIAN_POINT ( 'NONE',  ( 11.00000000000000888, 4.556349186104037940, 116.0312500040967905 ) ) ;
#48449=DIRECTION ( 'NONE',  ( 0.000000000000000000, 0.000000000000000000, 1.000000000000000000 ) ) ;
#48470=CARTESIAN_POINT ( 'NONE',  ( -7.778174593052023411, 7.778174593052023411, 82.00000000409676204 ) ) ;
#48475=DIRECTION ( 'NONE',  ( -1.000000000000000000, 0.000000000000000000, 0.000000000000000000 ) ) ;
#48478=CARTESIAN_POINT ( 'NONE',  ( -6.238412754330611322E-16, 10.18810118749999916, 94.28125000204836681 ) ) ;
#48481=LINE ( 'NONE', #31132, #60624 ) ;
#48493=CARTESIAN_POINT ( 'NONE',  ( -10.18810118749999916, 0.000000000000000000, 87.53125000204836681 ) ) ;
#48498=CARTESIAN_POINT ( 'NONE',  ( -4.220049686691937474, -10.18810118749999738, 74.31250000204836681 ) ) ;
#48505=CARTESIAN_POINT ( 'NONE',  ( 7.204075437095968759, -7.204075437095966983, 83.21875000204836681 ) ) ;
#48507=( BOUNDED_CURVE ( )  B_SPLINE_CURVE ( 2, ( #37344, #70926, #9045, #60723, #8670, #59976, #49020, #61095, #66377 ),
 .UNSPECIFIED., .F., .F. ) 
 B_SPLINE_CURVE_WITH_KNOTS ( ( 3, 2, 2, 2, 3 ),
 ( 0.9117647058823529216, 0.9154411764705882026, 0.9191176470588233727, 0.9227941176470587648, 0.9264705882352940458 ),
 .UNSPECIFIED. ) 
 CURVE ( )  GEOMETRIC_REPRESENTATION_ITEM ( )  RATIONAL_B_SPLINE_CURVE ( ( 1.000000000000000000, 0.9238795325112867385, 1.000000000000000000, 0.9238795325112867385, 1.000000000000000000, 0.9238795325112867385, 1.000000000000000000, 0.9238795325112890700, 0.9999999999999976685 ) ) 
 REPRESENTATION_ITEM ( '' )  );
#48515=CARTESIAN_POINT ( 'NONE',  ( 5.094050593753887135, 8.823154444699161658, 67.53052362291680311 ) ) ;
#48529=DIRECTION ( 'NONE',  ( -0.000000000000000000, -0.000000000000000000, -1.000000000000000000 ) ) ;
#48532=CARTESIAN_POINT ( 'NONE',  ( -10.99999999999996092, 4.556349186104085902, 114.9062499999999716 ) ) ;
#48536=CARTESIAN_POINT ( 'NONE',  ( 4.556349186104051263, -10.99999999999999822, 74.96874999999998579 ) ) ;
#48562=CARTESIAN_POINT ( 'NONE',  ( 10.18810118749999916, 4.220049686691935698, 89.87500000204836681 ) ) ;
#48564=CARTESIAN_POINT ( 'NONE',  ( -6.238412754330611322E-16, 10.18810118749999916, 110.7812500020483668 ) ) ;
#48576=CARTESIAN_POINT ( 'NONE',  ( 10.18810118749999916, 4.220049686691935698, 109.3750000020483810 ) ) ;
#48613=CARTESIAN_POINT ( 'NONE',  ( -11.00000000000000000, 0.000000000000000000, 83.49999999999998579 ) ) ;
#48617=CARTESIAN_POINT ( 'NONE',  ( -6.238412754330611322E-16, 10.18810118749999916, 77.78125000204836681 ) ) ;
#48620=CARTESIAN_POINT ( 'NONE',  ( -10.99999999999999822, -4.556349186104052151, 92.59374999999998579 ) ) ;
#48621=CARTESIAN_POINT ( 'NONE',  ( 11.00000000000010836, -4.556349186103939353, 105.1562499999999858 ) ) ;
#48625=CARTESIAN_POINT ( 'NONE',  ( 11.00000000000000000, 1.347111479062088405E-15, 75.43750000409676204 ) ) ;
#48649=CARTESIAN_POINT ( 'NONE',  ( -11.00000000000000000, 0.000000000000000000, 82.18750000409677625 ) ) ;
#48664=ORIENTED_EDGE ( 'NONE', *, *, #42517, .T. ) ;
#48666=CARTESIAN_POINT ( 'NONE',  ( 1.871523826299183495E-15, -10.18810118749999916, 80.03125000204836681 ) ) ;
#48675=CARTESIAN_POINT ( 'NONE',  ( 4.220049686691941027, -10.18810118749999738, 86.50000000204838102 ) ) ;
#48681=CARTESIAN_POINT ( 'NONE',  ( -6.238412754330611322E-16, 10.18810118749999916, 101.7812500020483810 ) ) ;
#48682=EDGE_CURVE ( 'NONE', #31332, #33217, #56760, .T. ) ;
#48690=CARTESIAN_POINT ( 'NONE',  ( 4.220049686691941027, -10.18810118749999738, 100.0000000020483668 ) ) ;
#48692=FACE_OUTER_BOUND ( 'NONE', #38287, .T. ) ;
#48708=CARTESIAN_POINT ( 'NONE',  ( -10.18810118749999916, 4.220049686691934809, 96.06250000204836681 ) ) ;
#48717=EDGE_CURVE ( 'NONE', #31137, #8706, #65792, .T. ) ;
#48725=CARTESIAN_POINT ( 'NONE',  ( -10.99999999999999822, -4.556349186104053040, 91.28125000409677625 ) ) ;
#48726=CARTESIAN_POINT ( 'NONE',  ( -11.00000000000000000, 0.000000000000000000, 111.9999999999999858 ) ) ;
#48734=DIRECTION ( 'NONE',  ( -0.000000000000000000, -0.000000000000000000, -1.000000000000000000 ) ) ;
#48739=CARTESIAN_POINT ( 'NONE',  ( 2.020667218593132706E-15, -11.00000000000000000, 97.56250000409677625 ) ) ;
#48740=CARTESIAN_POINT ( 'NONE',  ( 10.99999999999989697, -4.556349186104149851, 106.8437500040967620 ) ) ;
#48743=CARTESIAN_POINT ( 'NONE',  ( -4.556349186104048599, -10.99999999999999822, 107.7812500000000000 ) ) ;
#48763=CARTESIAN_POINT ( 'NONE',  ( -10.18810118749999916, 0.000000000000000000, 104.0312500020483810 ) ) ;
#48771=CARTESIAN_POINT ( 'NONE',  ( -10.18810118749999916, 4.220049686691934809, 70.93750000204838102 ) ) ;
#48783=CARTESIAN_POINT ( 'NONE',  ( -10.18810118749999916, 4.220049686691934809, 115.9375000020483668 ) ) ;
#48793=DIRECTION ( 'NONE',  ( -0.000000000000000000, -0.000000000000000000, -1.000000000000000000 ) ) ;
#48798=CARTESIAN_POINT ( 'NONE',  ( 7.204075437095968759, -7.204075437095966983, 116.2187500020483810 ) ) ;
#48807=FACE_OUTER_BOUND ( 'NONE', #72382, .T. ) ;
#48839=CARTESIAN_POINT ( 'NONE',  ( 11.00000000000000000, 1.347111479062088405E-15, 118.0000000000000000 ) ) ;
#48840=CARTESIAN_POINT ( 'NONE',  ( -11.00000000000000000, 0.000000000000000000, 104.6875000040967763 ) ) ;
#48847=CARTESIAN_POINT ( 'NONE',  ( 7.204075437095968759, -7.204075437095966983, 96.71875000204838102 ) ) ;
#48862=CARTESIAN_POINT ( 'NONE',  ( 4.220049686691941027, -10.18810118749999738, 89.50000000204836681 ) ) ;
#48867=CARTESIAN_POINT ( 'NONE',  ( 11.00000000000010836, -4.556349186103939353, 102.3437500040967905 ) ) ;
#48876=CARTESIAN_POINT ( 'NONE',  ( -4.220049686691935698, 10.18810118749999916, 85.37500000204839523 ) ) ;
#48907=CARTESIAN_POINT ( 'NONE',  ( -11.00000000000000000, 0.000000000000000000, 78.99999999999998579 ) ) ;
#48918=CARTESIAN_POINT ( 'NONE',  ( -4.556349186104047710, -10.99999999999999822, 113.9687500040967905 ) ) ;
#48935=CARTESIAN_POINT ( 'NONE',  ( 7.204075437095966983, 7.204075437095967871, 85.46875000204836681 ) ) ;
#48936=CARTESIAN_POINT ( 'NONE',  ( -10.18810118749999916, 4.220049686691934809, 114.0625000020483668 ) ) ;
#48943=VECTOR ( 'NONE', #40522, 1000.000000000000000 ) ;
#48949=CARTESIAN_POINT ( 'NONE',  ( 7.204075437095968759, -7.204075437095966983, 107.5937500020483810 ) ) ;
#48986=VECTOR ( 'NONE', #22846, 1000.000000000000000 ) ;
#48989=CARTESIAN_POINT ( 'NONE',  ( 10.18810118749999916, 4.220049686691935698, 80.50000000204839523 ) ) ;
#48992=CARTESIAN_POINT ( 'NONE',  ( -4.556349186104045934, 11.00000000000000000, 93.71874999999998579 ) ) ;
#49020=CARTESIAN_POINT ( 'NONE',  ( 7.778174593052021635, 7.778174593052023411, 69.62500000409677625 ) ) ;
#49022=CARTESIAN_POINT ( 'NONE',  ( -4.556349186104045934, 11.00000000000000000, 78.90625000409677625 ) ) ;
#49040=CARTESIAN_POINT ( 'NONE',  ( 10.18810118749999916, 1.247682550866122264E-15, 74.40625000204836681 ) ) ;
#49046=CARTESIAN_POINT ( 'NONE',  ( -11.00000000000000000, 0.000000000000000000, 108.9999999999999858 ) ) ;
#49048=CARTESIAN_POINT ( 'NONE',  ( -10.18810118749999738, -4.220049686691941915, 86.12500000204836681 ) ) ;
#49054=CARTESIAN_POINT ( 'NONE',  ( -10.18810118749999916, 4.220049686691934809, 94.56250000204838102 ) ) ;
#49057=VERTEX_POINT ( 'NONE', #55096 ) ;
#49061=CARTESIAN_POINT ( 'NONE',  ( -7.204075437095967871, 7.204075437095967871, 97.84375000204836681 ) ) ;
#49071=CARTESIAN_POINT ( 'NONE',  ( -7.778174593052020747, -7.778174593052023411, 95.87500000409676204 ) ) ;
#49078=ORIENTED_EDGE ( 'NONE', *, *, #13130, .F. ) ;
#49079=CARTESIAN_POINT ( 'NONE',  ( 10.18810118749999916, 4.220049686691935698, 100.0000000020483952 ) ) ;
#49099=CARTESIAN_POINT ( 'NONE',  ( -7.778174593052023411, 7.778174593052023411, 114.8125000000000000 ) ) ;
#49104=CARTESIAN_POINT ( 'NONE',  ( 4.556349186104052151, -10.99999999999999822, 101.9687500000000000 ) ) ;
#49107=DIRECTION ( 'NONE',  ( -1.000000000000000000, 0.000000000000000000, 0.000000000000000000 ) ) ;
#49112=CARTESIAN_POINT ( 'NONE',  ( 11.00000000000000000, 1.347111479062088405E-15, 97.93750000409677625 ) ) ;
#49126=ORIENTED_EDGE ( 'NONE', *, *, #1611, .T. ) ;
#49135=CARTESIAN_POINT ( 'NONE',  ( -6.238412754330611322E-16, 10.18810118749999916, 102.1562500020483810 ) ) ;
#49142=CARTESIAN_POINT ( 'NONE',  ( 7.204075437095968759, -7.204075437095966983, 73.09375000204838102 ) ) ;
#49157=CARTESIAN_POINT ( 'NONE',  ( 4.220049686691934809, 10.18810118749999916, 114.0625000020483668 ) ) ;
#49186=CYLINDRICAL_SURFACE ( 'NONE', #30981, 11.00000000000000000 ) ;
#49219=CARTESIAN_POINT ( 'NONE',  ( -11.00000000000000000, 0.000000000000000000, 95.49999999999998579 ) ) ;
#49224=CARTESIAN_POINT ( 'NONE',  ( -7.204075437095967871, 7.204075437095967871, 95.96875000204838102 ) ) ;
#49225=DIRECTION ( 'NONE',  ( -1.000000000000000000, 0.000000000000000000, 0.000000000000000000 ) ) ;
#49236=CARTESIAN_POINT ( 'NONE',  ( 7.204075437095966983, 7.204075437095967871, 88.46875000204838102 ) ) ;
#49250=CARTESIAN_POINT ( 'NONE',  ( 1.871523826299183495E-15, -10.18810118749999916, 83.03125000204838102 ) ) ;
#49272=VERTEX_POINT ( 'NONE', #40707 ) ;
#49285=CARTESIAN_POINT ( 'NONE',  ( 11.00000000000000355, -4.556349186104045046, 70.65625000000000000 ) ) ;
#49288=CARTESIAN_POINT ( 'NONE',  ( 7.778174593052021635, 7.778174593052023411, 110.1250000040967763 ) ) ;
#49289=ORIENTED_EDGE ( 'NONE', *, *, #54673, .T. ) ;
#49295=CARTESIAN_POINT ( 'NONE',  ( 11.00000000000000000, 1.347111479062088405E-15, 109.9375000040967763 ) ) ;
#49298=DIRECTION ( 'NONE',  ( 1.000000000000000000, 1.577021341797097560E-16, 0.000000000000000000 ) ) ;
#49302=CYLINDRICAL_SURFACE ( 'NONE', #12232, 11.00000000000000000 ) ;
#49304=VERTEX_POINT ( 'NONE', #63711 ) ;
#49311=CARTESIAN_POINT ( 'NONE',  ( -10.18810118749999916, 4.220049686691934809, 84.43750000204838102 ) ) ;
#49313=CARTESIAN_POINT ( 'NONE',  ( 4.220049686691934809, 10.18810118749999916, 112.1875000020483810 ) ) ;
#49321=EDGE_CURVE ( 'NONE', #37225, #8408, #22389, .T. ) ;
#49325=CARTESIAN_POINT ( 'NONE',  ( -4.556349186104045934, 11.00000000000000000, 113.2187500000000000 ) ) ;
#49329=CARTESIAN_POINT ( 'NONE',  ( -10.18810118749999916, 4.220049686691934809, 109.9375000020483810 ) ) ;
#49365=( BOUNDED_CURVE ( )  B_SPLINE_CURVE ( 2, ( #34145, #57144, #17132, #5836, #56400, #22790, #5094, #51469, #16016 ),
 .UNSPECIFIED., .F., .F. ) 
 B_SPLINE_CURVE_WITH_KNOTS ( ( 3, 2, 2, 2, 3 ),
 ( 0.1470588235294118529, 0.1507352941176471339, 0.1544117647058824427, 0.1580882352941177238, 0.1617647058823530326 ),
 .UNSPECIFIED. ) 
 CURVE ( )  GEOMETRIC_REPRESENTATION_ITEM ( )  RATIONAL_B_SPLINE_CURVE ( ( 0.9999999999999982236, 0.9238795325112885148, 1.000000000000000000, 0.9238795325112867385, 1.000000000000000000, 0.9238795325112867385, 1.000000000000000000, 0.9238795325112849621, 1.000000000000001776 ) ) 
 REPRESENTATION_ITEM ( '' )  );
#49367=CARTESIAN_POINT ( 'NONE',  ( 4.220049686691934809, 10.18810118749999916, 80.68750000204836681 ) ) ;
#49370=CARTESIAN_POINT ( 'NONE',  ( -7.778174593052023411, 7.778174593052023411, 90.81249999999998579 ) ) ;
#49384=DIRECTION ( 'NONE',  ( -0.000000000000000000, -0.000000000000000000, -1.000000000000000000 ) ) ;
#49394=ORIENTED_EDGE ( 'NONE', *, *, #64472, .F. ) ;
#49398=CARTESIAN_POINT ( 'NONE',  ( 7.778174593052023411, -7.778174593052021635, 81.25000000409676204 ) ) ;
#49416=CARTESIAN_POINT ( 'NONE',  ( 10.18810118749999916, 4.220049686691935698, 77.50000000204839523 ) ) ;
#49417=DIRECTION ( 'NONE',  ( -0.000000000000000000, -0.000000000000000000, -1.000000000000000000 ) ) ;
#49428=CARTESIAN_POINT ( 'NONE',  ( 7.204075437095966983, 7.204075437095967871, 85.46875000204836681 ) ) ;
#49431=CARTESIAN_POINT ( 'NONE',  ( 4.556349186104052151, -10.99999999999999822, 90.15625000409677625 ) ) ;
#49434=CARTESIAN_POINT ( 'NONE',  ( 4.220049686691934809, 10.18810118749999916, 92.68750000204838102 ) ) ;
#49443=CARTESIAN_POINT ( 'NONE',  ( -10.18810118749999916, 4.220049686691934809, 94.93750000204838102 ) ) ;
#49453=CARTESIAN_POINT ( 'NONE',  ( -10.99999999999994671, -4.556349186104105442, 95.78125000409679046 ) ) ;
#49460=CARTESIAN_POINT ( 'NONE',  ( 7.204075437095968759, -7.204075437095966983, 98.21875000204838102 ) ) ;
#49486=FACE_OUTER_BOUND ( 'NONE', #2641, .T. ) ;
#49488=DIRECTION ( 'NONE',  ( 0.000000000000000000, 0.000000000000000000, 1.000000000000000000 ) ) ;
#49489=ORIENTED_EDGE ( 'NONE', *, *, #1104, .T. ) ;
#49490=EDGE_CURVE ( 'NONE', #58474, #44494, #24822, .T. ) ;
#49493=CARTESIAN_POINT ( 'NONE',  ( 11.00000000000000000, 4.556349186104045934, 101.0312500040967620 ) ) ;
#49514=EDGE_CURVE ( 'NONE', #31332, #2280, #60483, .T. ) ;
#49517=CARTESIAN_POINT ( 'NONE',  ( 10.18810118749999916, 1.247682550866122264E-15, 106.2812500020483810 ) ) ;
#49518=ORIENTED_EDGE ( 'NONE', *, *, #23102, .F. ) ;
#49526=CARTESIAN_POINT ( 'NONE',  ( -10.18810118749999738, -4.220049686691941915, 112.7500000020483810 ) ) ;
#49534=ADVANCED_FACE ( 'NONE', ( #54632 ), #60651, .T. ) ;
#49536=CARTESIAN_POINT ( 'NONE',  ( -4.220049686691935698, 10.18810118749999916, 112.7500000020483810 ) ) ;
#49553=CARTESIAN_POINT ( 'NONE',  ( 4.220049686691934809, 10.18810118749999916, 116.6875000020483952 ) ) ;
#49562=PLANE ( 'NONE',  #48202 ) ;
#49568=DIRECTION ( 'NONE',  ( -0.000000000000000000, -0.000000000000000000, -1.000000000000000000 ) ) ;
#49575=FACE_OUTER_BOUND ( 'NONE', #28520, .T. ) ;
#49576=CARTESIAN_POINT ( 'NONE',  ( 5.094044972490348933, 8.823157690132404696, 67.53052377765949643 ) ) ;
#49577=CARTESIAN_POINT ( 'NONE',  ( -4.556349186104048599, -10.99999999999999822, 82.46875000409677625 ) ) ;
#49578=CARTESIAN_POINT ( 'NONE',  ( -11.00000000000000000, 0.000000000000000000, 118.0000000000000000 ) ) ;
#49579=LINE ( 'NONE', #38271, #33902 ) ;
#49583=CARTESIAN_POINT ( 'NONE',  ( 11.00000000000000000, 1.347111479062088405E-15, 76.93750000409677625 ) ) ;
#49607=CARTESIAN_POINT ( 'NONE',  ( 7.204075437095966983, 7.204075437095967871, 95.59375000204836681 ) ) ;
#49620=CARTESIAN_POINT ( 'NONE',  ( 10.18810118749999916, 1.247682550866122264E-15, 85.28125000204836681 ) ) ;
#49623=ORIENTED_EDGE ( 'NONE', *, *, #25899, .F. ) ;
#49635=CARTESIAN_POINT ( 'NONE',  ( -4.220049686691935698, 10.18810118749999916, 80.87500000204836681 ) ) ;
#49669=CARTESIAN_POINT ( 'NONE',  ( -11.00000000000000000, 4.556349186104045934, 69.90624999999998579 ) ) ;
#49681=CARTESIAN_POINT ( 'NONE',  ( 11.00000000000000000, 1.347111479062088405E-15, 112.9375000040967763 ) ) ;
#49689=DIRECTION ( 'NONE',  ( 0.000000000000000000, 0.000000000000000000, -1.000000000000000000 ) ) ;
#49700=CARTESIAN_POINT ( 'NONE',  ( -4.220049686691935698, 10.18810118749999916, 112.3750000020483810 ) ) ;
#49713=CARTESIAN_POINT ( 'NONE',  ( 4.220049686691941027, -10.18810118749999738, 106.0000000020483668 ) ) ;
#49751=CARTESIAN_POINT ( 'NONE',  ( 1.871523826299183495E-15, -10.18810118749999916, 83.03125000204838102 ) ) ;
#49754=CARTESIAN_POINT ( 'NONE',  ( 7.778174593052021635, 7.778174593052023411, 87.43749999999998579 ) ) ;
#49758=CARTESIAN_POINT ( 'NONE',  ( 11.00000000000010836, -4.556349186103939353, 84.15624999999998579 ) ) ;
#49763=ORIENTED_EDGE ( 'NONE', *, *, #7352, .F. ) ;
#49781=AXIS2_PLACEMENT_3D ( 'NONE', #18740, #71507, #19831 ) ;
#49784=CARTESIAN_POINT ( 'NONE',  ( -4.556349186104047710, -10.99999999999999822, 77.96875000409679046 ) ) ;
#49787=CARTESIAN_POINT ( 'NONE',  ( -11.00000000000000000, 0.000000000000000000, 79.18750000409677625 ) ) ;
#49800=CARTESIAN_POINT ( 'NONE',  ( -6.238412754330611322E-16, 10.18810118749999916, 77.78125000204836681 ) ) ;
#49801=CARTESIAN_POINT ( 'NONE',  ( -11.00000000000000000, 0.000000000000000000, 99.99999999999998579 ) ) ;
#49807=CARTESIAN_POINT ( 'NONE',  ( 1.871523826299183495E-15, -10.18810118749999916, 84.90625000204838102 ) ) ;
#49810=CARTESIAN_POINT ( 'NONE',  ( -4.556349186104045934, 11.00000000000000000, 105.7187499999999858 ) ) ;
#49812=CARTESIAN_POINT ( 'NONE',  ( -4.220049686691935698, 10.18810118749999916, 94.37500000204839523 ) ) ;
#49819=CARTESIAN_POINT ( 'NONE',  ( -6.238412754330611322E-16, 10.18810118749999916, 91.65625000204836681 ) ) ;
#49836=CARTESIAN_POINT ( 'NONE',  ( -4.220049686691935698, 10.18810118749999916, 98.87500000204838102 ) ) ;
#49839=CARTESIAN_POINT ( 'NONE',  ( 2.020667218593132706E-15, -11.00000000000000000, 106.3750000000000000 ) ) ;
#49870=CARTESIAN_POINT ( 'NONE',  ( 11.00000000000000355, -4.556349186104045046, 96.34375000409677625 ) ) ;
#49872=ADVANCED_FACE ( 'NONE', ( #68547 ), #16850, .T. ) ;
#49874=LINE ( 'NONE', #72889, #38223 ) ;
#49892=FACE_OUTER_BOUND ( 'NONE', #28944, .T. ) ;
#49893=CARTESIAN_POINT ( 'NONE',  ( 10.18810118750000093, -4.220049686691933921, 101.6875000020483810 ) ) ;
#49894=ORIENTED_EDGE ( 'NONE', *, *, #47443, .F. ) ;
#49898=CARTESIAN_POINT ( 'NONE',  ( -11.00000000000000000, 0.000000000000000000, 98.49999999999998579 ) ) ;
#49903=CARTESIAN_POINT ( 'NONE',  ( -10.18810118749999916, 0.000000000000000000, 114.1562500020483810 ) ) ;
#49911=CARTESIAN_POINT ( 'NONE',  ( -10.18810118749999916, 0.000000000000000000, 108.5312500020483810 ) ) ;
#49912=PRODUCT ( 'square bolt', 'square bolt', '', ( #22178 ) ) ;
#49920=CARTESIAN_POINT ( 'NONE',  ( 10.18810118749999916, 4.220049686691935698, 71.87500000204836681 ) ) ;
#49925=CARTESIAN_POINT ( 'NONE',  ( -4.556349186104045934, 11.00000000000000000, 90.71874999999998579 ) ) ;
#49927=CARTESIAN_POINT ( 'NONE',  ( -10.18810118749999916, 0.000000000000000000, 117.1562500020483810 ) ) ;
#49943=DIRECTION ( 'NONE',  ( -1.000000000000000000, 0.000000000000000000, 0.000000000000000000 ) ) ;
#49951=CARTESIAN_POINT ( 'NONE',  ( -11.00000000000000000, 0.000000000000000000, 88.18750000409677625 ) ) ;
#49955=CYLINDRICAL_SURFACE ( 'NONE', #14577, 11.00000000000000000 ) ;
#49961=CARTESIAN_POINT ( 'NONE',  ( 7.778174593052023411, -7.778174593052021635, 79.56249999999998579 ) ) ;
#49975=ORIENTED_EDGE ( 'NONE', *, *, #41335, .T. ) ;
#49977=CARTESIAN_POINT ( 'NONE',  ( -4.220049686691935698, 10.18810118749999916, 86.87500000204836681 ) ) ;
#49978=CARTESIAN_POINT ( 'NONE',  ( 0.000000000000000000, 0.000000000000000000, 118.0000000000000000 ) ) ;
#49985=EDGE_CURVE ( 'NONE', #66203, #29969, #23492, .T. ) ;
#49990=CARTESIAN_POINT ( 'NONE',  ( 10.18810118750000093, -4.220049686691933033, 82.18750000204836681 ) ) ;
#50003=CARTESIAN_POINT ( 'NONE',  ( -6.238412754330611322E-16, 10.18810118749999916, 74.78125000204836681 ) ) ;
#50025=ORIENTED_EDGE ( 'NONE', *, *, #34457, .F. ) ;
#50032=( BOUNDED_CURVE ( )  B_SPLINE_CURVE ( 2, ( #65238, #46782, #70905, #794, #41864, #1532, #12084, #24512, #1159 ),
 .UNSPECIFIED., .F., .F. ) 
 B_SPLINE_CURVE_WITH_KNOTS ( ( 3, 2, 2, 2, 3 ),
 ( 0.7647058823529411242, 0.7683823529411765163, 0.7720588235294117974, 0.7757352941176470784, 0.7794117647058823595 ),
 .UNSPECIFIED. ) 
 CURVE ( )  GEOMETRIC_REPRESENTATION_ITEM ( )  RATIONAL_B_SPLINE_CURVE ( ( 1.000000000000000000, 0.9238795325112867385, 1.000000000000000000, 0.9238795325112867385, 1.000000000000000000, 0.9238795325112867385, 1.000000000000000000, 0.9238795325112867385, 1.000000000000000000 ) ) 
 REPRESENTATION_ITEM ( '' )  );
#50039=CARTESIAN_POINT ( 'NONE',  ( 11.00000000000000000, 4.556349186104045934, 73.84374999999998579 ) ) ;
#50054=CARTESIAN_POINT ( 'NONE',  ( -11.00000000000000000, 0.000000000000000000, 86.50000000000000000 ) ) ;
#50067=CARTESIAN_POINT ( 'NONE',  ( 10.18810118749999916, 1.247682550866122264E-15, 105.9062500020483810 ) ) ;
#50083=CARTESIAN_POINT ( 'NONE',  ( -7.204075437095965206, -7.204075437095968759, 99.71875000204838102 ) ) ;
#50091=CARTESIAN_POINT ( 'NONE',  ( 11.00000000000000000, 1.347111479062088405E-15, 72.43750000409676204 ) ) ;
#50103=CARTESIAN_POINT ( 'NONE',  ( 10.18810118750000093, -4.220049686691933921, 82.18750000204836681 ) ) ;
#50105=EDGE_CURVE ( 'NONE', #46282, #6126, #62504, .T. ) ;
#50122=CARTESIAN_POINT ( 'NONE',  ( 10.18810118750000093, -4.220049686691933033, 74.31250000204836681 ) ) ;
#50125=CARTESIAN_POINT ( 'NONE',  ( 11.00000000000000000, 4.556349186104045934, 91.84374999999998579 ) ) ;
#50129=CARTESIAN_POINT ( 'NONE',  ( -7.778174593052020747, -7.778174593052023411, 83.68750000000000000 ) ) ;
#50138=CARTESIAN_POINT ( 'NONE',  ( 7.778174593052023411, -7.778174593052021635, 99.25000000409679046 ) ) ;
#50153=CARTESIAN_POINT ( 'NONE',  ( -7.778174593052020747, -7.778174593052023411, 74.87500000409677625 ) ) ;
#50170=CARTESIAN_POINT ( 'NONE',  ( -10.18810118749999916, 0.000000000000000000, 75.15625000204836681 ) ) ;
#50178=CARTESIAN_POINT ( 'NONE',  ( 4.220049686691941027, -10.18810118749999738, 83.50000000204840944 ) ) ;
#50180=CYLINDRICAL_SURFACE ( 'NONE', #32891, 11.00000000000000000 ) ;
#50181=CARTESIAN_POINT ( 'NONE',  ( 4.556349186104045934, 11.00000000000000000, 105.5312500000000142 ) ) ;
#50184=VERTEX_POINT ( 'NONE', #65476 ) ;
#50190=CARTESIAN_POINT ( 'NONE',  ( -7.204075437095967871, 7.204075437095967871, 91.84375000204838102 ) ) ;
#50201=CARTESIAN_POINT ( 'NONE',  ( 2.020667218593132706E-15, -11.00000000000000000, 96.06250000409677625 ) ) ;
#50207=CARTESIAN_POINT ( 'NONE',  ( -7.204075437095967871, 7.204075437095967871, 94.46875000204838102 ) ) ;
#50209=CARTESIAN_POINT ( 'NONE',  ( -6.735557395310442023E-16, 11.00000000000000000, 108.6250000000000000 ) ) ;
#50223=DIRECTION ( 'NONE',  ( -7.885106708985487801E-17, 1.000000000000000000, -0.000000000000000000 ) ) ;
#50233=DIRECTION ( 'NONE',  ( -1.000000000000000000, 0.000000000000000000, 0.000000000000000000 ) ) ;
#50239=CARTESIAN_POINT ( 'NONE',  ( -11.00000000000000000, 0.000000000000000000, 98.68750000409677625 ) ) ;
#50252=ORIENTED_EDGE ( 'NONE', *, *, #43625, .F. ) ;
#50259=CARTESIAN_POINT ( 'NONE',  ( 1.871523826299183495E-15, -10.18810118749999916, 104.4062500020483810 ) ) ;
#50271=CARTESIAN_POINT ( 'NONE',  ( -7.204075437095965206, -7.204075437095968759, 114.3437500020483810 ) ) ;
#50278=FACE_OUTER_BOUND ( 'NONE', #61707, .T. ) ;
#50280=CARTESIAN_POINT ( 'NONE',  ( 4.556349186104052151, -10.99999999999999822, 103.6562500040967905 ) ) ;
#50281=CARTESIAN_POINT ( 'NONE',  ( 7.204075437095966983, 7.204075437095967871, 110.9687500020483810 ) ) ;
#50290=AXIS2_PLACEMENT_3D ( 'NONE', #10705, #62744, #46148 ) ;
#50297=CARTESIAN_POINT ( 'NONE',  ( 7.204075437095966983, 7.204075437095967871, 113.5937500020483810 ) ) ;
#50345=CARTESIAN_POINT ( 'NONE',  ( -7.204075437095965206, -7.204075437095968759, 90.34375000204838102 ) ) ;
#50346=CARTESIAN_POINT ( 'NONE',  ( 7.778174593052021635, 7.778174593052023411, 93.43749999999998579 ) ) ;
#50358=CARTESIAN_POINT ( 'NONE',  ( 1.871523826299183495E-15, -10.18810118749999916, 80.40625000204838102 ) ) ;
#50365=EDGE_CURVE ( 'NONE', #18351, #37225, #2759, .T. ) ;
#50366=DIRECTION ( 'NONE',  ( -0.000000000000000000, -0.000000000000000000, -1.000000000000000000 ) ) ;
#50371=EDGE_CURVE ( 'NONE', #2929, #18351, #6118, .T. ) ;
#50373=CARTESIAN_POINT ( 'NONE',  ( 4.220049686691941027, -10.18810118749999738, 77.12500000204838102 ) ) ;
#50406=CARTESIAN_POINT ( 'NONE',  ( -11.00000000000001421, -4.556349186104037052, 115.2812500040967763 ) ) ;
#50411=CARTESIAN_POINT ( 'NONE',  ( -7.778174593052023411, 7.778174593052023411, 68.31249999999998579 ) ) ;
#50433=EDGE_LOOP ( 'NONE', ( #12806, #60211, #45431, #45817 ) ) ;
#50436=CARTESIAN_POINT ( 'NONE',  ( -7.204075437095967871, 7.204075437095967871, 104.9687500020483810 ) ) ;
#50447=CARTESIAN_POINT ( 'NONE',  ( 4.220049686691934809, 10.18810118749999916, 100.5625000020483668 ) ) ;
#50452=DIRECTION ( 'NONE',  ( 1.000000000000000000, 0.000000000000000000, 0.000000000000000000 ) ) ;
#50468=CARTESIAN_POINT ( 'NONE',  ( -7.204075437095965206, -7.204075437095968759, 80.21875000204836681 ) ) ;
#50475=CARTESIAN_POINT ( 'NONE',  ( -11.00000000000000000, 0.000000000000000000, 118.0000000000000000 ) ) ;
#50483=ADVANCED_FACE ( 'NONE', ( #25378 ), #35988, .T. ) ;
#50488=CARTESIAN_POINT ( 'NONE',  ( -4.220049686691935698, 10.18810118749999916, 74.87500000204836681 ) ) ;
#50491=CARTESIAN_POINT ( 'NONE',  ( 7.778174593052021635, 7.778174593052023411, 91.93749999999998579 ) ) ;
#50500=VERTEX_POINT ( 'NONE', #19724 ) ;
#50512=DIRECTION ( 'NONE',  ( -0.000000000000000000, -0.000000000000000000, -1.000000000000000000 ) ) ;
#50518=CARTESIAN_POINT ( 'NONE',  ( 7.778174593052021635, 7.778174593052023411, 72.62500000409677625 ) ) ;
#50534=CARTESIAN_POINT ( 'NONE',  ( 10.18810118750000093, -4.220049686691933033, 116.6875000020483952 ) ) ;
#50537=CARTESIAN_POINT ( 'NONE',  ( -7.204075437095965206, -7.204075437095968759, 70.84375000204836681 ) ) ;
#50540=FACE_OUTER_BOUND ( 'NONE', #43311, .T. ) ;
#50543=CARTESIAN_POINT ( 'NONE',  ( -11.00000000000000000, 0.000000000000000000, 79.18750000409677625 ) ) ;
#50546=CARTESIAN_POINT ( 'NONE',  ( -10.18810118749999738, -4.220049686691941915, 81.62500000204836681 ) ) ;
#50555=ORIENTED_EDGE ( 'NONE', *, *, #5266, .F. ) ;
#50560=CARTESIAN_POINT ( 'NONE',  ( -4.220049686691935698, 10.18810118749999916, 93.25000000204838102 ) ) ;
#50574=ORIENTED_EDGE ( 'NONE', *, *, #25734, .F. ) ;
#50575=CARTESIAN_POINT ( 'NONE',  ( 7.204075437095968759, -7.204075437095966983, 90.71875000204838102 ) ) ;
#50578=CARTESIAN_POINT ( 'NONE',  ( -7.778174593052020747, -7.778174593052023411, 107.6874999999999858 ) ) ;
#50601=DIRECTION ( 'NONE',  ( -1.000000000000000000, 0.000000000000000000, 0.000000000000000000 ) ) ;
#50608=CARTESIAN_POINT ( 'NONE',  ( -7.778174593052023411, 7.778174593052023411, 92.50000000409677625 ) ) ;
#50622=VERTEX_POINT ( 'NONE', #72911 ) ;
#50630=CARTESIAN_POINT ( 'NONE',  ( -10.18810118749999916, 4.220049686691934809, 96.43750000204836681 ) ) ;
#50640=CARTESIAN_POINT ( 'NONE',  ( 1.871523826299183495E-15, -10.18810118749999916, 116.0312500020483810 ) ) ;
#50647=CARTESIAN_POINT ( 'NONE',  ( -7.204075437095967871, 7.204075437095967871, 108.3437500020483810 ) ) ;
#50664=CARTESIAN_POINT ( 'NONE',  ( -7.204075437095965206, -7.204075437095968759, 111.3437500020483810 ) ) ;
#50687=CARTESIAN_POINT ( 'NONE',  ( -11.00000000000000000, 0.000000000000000000, 82.18750000409677625 ) ) ;
#50716=CARTESIAN_POINT ( 'NONE',  ( 4.220049686691934809, 10.18810118749999916, 86.68750000204836681 ) ) ;
#50720=CARTESIAN_POINT ( 'NONE',  ( -11.00000000000000000, 0.000000000000000000, 113.4999999999999858 ) ) ;
#50730=CARTESIAN_POINT ( 'NONE',  ( 7.204075437095966983, 7.204075437095967871, 82.46875000204836681 ) ) ;
#50743=CARTESIAN_POINT ( 'NONE',  ( -10.18810118749999738, -4.220049686691941915, 78.25000000204836681 ) ) ;
#50757=CARTESIAN_POINT ( 'NONE',  ( -10.99999999999999822, -4.556349186104053040, 73.28125000409677625 ) ) ;
#50779=CARTESIAN_POINT ( 'NONE',  ( -6.735557395310442023E-16, 11.00000000000000000, 71.12500000000000000 ) ) ;
#50809=CARTESIAN_POINT ( 'NONE',  ( -10.18810118749999738, -4.220049686691941915, 105.2500000020483952 ) ) ;
#50813=CARTESIAN_POINT ( 'NONE',  ( -7.778174593052020747, -7.778174593052023411, 97.18749999999998579 ) ) ;
#50825=CARTESIAN_POINT ( 'NONE',  ( -6.238412754330611322E-16, 10.18810118749999916, 100.6562500020483810 ) ) ;
#50844=CARTESIAN_POINT ( 'NONE',  ( 10.18810118749999916, 1.247682550866122264E-15, 82.28125000204838102 ) ) ;
#50864=CARTESIAN_POINT ( 'NONE',  ( 4.220049686691934809, 10.18810118749999916, 74.68750000204838102 ) ) ;
#50867=CARTESIAN_POINT ( 'NONE',  ( -11.00000000000000000, 0.000000000000000000, 86.50000000000000000 ) ) ;
#50892=CARTESIAN_POINT ( 'NONE',  ( -4.556349186104045934, 11.00000000000000000, 80.40625000409676204 ) ) ;
#50894=CARTESIAN_POINT ( 'NONE',  ( -10.99999999999999822, -4.556349186104052151, 76.28125000409676204 ) ) ;
#50912=CARTESIAN_POINT ( 'NONE',  ( -4.220049686691937474, -10.18810118749999738, 69.43750000204838102 ) ) ;
#50923=CARTESIAN_POINT ( 'NONE',  ( 10.18810118749999916, 4.220049686691935698, 77.87500000204838102 ) ) ;
#50947=( NAMED_UNIT ( * ) SI_UNIT ( $, .STERADIAN. ) SOLID_ANGLE_UNIT ( ) );
#50951=ADVANCED_FACE ( 'NONE', ( #28741 ), #16289, .T. ) ;
#50953=CARTESIAN_POINT ( 'NONE',  ( 7.204075437095968759, -7.204075437095966983, 92.21875000204838102 ) ) ;
#50955=CARTESIAN_POINT ( 'NONE',  ( -4.556349186104045934, 11.00000000000000000, 108.7187499999999858 ) ) ;
#50979=PRODUCT_DEFINITION ( 'UNKNOWN', '', #53833, #74226 ) ;
#50985=CARTESIAN_POINT ( 'NONE',  ( 2.020667218593132706E-15, -11.00000000000000000, 91.56250000409677625 ) ) ;
#51006=( LENGTH_UNIT ( ) NAMED_UNIT ( * ) SI_UNIT ( .MILLI., .METRE. ) );
#51010=CARTESIAN_POINT ( 'NONE',  ( 4.220049686691941027, -10.18810118749999738, 100.0000000020483668 ) ) ;
#51018=CARTESIAN_POINT ( 'NONE',  ( 7.204075437095966983, 7.204075437095967871, 115.0937500020483810 ) ) ;
#51027=CARTESIAN_POINT ( 'NONE',  ( 10.18810118749999916, 1.247682550866122264E-15, 112.2812500020483810 ) ) ;
#51045=CARTESIAN_POINT ( 'NONE',  ( 7.204075437095968759, -7.204075437095966983, 111.7187500020483810 ) ) ;
#51046=CARTESIAN_POINT ( 'NONE',  ( -11.00000000000000000, 0.000000000000000000, 97.18750000409677625 ) ) ;
#51053=CYLINDRICAL_SURFACE ( 'NONE', #51782, 11.00000000000000000 ) ;
#51064=CARTESIAN_POINT ( 'NONE',  ( 7.778174593052023411, -7.778174593052021635, 82.75000000409676204 ) ) ;
#51071=CARTESIAN_POINT ( 'NONE',  ( -7.778174593052020747, -7.778174593052023411, 110.8750000040967763 ) ) ;
#51093=CARTESIAN_POINT ( 'NONE',  ( 4.220049686691941027, -10.18810118749999738, 89.12500000204836681 ) ) ;
#51098=CARTESIAN_POINT ( 'NONE',  ( 4.220049686691934809, 10.18810118749999916, 114.0625000020483668 ) ) ;
#51099=ORIENTED_EDGE ( 'NONE', *, *, #23828, .F. ) ;
#51106=CARTESIAN_POINT ( 'NONE',  ( -7.204075437095967871, 7.204075437095967871, 81.34375000204838102 ) ) ;
#51119=CARTESIAN_POINT ( 'NONE',  ( 1.871523826299183495E-15, -10.18810118749999916, 80.03125000204836681 ) ) ;
#51131=EDGE_CURVE ( 'NONE', #38757, #33088, #57238, .T. ) ;
#51149=( BOUNDED_CURVE ( )  B_SPLINE_CURVE ( 2, ( #46616, #35322, #46981, #19055, #18694, #42058, #18321, #17950, #2078 ),
 .UNSPECIFIED., .F., .F. ) 
 B_SPLINE_CURVE_WITH_KNOTS ( ( 3, 2, 2, 2, 3 ),
 ( 0.9411764705882353921, 0.9448529411764706731, 0.9485294117647058432, 0.9522058823529411242, 0.9558823529411765163 ),
 .UNSPECIFIED. ) 
 CURVE ( )  GEOMETRIC_REPRESENTATION_ITEM ( )  RATIONAL_B_SPLINE_CURVE ( ( 0.9999999999999976685, 0.9238795325112890700, 1.000000000000000000, 0.9238795325112867385, 1.000000000000000000, 0.9238795325112867385, 1.000000000000000000, 0.9238795325112867385, 1.000000000000000000 ) ) 
 REPRESENTATION_ITEM ( '' )  );
#51163=CARTESIAN_POINT ( 'NONE',  ( 11.00000000000000000, 1.347111479062088405E-15, 76.74999999999998579 ) ) ;
#51180=ORIENTED_EDGE ( 'NONE', *, *, #10691, .T. ) ;
#51182=CARTESIAN_POINT ( 'NONE',  ( 10.18810118749999916, 1.247682550866122264E-15, 104.4062500020483810 ) ) ;
#51198=CARTESIAN_POINT ( 'NONE',  ( 4.220049686691934809, 10.18810118749999916, 102.0625000020483810 ) ) ;
#51212=CARTESIAN_POINT ( 'NONE',  ( -4.220049686691937474, -10.18810118749999738, 97.93750000204836681 ) ) ;
#51217=ADVANCED_FACE ( 'NONE', ( #25661 ), #50180, .T. ) ;
#51221=CARTESIAN_POINT ( 'NONE',  ( -4.220049686691935698, 10.18810118749999916, 82.75000000204838102 ) ) ;
#51222=ORIENTED_EDGE ( 'NONE', *, *, #10232, .F. ) ;
#51238=CARTESIAN_POINT ( 'NONE',  ( 4.220049686691941027, -10.18810118749999738, 74.12500000204836681 ) ) ;
#51241=CARTESIAN_POINT ( 'NONE',  ( -4.556349186104047710, -10.99999999999999822, 83.78125000000000000 ) ) ;
#51268=CARTESIAN_POINT ( 'NONE',  ( -10.99999999999999822, -4.556349186104052151, 73.28125000409677625 ) ) ;
#51286=CARTESIAN_POINT ( 'NONE',  ( 7.204075437095968759, -7.204075437095966983, 74.21875000204836681 ) ) ;
#51292=CARTESIAN_POINT ( 'NONE',  ( 11.00000000000000000, 1.347111479062088405E-15, 79.93750000409677625 ) ) ;
#51308=VECTOR ( 'NONE', #58570, 1000.000000000000000 ) ;
#51324=CARTESIAN_POINT ( 'NONE',  ( 1.871523826299183495E-15, -10.18810118749999916, 93.53125000204836681 ) ) ;
#51327=CARTESIAN_POINT ( 'NONE',  ( -7.778174593052023411, 7.778174593052023411, 105.8124999999999858 ) ) ;
#51330=CARTESIAN_POINT ( 'NONE',  ( 1.734723475976807489E-15, -16.00000000000000355, 38.34805510287551300 ) ) ;
#51348=CARTESIAN_POINT ( 'NONE',  ( -11.00000000000000000, 0.000000000000000000, 103.1875000040967763 ) ) ;
#51354=CARTESIAN_POINT ( 'NONE',  ( 4.556349186104045934, 11.00000000000000000, 93.71875000409676204 ) ) ;
#51378=CARTESIAN_POINT ( 'NONE',  ( 1.871523826299183495E-15, -10.18810118749999916, 98.40625000204838102 ) ) ;
#51380=AXIS2_PLACEMENT_3D ( 'NONE', #49978, #62042, #49225 ) ;
#51386=CARTESIAN_POINT ( 'NONE',  ( 10.18810118750000093, -4.220049686691933921, 110.3125000020483810 ) ) ;
#51395=CARTESIAN_POINT ( 'NONE',  ( -10.18810118749999738, -4.220049686691941915, 104.1250000020483810 ) ) ;
#51412=ORIENTED_EDGE ( 'NONE', *, *, #23939, .T. ) ;
#51413=CARTESIAN_POINT ( 'NONE',  ( 7.204075437095968759, -7.204075437095966983, 110.2187500020483810 ) ) ;
#51429=CARTESIAN_POINT ( 'NONE',  ( -11.00000000000000000, 0.000000000000000000, 88.00000000000000000 ) ) ;
#51440=CARTESIAN_POINT ( 'NONE',  ( -11.00000000000000000, 0.000000000000000000, 112.1875000040967763 ) ) ;
#51461=CARTESIAN_POINT ( 'NONE',  ( 4.220049686691941027, -10.18810118749999738, 86.12500000204836681 ) ) ;
#51466=EDGE_CURVE ( 'NONE', #33088, #13669, #11397, .T. ) ;
#51467=CARTESIAN_POINT ( 'NONE',  ( 7.204075437095966983, 7.204075437095967871, 113.9687500020483810 ) ) ;
#51469=CARTESIAN_POINT ( 'NONE',  ( 11.00000000000007994, 4.556349186103967774, 108.5312500040967905 ) ) ;
#51475=CARTESIAN_POINT ( 'NONE',  ( -4.220049686691935698, 10.18810118749999916, 78.25000000204838102 ) ) ;
#51490=CARTESIAN_POINT ( 'NONE',  ( 7.204075437095966983, 7.204075437095967871, 74.59375000204838102 ) ) ;
#51499=CARTESIAN_POINT ( 'NONE',  ( 11.00000000000000000, 1.347111479062088405E-15, 75.43750000409676204 ) ) ;
#51511=CARTESIAN_POINT ( 'NONE',  ( 4.556349186104045934, 11.00000000000000000, 74.21875000409676204 ) ) ;
#51550=CARTESIAN_POINT ( 'NONE',  ( -6.238412754330611322E-16, 10.18810118749999916, 107.7812500020483810 ) ) ;
#51566=CARTESIAN_POINT ( 'NONE',  ( -4.220049686691935698, 10.18810118749999916, 97.75000000204838102 ) ) ;
#51579=CARTESIAN_POINT ( 'NONE',  ( -4.220049686691935698, 10.18810118749999916, 92.87500000204838102 ) ) ;
#51591=CARTESIAN_POINT ( 'NONE',  ( -10.18810118749999916, 4.220049686691934809, 79.93750000204839523 ) ) ;
#51592=ORIENTED_EDGE ( 'NONE', *, *, #70693, .F. ) ;
#51594=( BOUNDED_CURVE ( )  B_SPLINE_CURVE ( 2, ( #8669, #1550, #47536, #7563, #70561, #18877, #59613, #25260, #71285 ),
 .UNSPECIFIED., .F., .F. ) 
 B_SPLINE_CURVE_WITH_KNOTS ( ( 3, 2, 2, 2, 3 ),
 ( 0.2352941176470586815, 0.2389705882352939903, 0.2426470588235292714, 0.2463235294117645802, 0.2499999999999998612 ),
 .UNSPECIFIED. ) 
 CURVE ( )  GEOMETRIC_REPRESENTATION_ITEM ( )  RATIONAL_B_SPLINE_CURVE ( ( 1.000000000000002887, 0.9238795325112838519, 1.000000000000000000, 0.9238795325112867385, 1.000000000000000000, 0.9238795325112867385, 1.000000000000000000, 0.9238795325112896251, 0.9999999999999971134 ) ) 
 REPRESENTATION_ITEM ( '' )  );
#51606=EDGE_LOOP ( 'NONE', ( #48147, #42846, #36726, #38814 ) ) ;
#51612=CARTESIAN_POINT ( 'NONE',  ( -10.18810118749999916, 4.220049686691934809, 75.06250000204836681 ) ) ;
#51615=CARTESIAN_POINT ( 'NONE',  ( -11.00000000000000000, 4.556349186104045934, 81.90625000000000000 ) ) ;
#51618=CYLINDRICAL_SURFACE ( 'NONE', #15732, 11.00000000000000000 ) ;
#51645=CARTESIAN_POINT ( 'NONE',  ( -7.778174593052020747, -7.778174593052023411, 73.37500000409677625 ) ) ;
#51662=CARTESIAN_POINT ( 'NONE',  ( -7.204075437095967871, 7.204075437095967871, 68.96875000204836681 ) ) ;
#51679=VECTOR ( 'NONE', #68879, 1000.000000000000000 ) ;
#51696=CARTESIAN_POINT ( 'NONE',  ( -10.18810118749999916, 4.220049686691934809, 90.06250000204838102 ) ) ;
#51699=CARTESIAN_POINT ( 'NONE',  ( -7.778174593052020747, -7.778174593052023411, 103.1874999999999858 ) ) ;
#51716=CARTESIAN_POINT ( 'NONE',  ( 7.778174593052021635, 7.778174593052023411, 85.93749999999998579 ) ) ;
#51727=ADVANCED_FACE ( 'NONE', ( #8519 ), #70423, .T. ) ;
#51730=CARTESIAN_POINT ( 'NONE',  ( -10.99999999999999822, -4.556349186104052151, 94.28125000409676204 ) ) ;
#51731=DIRECTION ( 'NONE',  ( 0.000000000000000000, -1.000000000000000000, 0.000000000000000000 ) ) ;
#51755=CARTESIAN_POINT ( 'NONE',  ( -10.18810118749999916, 4.220049686691934809, 99.43750000204836681 ) ) ;
#51762=CARTESIAN_POINT ( 'NONE',  ( 4.220049686691934809, 10.18810118749999916, 106.1875000020483810 ) ) ;
#51771=CARTESIAN_POINT ( 'NONE',  ( -7.204075437095967871, 7.204075437095967871, 106.8437500020483810 ) ) ;
#51782=AXIS2_PLACEMENT_3D ( 'NONE', #68403, #22363, #74064 ) ;
#51787=CARTESIAN_POINT ( 'NONE',  ( -10.18810118749999738, -4.220049686691941915, 108.2500000020483810 ) ) ;
#51788=CARTESIAN_POINT ( 'NONE',  ( 10.99999999999994849, 4.556349186104097448, 96.53125000409677625 ) ) ;
#51798=ORIENTED_EDGE ( 'NONE', *, *, #33167, .F. ) ;
#51805=CARTESIAN_POINT ( 'NONE',  ( 11.00000000000000000, 1.347111479062088405E-15, 72.43750000409676204 ) ) ;
#51806=CARTESIAN_POINT ( 'NONE',  ( 1.871523826299183495E-15, -10.18810118749999916, 68.40625000204836681 ) ) ;
#51819=CARTESIAN_POINT ( 'NONE',  ( 4.556349186104051263, -10.99999999999999822, 109.6562500040967905 ) ) ;
#51840=CARTESIAN_POINT ( 'NONE',  ( 10.18810118749999916, 4.220049686691935698, 82.00000000204836681 ) ) ;
#51845=CARTESIAN_POINT ( 'NONE',  ( -10.18810118749999916, 4.220049686691934809, 117.4375000020483810 ) ) ;
#51854=CARTESIAN_POINT ( 'NONE',  ( 10.18810118750000093, -4.220049686691933033, 77.68750000204838102 ) ) ;
#51871=CARTESIAN_POINT ( 'NONE',  ( 10.18810118749999916, 4.220049686691935698, 68.50000000204838102 ) ) ;
#51893=EDGE_LOOP ( 'NONE', ( #36235, #13259, #39157, #37616, #23648 ) ) ;
#51910=CARTESIAN_POINT ( 'NONE',  ( -7.778174593052023411, 7.778174593052023411, 85.00000000409677625 ) ) ;
#51935=CARTESIAN_POINT ( 'NONE',  ( -10.18810118749999738, -4.220049686691941915, 103.7500000020483668 ) ) ;
#51953=CARTESIAN_POINT ( 'NONE',  ( 10.18810118749999916, 4.220049686691935698, 97.37500000204839523 ) ) ;
#51957=DIRECTION ( 'NONE',  ( -0.000000000000000000, -0.000000000000000000, -1.000000000000000000 ) ) ;
#51966=CARTESIAN_POINT ( 'NONE',  ( -7.204075437095967871, 7.204075437095967871, 88.46875000204838102 ) ) ;
#51976=CARTESIAN_POINT ( 'NONE',  ( -6.238412754330611322E-16, 10.18810118749999916, 75.15625000204836681 ) ) ;
#51992=EDGE_CURVE ( 'NONE', #1123, #40106, #45826, .T. ) ;
#51997=CARTESIAN_POINT ( 'NONE',  ( 11.00000000000000355, -4.556349186104045046, 84.15624999999998579 ) ) ;
#52019=ORIENTED_EDGE ( 'NONE', *, *, #50365, .F. ) ;
#52020=CARTESIAN_POINT ( 'NONE',  ( 0.000000000000000000, 0.000000000000000000, 118.0000000000000000 ) ) ;
#52023=CARTESIAN_POINT ( 'NONE',  ( 4.556349186104051263, -10.99999999999999822, 69.15625000409676204 ) ) ;
#52037=CARTESIAN_POINT ( 'NONE',  ( 10.18810118749999916, 1.247682550866122264E-15, 110.7812500020483668 ) ) ;
#52041=CARTESIAN_POINT ( 'NONE',  ( -10.18810118749999916, 0.000000000000000000, 70.65625000204836681 ) ) ;
#52072=CARTESIAN_POINT ( 'NONE',  ( 11.00000000000000000, 1.347111479062088405E-15, 96.43750000409677625 ) ) ;
#52082=CARTESIAN_POINT ( 'NONE',  ( -7.204075437095965206, -7.204075437095968759, 84.34375000204836681 ) ) ;
#52085=CARTESIAN_POINT ( 'NONE',  ( -7.778174593052020747, -7.778174593052023411, 98.68749999999998579 ) ) ;
#52116=CARTESIAN_POINT ( 'NONE',  ( -11.00000000000000000, 4.556349186104045934, 94.09375000409679046 ) ) ;
#52127=CARTESIAN_POINT ( 'NONE',  ( 11.00000000000000000, 1.347111479062088405E-15, 102.4375000040967763 ) ) ;
#52138=CARTESIAN_POINT ( 'NONE',  ( 10.18810118750000093, -4.220049686691933921, 95.68750000204838102 ) ) ;
#52144=CARTESIAN_POINT ( 'NONE',  ( -6.238412754330611322E-16, 10.18810118749999916, 106.2812500020483810 ) ) ;
#52147=ORIENTED_EDGE ( 'NONE', *, *, #59129, .T. ) ;
#52153=CARTESIAN_POINT ( 'NONE',  ( -7.204075437095965206, -7.204075437095968759, 102.7187500020483668 ) ) ;
#52171=CARTESIAN_POINT ( 'NONE',  ( 10.18810118749999916, 1.247682550866122264E-15, 113.4062500020483810 ) ) ;
#52189=CARTESIAN_POINT ( 'NONE',  ( 4.220049686691941027, -10.18810118749999738, 68.50000000204838102 ) ) ;
#52193=CARTESIAN_POINT ( 'NONE',  ( 16.00000000000000711, 16.00000000000000355, 20.00000000000000000 ) ) ;
#52200=CARTESIAN_POINT ( 'NONE',  ( 4.556349186104045934, 11.00000000000000000, 110.2187500040968047 ) ) ;
#52203=CARTESIAN_POINT ( 'NONE',  ( -4.556349186104048599, -10.99999999999999822, 107.9687500040967905 ) ) ;
#52213=CARTESIAN_POINT ( 'NONE',  ( 11.00000000000002487, 4.556349186104019289, 115.8437500000000000 ) ) ;
#52220=CARTESIAN_POINT ( 'NONE',  ( -10.18810118749999916, 0.000000000000000000, 84.15625000204838102 ) ) ;
#52223=CYLINDRICAL_SURFACE ( 'NONE', #57912, 11.00000000000000000 ) ;
#52224=CARTESIAN_POINT ( 'NONE',  ( -10.18810118749999916, 0.000000000000000000, 114.5312500020483810 ) ) ;
#52231=CARTESIAN_POINT ( 'NONE',  ( -10.18810118749999916, 0.000000000000000000, 78.53125000204836681 ) ) ;
#52243=CARTESIAN_POINT ( 'NONE',  ( -10.18810118749999738, -4.220049686691941915, 72.25000000204836681 ) ) ;
#52286=ORIENTED_EDGE ( 'NONE', *, *, #49490, .F. ) ;
#52308=CARTESIAN_POINT ( 'NONE',  ( -10.18810118749999916, 0.000000000000000000, 103.6562500020483810 ) ) ;
#52319=CARTESIAN_POINT ( 'NONE',  ( 5.094044972490348933, 8.823157690132404696, 67.53052377765949643 ) ) ;
#52324=CARTESIAN_POINT ( 'NONE',  ( 10.18810118749999916, 4.220049686691935698, 94.37500000204839523 ) ) ;
#52330=CARTESIAN_POINT ( 'NONE',  ( -7.204075437095965206, -7.204075437095968759, 80.21875000204836681 ) ) ;
#52337=CARTESIAN_POINT ( 'NONE',  ( 10.18810118749999916, 1.247682550866122264E-15, 90.90625000204836681 ) ) ;
#52349=CARTESIAN_POINT ( 'NONE',  ( 10.18810118750000093, -4.220049686691933921, 77.68750000204838102 ) ) ;
#52357=CARTESIAN_POINT ( 'NONE',  ( -10.99999999999978684, -4.556349186104264426, 88.28125000409679046 ) ) ;
#52363=ADVANCED_FACE ( 'NONE', ( #50278 ), #54838, .T. ) ;
#52365=CARTESIAN_POINT ( 'NONE',  ( 10.18810118749999916, 4.220049686691935698, 70.00000000204836681 ) ) ;
#52368=CARTESIAN_POINT ( 'NONE',  ( 4.556349186104051263, -10.99999999999999822, 82.46874999999998579 ) ) ;
#52374=DIRECTION ( 'NONE',  ( -1.000000000000000000, 0.000000000000000000, 0.000000000000000000 ) ) ;
#52394=CARTESIAN_POINT ( 'NONE',  ( -10.99999999999989164, -4.556349186104158733, 80.78125000409679046 ) ) ;
#52396=CARTESIAN_POINT ( 'NONE',  ( -10.18810118749999916, 4.220049686691934809, 117.0625000020483668 ) ) ;
#52409=CARTESIAN_POINT ( 'NONE',  ( -4.220049686691937474, -10.18810118749999738, 113.3125000020483668 ) ) ;
#52437=CARTESIAN_POINT ( 'NONE',  ( 16.00000000000000711, 0.000000000000000000, 38.34805510287551300 ) ) ;
#52446=CARTESIAN_POINT ( 'NONE',  ( -10.18810118749999916, 4.220049686691934809, 88.56250000204838102 ) ) ;
#52449=CARTESIAN_POINT ( 'NONE',  ( -6.735557395310442023E-16, 11.00000000000000000, 99.62499999999998579 ) ) ;
#52479=CARTESIAN_POINT ( 'NONE',  ( 7.778174593052023411, -7.778174593052021635, 88.75000000409677625 ) ) ;
#52503=CARTESIAN_POINT ( 'NONE',  ( -10.18810118749999738, -4.220049686691941915, 92.12500000204836681 ) ) ;
#52511=CARTESIAN_POINT ( 'NONE',  ( -4.220049686691937474, -10.18810118749999738, 108.4375000020483668 ) ) ;
#52520=CARTESIAN_POINT ( 'NONE',  ( 10.18810118749999916, 4.220049686691935698, 101.8750000020483810 ) ) ;
#52533=ORIENTED_EDGE ( 'NONE', *, *, #2596, .F. ) ;
#52534=CARTESIAN_POINT ( 'NONE',  ( 10.18810118750000093, -4.220049686691933033, 105.8125000020483952 ) ) ;
#52552=CARTESIAN_POINT ( 'NONE',  ( -10.18810118749999916, 4.220049686691934809, 70.93750000204838102 ) ) ;
#52562=CARTESIAN_POINT ( 'NONE',  ( -4.556349186104047710, -10.99999999999999822, 104.9687500040967763 ) ) ;
#52581=PLANE ( 'NONE',  #25439 ) ;
#52586=CARTESIAN_POINT ( 'NONE',  ( 7.204075437095968759, -7.204075437095966983, 84.71875000204836681 ) ) ;
#52590=CARTESIAN_POINT ( 'NONE',  ( 10.18810118750000093, -4.220049686691933921, 107.6875000020483810 ) ) ;
#52598=CARTESIAN_POINT ( 'NONE',  ( -7.204075437095965206, -7.204075437095968759, 78.71875000204836681 ) ) ;
#52612=CARTESIAN_POINT ( 'NONE',  ( 10.18810118749999916, 1.247682550866122264E-15, 69.90625000204836681 ) ) ;
#52623=CARTESIAN_POINT ( 'NONE',  ( -11.00000000000000000, 4.556349186104045934, 94.09375000409679046 ) ) ;
#52665=CARTESIAN_POINT ( 'NONE',  ( 10.99999999999989342, 4.556349186104152515, 101.0312500040967763 ) ) ;
#52674=CARTESIAN_POINT ( 'NONE',  ( -10.11200329296622868, 3.728704622900627985, 117.7636805921466703 ) ) ;
#52675=EDGE_CURVE ( 'NONE', #67207, #545, #57675, .T. ) ;
#52677=CARTESIAN_POINT ( 'NONE',  ( -10.18810118749999916, 4.220049686691934809, 99.06250000204836681 ) ) ;
#52687=EDGE_CURVE ( 'NONE', #68592, #46063, #19098, .T. ) ;
#52690=CARTESIAN_POINT ( 'NONE',  ( -11.00000000000010658, 4.556349186103942017, 100.0937500040967763 ) ) ;
#52694=CARTESIAN_POINT ( 'NONE',  ( 7.204075437095966983, 7.204075437095967871, 95.96875000204838102 ) ) ;
#52696=ORIENTED_EDGE ( 'NONE', *, *, #57962, .T. ) ;
#52700=CARTESIAN_POINT ( 'NONE',  ( 10.18810118749999916, 1.247682550866122264E-15, 80.78125000204838102 ) ) ;
#52708=CARTESIAN_POINT ( 'NONE',  ( -10.18810118749999916, 4.220049686691934809, 91.56250000204836681 ) ) ;
#52719=CARTESIAN_POINT ( 'NONE',  ( -10.18810118749999916, 4.220049686691934809, 75.43750000204836681 ) ) ;
#52728=CARTESIAN_POINT ( 'NONE',  ( 11.00000000000000000, 1.347111479062088405E-15, 88.93750000409677625 ) ) ;
#52735=CARTESIAN_POINT ( 'NONE',  ( 2.729887517050593182, 10.18810118749999916, 67.22060451829244698 ) ) ;
#52738=CARTESIAN_POINT ( 'NONE',  ( 11.00000000000000000, 1.347111479062088405E-15, 82.74999999999998579 ) ) ;
#52759=ORIENTED_EDGE ( 'NONE', *, *, #6951, .F. ) ;
#52762=CARTESIAN_POINT ( 'NONE',  ( 11.00000000000000000, 1.347111479062088405E-15, 69.43750000409676204 ) ) ;
#52774=CARTESIAN_POINT ( 'NONE',  ( -7.204075437095965206, -7.204075437095968759, 110.2187500020483810 ) ) ;
#52790=EDGE_CURVE ( 'NONE', #40180, #40560, #65362, .T. ) ;
#52793=DIRECTION ( 'NONE',  ( 1.000000000000000000, 0.000000000000000000, 0.000000000000000000 ) ) ;
#52794=ORIENTED_EDGE ( 'NONE', *, *, #18005, .F. ) ;
#52803=FACE_OUTER_BOUND ( 'NONE', #17655, .T. ) ;
#52813=ORIENTED_EDGE ( 'NONE', *, *, #73567, .T. ) ;
#52815=CARTESIAN_POINT ( 'NONE',  ( 7.204075437095966983, 7.204075437095967871, 88.09375000204836681 ) ) ;
#52817=CARTESIAN_POINT ( 'NONE',  ( 11.00000000000000000, 4.556349186104045934, 100.8437499999999858 ) ) ;
#52824=CARTESIAN_POINT ( 'NONE',  ( 11.00000000000000000, 1.347111479062088405E-15, 97.74999999999998579 ) ) ;
#52843=FACE_OUTER_BOUND ( 'NONE', #15121, .T. ) ;
#52849=CARTESIAN_POINT ( 'NONE',  ( -7.778174593052020747, -7.778174593052023411, 83.87500000409677625 ) ) ;
#52852=DIRECTION ( 'NONE',  ( 1.000000000000000000, 1.084202172485504434E-16, 0.000000000000000000 ) ) ;
#52862=ORIENTED_EDGE ( 'NONE', *, *, #42516, .F. ) ;
#52866=CARTESIAN_POINT ( 'NONE',  ( -10.99999999999994671, -4.556349186104105442, 100.0937500000000000 ) ) ;
#52874=CARTESIAN_POINT ( 'NONE',  ( -4.220049686691935698, 10.18810118749999916, 90.25000000204838102 ) ) ;
#52882=CARTESIAN_POINT ( 'NONE',  ( -10.18810118749999738, -4.220049686691941915, 105.2500000020483952 ) ) ;
#52891=CARTESIAN_POINT ( 'NONE',  ( -4.220049686691937474, -10.18810118749999738, 101.3125000020483810 ) ) ;
#52904=( BOUNDED_CURVE ( )  B_SPLINE_CURVE ( 2, ( #3471, #65711, #1980, #49104, #72116, #24972, #43445, #31013, #20429 ),
 .UNSPECIFIED., .F., .F. ) 
 B_SPLINE_CURVE_WITH_KNOTS ( ( 3, 2, 2, 2, 3 ),
 ( 0.3088235294117646634, 0.3124999999999999445, 0.3161764705882352255, 0.3198529411764705066, 0.3235294117647058432 ),
 .UNSPECIFIED. ) 
 CURVE ( )  GEOMETRIC_REPRESENTATION_ITEM ( )  RATIONAL_B_SPLINE_CURVE ( ( 1.000000000000001110, 0.9238795325112856283, 1.000000000000000000, 0.9238795325112867385, 1.000000000000000000, 0.9238795325112867385, 1.000000000000000000, 0.9238795325112878487, 0.9999999999999988898 ) ) 
 REPRESENTATION_ITEM ( '' )  );
#52906=CARTESIAN_POINT ( 'NONE',  ( 7.204075437095966983, 7.204075437095967871, 106.0937500020483810 ) ) ;
#52907=CARTESIAN_POINT ( 'NONE',  ( 7.778174593052023411, -7.778174593052021635, 103.5624999999999858 ) ) ;
#52917=CARTESIAN_POINT ( 'NONE',  ( 4.556349186104045934, 11.00000000000000000, 74.03125000000000000 ) ) ;
#52925=CARTESIAN_POINT ( 'NONE',  ( -6.238412754330611322E-16, 10.18810118749999916, 69.15625000204836681 ) ) ;
#52932=CARTESIAN_POINT ( 'NONE',  ( -4.556349186104048599, -10.99999999999999822, 97.46875000409677625 ) ) ;
#52939=CARTESIAN_POINT ( 'NONE',  ( 2.020667218593132706E-15, -11.00000000000000000, 102.0625000040967763 ) ) ;
#52957=CARTESIAN_POINT ( 'NONE',  ( -7.204075437095965206, -7.204075437095968759, 81.34375000204838102 ) ) ;
#52958=CARTESIAN_POINT ( 'NONE',  ( 11.00000000000000000, 1.347111479062088405E-15, 118.0000000000000000 ) ) ;
#52961=CARTESIAN_POINT ( 'NONE',  ( -10.18810118749999738, -4.220049686691941915, 110.1250000020483810 ) ) ;
#52968=CARTESIAN_POINT ( 'NONE',  ( 10.18810118749999916, 1.247682550866122264E-15, 79.28125000204836681 ) ) ;
#52980=CARTESIAN_POINT ( 'NONE',  ( 10.18810118750000093, -4.220049686691933921, 74.31250000204836681 ) ) ;
#53028=CARTESIAN_POINT ( 'NONE',  ( -11.00000000000000000, 0.000000000000000000, 91.18750000409677625 ) ) ;
#53042=CARTESIAN_POINT ( 'NONE',  ( -7.778174593052020747, -7.778174593052023411, 115.1875000000000000 ) ) ;
#53046=CARTESIAN_POINT ( 'NONE',  ( -4.527972964883675289, 9.877574257516585021, 117.6444479903747151 ) ) ;
#53048=CARTESIAN_POINT ( 'NONE',  ( 10.18810118749999916, 1.247682550866122264E-15, 98.40625000204838102 ) ) ;
#53059=CARTESIAN_POINT ( 'NONE',  ( -6.735557395310442023E-16, 11.00000000000000000, 83.31250000409676204 ) ) ;
#53063=CARTESIAN_POINT ( 'NONE',  ( 10.18810118750000093, -4.220049686691933033, 94.18750000204836681 ) ) ;
#53069=CARTESIAN_POINT ( 'NONE',  ( 4.220049686691941027, -10.18810118749999738, 74.50000000204838102 ) ) ;
#53071=CARTESIAN_POINT ( 'NONE',  ( 0.000000000000000000, 0.000000000000000000, 41.99999999999999289 ) ) ;
#53074=CARTESIAN_POINT ( 'NONE',  ( -6.735557395310442023E-16, 11.00000000000000000, 89.31250000409676204 ) ) ;
#53077=CARTESIAN_POINT ( 'NONE',  ( -10.18810118749999916, 4.220049686691934809, 87.06250000204838102 ) ) ;
#53087=CARTESIAN_POINT ( 'NONE',  ( -7.204075437095965206, -7.204075437095968759, 77.21875000204836681 ) ) ;
#53106=ORIENTED_EDGE ( 'NONE', *, *, #46389, .T. ) ;
#53107=CARTESIAN_POINT ( 'NONE',  ( 5.094045771088254959, 8.823157229062946527, 67.15552375567561683 ) ) ;
#53110=CARTESIAN_POINT ( 'NONE',  ( 11.00000000000000000, 4.556349186104045934, 78.34374999999998579 ) ) ;
#53131=FACE_OUTER_BOUND ( 'NONE', #16827, .T. ) ;
#53137=CARTESIAN_POINT ( 'NONE',  ( 11.00000000000000000, 4.556349186104045934, 71.03125000409677625 ) ) ;
#53149=CARTESIAN_POINT ( 'NONE',  ( 7.204075437095966983, 7.204075437095967871, 112.4687500020483810 ) ) ;
#53153=CARTESIAN_POINT ( 'NONE',  ( -6.238412754330611322E-16, 10.18810118749999916, 67.28125000204838102 ) ) ;
#53174=AXIS2_PLACEMENT_3D ( 'NONE', #4168, #4533, #21864 ) ;
#53175=EDGE_CURVE ( 'NONE', #39873, #9385, #15303, .T. ) ;
#53187=CARTESIAN_POINT ( 'NONE',  ( 7.204075437095968759, -7.204075437095966983, 89.21875000204838102 ) ) ;
#53190=CARTESIAN_POINT ( 'NONE',  ( 7.778174593052021635, 7.778174593052023411, 100.9374999999999858 ) ) ;
#53195=CARTESIAN_POINT ( 'NONE',  ( 10.99999999999986855, 4.556349186104178273, 105.5312500040967763 ) ) ;
#53222=CARTESIAN_POINT ( 'NONE',  ( -4.556349186104047710, -10.99999999999999822, 88.46875000409677625 ) ) ;
#53247=CARTESIAN_POINT ( 'NONE',  ( 10.18810118749999916, 4.220049686691935698, 89.87500000204836681 ) ) ;
#53252=CARTESIAN_POINT ( 'NONE',  ( -4.220049686691937474, -10.18810118749999738, 100.9375000020483810 ) ) ;
#53259=CARTESIAN_POINT ( 'NONE',  ( -7.778174593052023411, 7.778174593052023411, 96.81250000000000000 ) ) ;
#53261=CARTESIAN_POINT ( 'NONE',  ( 4.220049686691934809, 10.18810118749999916, 100.5625000020483668 ) ) ;
#53274=AXIS2_PLACEMENT_3D ( 'NONE', #3178, #43910, #20136 ) ;
#53280=CARTESIAN_POINT ( 'NONE',  ( 7.204075437095968759, -7.204075437095966983, 104.2187500020483810 ) ) ;
#53291=CARTESIAN_POINT ( 'NONE',  ( 11.00000000000000000, 1.347111479062088405E-15, 73.74999999999998579 ) ) ;
#53298=CARTESIAN_POINT ( 'NONE',  ( 10.99999999999995026, -4.556349186104096560, 91.84375000409677625 ) ) ;
#53299=CARTESIAN_POINT ( 'NONE',  ( -7.204075437095965206, -7.204075437095968759, 68.21875000204836681 ) ) ;
#53307=DIRECTION ( 'NONE',  ( 7.885106708985487801E-17, -1.000000000000000000, 0.000000000000000000 ) ) ;
#53311=CARTESIAN_POINT ( 'NONE',  ( -7.778174593052023411, 7.778174593052023411, 107.5000000040967763 ) ) ;
#53323=VERTEX_POINT ( 'NONE', #40014 ) ;
#53332=CARTESIAN_POINT ( 'NONE',  ( -10.18810118749999738, -4.220049686691941915, 107.1250000020483810 ) ) ;
#53338=CARTESIAN_POINT ( 'NONE',  ( 0.000000000000000000, 0.000000000000000000, 118.0000000000000000 ) ) ;
#53339=CARTESIAN_POINT ( 'NONE',  ( -6.238412754330611322E-16, 10.18810118749999916, 69.15625000204836681 ) ) ;
#53353=CARTESIAN_POINT ( 'NONE',  ( -10.18810118749999738, -4.220049686691941915, 70.75000000204836681 ) ) ;
#53380=EDGE_LOOP ( 'NONE', ( #30323, #48067, #2428, #72581 ) ) ;
#53396=CARTESIAN_POINT ( 'NONE',  ( 11.00000000000000000, 1.347111479062088405E-15, 118.0000000000000000 ) ) ;
#53398=ORIENTED_EDGE ( 'NONE', *, *, #1759, .T. ) ;
#53411=CARTESIAN_POINT ( 'NONE',  ( 2.020667218593132706E-15, -11.00000000000000000, 105.0625000040967763 ) ) ;
#53412=ORIENTED_EDGE ( 'NONE', *, *, #50365, .T. ) ;
#53419=CARTESIAN_POINT ( 'NONE',  ( 10.18810118750000093, -4.220049686691933921, 98.31250000204836681 ) ) ;
#53420=CARTESIAN_POINT ( 'NONE',  ( -4.556349186104045934, 11.00000000000000000, 86.40625000409677625 ) ) ;
#53427=ORIENTED_EDGE ( 'NONE', *, *, #62904, .T. ) ;
#53430=CARTESIAN_POINT ( 'NONE',  ( -4.556349186104048599, -10.99999999999999822, 73.28124999999997158 ) ) ;
#53437=CARTESIAN_POINT ( 'NONE',  ( 10.18810118749999916, 1.247682550866122264E-15, 86.78125000204836681 ) ) ;
#53442=CARTESIAN_POINT ( 'NONE',  ( -11.00000000000000000, 0.000000000000000000, 103.0000000000000000 ) ) ;
#53443=CARTESIAN_POINT ( 'NONE',  ( 4.220049686691934809, 10.18810118749999916, 73.56250000204835260 ) ) ;
#53450=CARTESIAN_POINT ( 'NONE',  ( -7.204075437095965206, -7.204075437095968759, 90.34375000204838102 ) ) ;
#53461=CARTESIAN_POINT ( 'NONE',  ( -4.220049686691937474, -10.18810118749999738, 72.81250000204836681 ) ) ;
#53464=CARTESIAN_POINT ( 'NONE',  ( 2.020667218593132706E-15, -11.00000000000000000, 112.3749999999999858 ) ) ;
#53480=CARTESIAN_POINT ( 'NONE',  ( 7.778174593052021635, 7.778174593052023411, 75.43749999999998579 ) ) ;
#53483=CARTESIAN_POINT ( 'NONE',  ( -11.00000000000000000, 0.000000000000000000, 113.4999999999999858 ) ) ;
#53484=VERTEX_POINT ( 'NONE', #62184 ) ;
#53505=CARTESIAN_POINT ( 'NONE',  ( 10.18810118749999916, 4.220049686691935698, 85.37500000204839523 ) ) ;
#53506=CARTESIAN_POINT ( 'NONE',  ( 4.556349186104045934, 11.00000000000000000, 69.71875000409677625 ) ) ;
#53519=CARTESIAN_POINT ( 'NONE',  ( -6.238412754330611322E-16, 10.18810118749999916, 111.1562500020483668 ) ) ;
#53557=CARTESIAN_POINT ( 'NONE',  ( 10.18810118749999916, 1.247682550866122264E-15, 87.90625000204838102 ) ) ;
#53559=CARTESIAN_POINT ( 'NONE',  ( -4.556349186104047710, -10.99999999999999822, 97.28124999999997158 ) ) ;
#53572=CARTESIAN_POINT ( 'NONE',  ( -11.00000000000000533, -11.00000000000000355, 20.00000000000000000 ) ) ;
#53593=CARTESIAN_POINT ( 'NONE',  ( 11.00000000000000000, 4.556349186104045934, 86.03125000409676204 ) ) ;
#53615=CARTESIAN_POINT ( 'NONE',  ( 1.871523826299183495E-15, -10.18810118749999916, 89.40625000204838102 ) ) ;
#53618=ADVANCED_FACE ( 'NONE', ( #72770 ), #44100, .T. ) ;
#53622=CARTESIAN_POINT ( 'NONE',  ( 7.204075437095966983, 7.204075437095967871, 100.0937500020483668 ) ) ;
#53625=ORIENTED_EDGE ( 'NONE', *, *, #68944, .F. ) ;
#53632=CARTESIAN_POINT ( 'NONE',  ( 10.18810118749999916, 1.247682550866122264E-15, 98.78125000204838102 ) ) ;
#53645=CARTESIAN_POINT ( 'NONE',  ( -7.778174593052023411, 7.778174593052023411, 68.31249999999998579 ) ) ;
#53649=CARTESIAN_POINT ( 'NONE',  ( -4.220049686691937474, -10.18810118749999738, 102.4375000020483810 ) ) ;
#53658=CARTESIAN_POINT ( 'NONE',  ( 4.556349186104052151, -10.99999999999999822, 109.4687499999999858 ) ) ;
#53664=CARTESIAN_POINT ( 'NONE',  ( -4.556349186104047710, -10.99999999999999822, 113.7812500000000142 ) ) ;
#53671=ORIENTED_EDGE ( 'NONE', *, *, #395, .F. ) ;
#53672=( BOUNDED_CURVE ( )  B_SPLINE_CURVE ( 2, ( #57457, #23474, #12882, #35918, #24207, #63838, #46856, #47218, #58937 ),
 .UNSPECIFIED., .F., .F. ) 
 B_SPLINE_CURVE_WITH_KNOTS ( ( 3, 2, 2, 2, 3 ),
 ( 0.7205882352941176405, 0.7242647058823529216, 0.7279411764705880916, 0.7316176470588233727, 0.7352941176470587648 ),
 .UNSPECIFIED. ) 
 CURVE ( )  GEOMETRIC_REPRESENTATION_ITEM ( )  RATIONAL_B_SPLINE_CURVE ( ( 1.000000000000000000, 0.9238795325112867385, 1.000000000000000000, 0.9238795325112867385, 1.000000000000000000, 0.9238795325112867385, 1.000000000000000000, 0.9238795325112890700, 0.9999999999999976685 ) ) 
 REPRESENTATION_ITEM ( '' )  );
#53676=CARTESIAN_POINT ( 'NONE',  ( 11.00000000000000000, 4.556349186104045934, 105.5312500040967905 ) ) ;
#53680=CARTESIAN_POINT ( 'NONE',  ( -6.735557395310442023E-16, 11.00000000000000000, 95.31250000409677625 ) ) ;
#53700=CARTESIAN_POINT ( 'NONE',  ( -10.18810118749999916, 4.220049686691934809, 111.4375000020483810 ) ) ;
#53708=CARTESIAN_POINT ( 'NONE',  ( 10.18810118750000093, -4.220049686691933033, 68.68750000204838102 ) ) ;
#53719=CARTESIAN_POINT ( 'NONE',  ( 7.204075437095968759, -7.204075437095966983, 116.5937500020483810 ) ) ;
#53723=CYLINDRICAL_SURFACE ( 'NONE', #22164, 11.00000000000000000 ) ;
#53735=ORIENTED_EDGE ( 'NONE', *, *, #36094, .T. ) ;
#53761=DIRECTION ( 'NONE',  ( -0.000000000000000000, -0.000000000000000000, -1.000000000000000000 ) ) ;
#53775=CARTESIAN_POINT ( 'NONE',  ( -7.778174593052020747, -7.778174593052023411, 85.18749999999998579 ) ) ;
#53786=CARTESIAN_POINT ( 'NONE',  ( 4.220049686691941027, -10.18810118749999738, 93.62500000204838102 ) ) ;
#53802=CARTESIAN_POINT ( 'NONE',  ( 7.204075437095968759, -7.204075437095966983, 89.59375000204838102 ) ) ;
#53808=CARTESIAN_POINT ( 'NONE',  ( -10.18810118749999916, 4.220049686691934809, 72.43750000204838102 ) ) ;
#53815=CARTESIAN_POINT ( 'NONE',  ( 7.204075437095966983, 7.204075437095967871, 80.59375000204838102 ) ) ;
#53827=CARTESIAN_POINT ( 'NONE',  ( -4.220049686691935698, 10.18810118749999916, 70.75000000204836681 ) ) ;
#53833=PRODUCT_DEFINITION_FORMATION_WITH_SPECIFIED_SOURCE ( 'ANY', '', #49912, .NOT_KNOWN. ) ;
#53846=CARTESIAN_POINT ( 'NONE',  ( 11.00000000000000000, 4.556349186104045934, 76.84374999999998579 ) ) ;
#53859=FACE_OUTER_BOUND ( 'NONE', #37257, .T. ) ;
#53874=CARTESIAN_POINT ( 'NONE',  ( -4.220049686691937474, -10.18810118749999738, 87.81250000204838102 ) ) ;
#53875=CARTESIAN_POINT ( 'NONE',  ( 4.220049686691941027, -10.18810118749999738, 114.6250000020483810 ) ) ;
#53886=CARTESIAN_POINT ( 'NONE',  ( -4.220049686691937474, -10.18810118749999738, 107.3125000020483810 ) ) ;
#53924=CARTESIAN_POINT ( 'NONE',  ( -10.18810118749999738, -4.220049686691941915, 78.25000000204838102 ) ) ;
#53926=CARTESIAN_POINT ( 'NONE',  ( 7.778174593052021635, 7.778174593052023411, 93.43749999999998579 ) ) ;
#53950=SPHERICAL_SURFACE ( 'NONE', #13852, 38.34805510287551300 ) ;
#53956=CARTESIAN_POINT ( 'NONE',  ( 11.00000000000000000, 1.347111479062088405E-15, 84.43750000409677625 ) ) ;
#53981=CARTESIAN_POINT ( 'NONE',  ( 4.220049686691941027, -10.18810118749999738, 94.00000000204838102 ) ) ;
#53986=CARTESIAN_POINT ( 'NONE',  ( -7.204075437095967871, 7.204075437095967871, 101.9687500020483668 ) ) ;
#53988=ORIENTED_EDGE ( 'NONE', *, *, #5862, .F. ) ;
#53994=CARTESIAN_POINT ( 'NONE',  ( -4.220049686691935698, 10.18810118749999916, 97.75000000204838102 ) ) ;
#53997=CARTESIAN_POINT ( 'NONE',  ( -3.469446951953614189E-15, 16.00000000000000000, 38.34805510287551300 ) ) ;
#54011=( BOUNDED_CURVE ( )  B_SPLINE_CURVE ( 2, ( #2465, #25456, #48470, #71475, #19800, #63989, #61671, #66952, #9239 ),
 .UNSPECIFIED., .F., .F. ) 
 B_SPLINE_CURVE_WITH_KNOTS ( ( 3, 2, 2, 2, 3 ),
 ( 0.6764705882352939348, 0.6801470588235292158, 0.6838235294117644969, 0.6874999999999998890, 0.6911764705882351700 ),
 .UNSPECIFIED. ) 
 CURVE ( )  GEOMETRIC_REPRESENTATION_ITEM ( )  RATIONAL_B_SPLINE_CURVE ( ( 1.000000000000004663, 0.9238795325112821866, 1.000000000000000000, 0.9238795325112867385, 1.000000000000000000, 0.9238795325112867385, 1.000000000000000000, 0.9238795325112890700, 0.9999999999999976685 ) ) 
 REPRESENTATION_ITEM ( '' )  );
#54014=CARTESIAN_POINT ( 'NONE',  ( 4.220049686691934809, 10.18810118749999916, 101.6875000020483810 ) ) ;
#54033=CARTESIAN_POINT ( 'NONE',  ( -4.556349186104048599, -10.99999999999999822, 91.46875000409676204 ) ) ;
#54034=CARTESIAN_POINT ( 'NONE',  ( -4.556349186104047710, -10.99999999999999822, 110.7812500000000000 ) ) ;
#54046=CARTESIAN_POINT ( 'NONE',  ( -11.00000000000000000, 4.556349186104045934, 107.5937500040967763 ) ) ;
#54050=CARTESIAN_POINT ( 'NONE',  ( -10.99999999999989342, 4.556349186104152515, 71.40624999999995737 ) ) ;
#54062=ORIENTED_EDGE ( 'NONE', *, *, #46389, .F. ) ;
#54065=CARTESIAN_POINT ( 'NONE',  ( 11.00000000000000000, 1.347111479062088405E-15, 94.93750000409677625 ) ) ;
#54068=CARTESIAN_POINT ( 'NONE',  ( 7.778174593052023411, -7.778174593052021635, 70.75000000409677625 ) ) ;
#54069=CARTESIAN_POINT ( 'NONE',  ( -4.220049686691937474, -10.18810118749999738, 108.8125000020484094 ) ) ;
#54077=CARTESIAN_POINT ( 'NONE',  ( -10.18810118749999916, 4.220049686691934809, 72.43750000204838102 ) ) ;
#54089=CARTESIAN_POINT ( 'NONE',  ( 1.871523826299183495E-15, -10.18810118749999916, 68.03125000204838102 ) ) ;
#54117=ORIENTED_EDGE ( 'NONE', *, *, #5325, .T. ) ;
#54132=DIRECTION ( 'NONE',  ( -0.000000000000000000, -0.000000000000000000, -1.000000000000000000 ) ) ;
#54137=DIRECTION ( 'NONE',  ( -0.000000000000000000, -0.000000000000000000, -1.000000000000000000 ) ) ;
#54161=CARTESIAN_POINT ( 'NONE',  ( 10.18810118750000093, -4.220049686691933921, 92.31250000204838102 ) ) ;
#54162=CARTESIAN_POINT ( 'NONE',  ( 10.99999999999989342, 4.556349186104152515, 86.03125000409676204 ) ) ;
#54172=EDGE_CURVE ( 'NONE', #67283, #49304, #17565, .T. ) ;
#54177=CARTESIAN_POINT ( 'NONE',  ( -10.18810118749999916, 4.220049686691934809, 88.93750000204839523 ) ) ;
#54183=CARTESIAN_POINT ( 'NONE',  ( 11.00000000000000000, 1.347111479062088405E-15, 102.4375000040967763 ) ) ;
#54184=CARTESIAN_POINT ( 'NONE',  ( -6.238412754330611322E-16, 10.18810118749999916, 76.65625000204836681 ) ) ;
#54190=CARTESIAN_POINT ( 'NONE',  ( 10.18810118749999916, 1.247682550866122264E-15, 84.90625000204838102 ) ) ;
#54199=CARTESIAN_POINT ( 'NONE',  ( 10.18810118750000093, -4.220049686691933921, 70.18750000204838102 ) ) ;
#54200=ORIENTED_EDGE ( 'NONE', *, *, #41293, .F. ) ;
#54222=CARTESIAN_POINT ( 'NONE',  ( 11.00000000000000000, 1.347111479062088405E-15, 75.24999999999998579 ) ) ;
#54243=( BOUNDED_CURVE ( )  B_SPLINE_CURVE ( 2, ( #2848, #32656, #25837, #38682, #3982, #60931, #61684, #19815, #71866 ),
 .UNSPECIFIED., .F., .F. ) 
 B_SPLINE_CURVE_WITH_KNOTS ( ( 3, 2, 2, 2, 3 ),
 ( 0.7941176470588234837, 0.7977941176470588758, 0.8014705882352941568, 0.8051470588235294379, 0.8088235294117647189 ),
 .UNSPECIFIED. ) 
 CURVE ( )  GEOMETRIC_REPRESENTATION_ITEM ( )  RATIONAL_B_SPLINE_CURVE ( ( 1.000000000000000000, 0.9238795325112867385, 1.000000000000000000, 0.9238795325112867385, 1.000000000000000000, 0.9238795325112867385, 1.000000000000000000, 0.9238795325112867385, 1.000000000000000000 ) ) 
 REPRESENTATION_ITEM ( '' )  );
#54249=CARTESIAN_POINT ( 'NONE',  ( 1.871523826299183495E-15, -10.18810118749999916, 89.40625000204838102 ) ) ;
#54250=CARTESIAN_POINT ( 'NONE',  ( -10.18810118749999916, 0.000000000000000000, 111.1562500020483668 ) ) ;
#54264=CARTESIAN_POINT ( 'NONE',  ( 4.220049686691941027, -10.18810118749999738, 104.5000000020483668 ) ) ;
#54280=ORIENTED_EDGE ( 'NONE', *, *, #23608, .T. ) ;
#54281=VECTOR ( 'NONE', #43644, 1000.000000000000000 ) ;
#54297=ORIENTED_EDGE ( 'NONE', *, *, #19940, .T. ) ;
#54303=CARTESIAN_POINT ( 'NONE',  ( 10.18810118749999916, 1.247682550866122264E-15, 80.40625000204838102 ) ) ;
#54306=CARTESIAN_POINT ( 'NONE',  ( 2.020667218593132706E-15, -11.00000000000000000, 95.87499999999998579 ) ) ;
#54334=CARTESIAN_POINT ( 'NONE',  ( 7.778174593052021635, 7.778174593052023411, 83.12500000409676204 ) ) ;
#54337=CARTESIAN_POINT ( 'NONE',  ( -11.00000000000000000, 0.000000000000000000, 118.0000000000000000 ) ) ;
#54344=ORIENTED_EDGE ( 'NONE', *, *, #13597, .F. ) ;
#54349=CARTESIAN_POINT ( 'NONE',  ( -7.204075437095965206, -7.204075437095968759, 79.84375000204838102 ) ) ;
#54358=CARTESIAN_POINT ( 'NONE',  ( 4.220049686691934809, 10.18810118749999916, 84.06250000204838102 ) ) ;
#54366=CARTESIAN_POINT ( 'NONE',  ( -7.204075437095967871, 7.204075437095967871, 103.4687500020483668 ) ) ;
#54375=CARTESIAN_POINT ( 'NONE',  ( -7.204075437095965206, -7.204075437095968759, 96.71875000204838102 ) ) ;
#54378=EDGE_CURVE ( 'NONE', #545, #69783, #14892, .T. ) ;
#54393=CARTESIAN_POINT ( 'NONE',  ( 1.871523826299183495E-15, -10.18810118749999916, 96.53125000204838102 ) ) ;
#54394=CARTESIAN_POINT ( 'NONE',  ( -7.778174593052023411, 7.778174593052023411, 115.0000000040967905 ) ) ;
#54404=CARTESIAN_POINT ( 'NONE',  ( 7.778174593052023411, -7.778174593052021635, 109.5625000000000000 ) ) ;
#54411=CARTESIAN_POINT ( 'NONE',  ( 11.00000000000000000, 4.556349186104045934, 112.8437500000000000 ) ) ;
#54424=CARTESIAN_POINT ( 'NONE',  ( -10.99999999999999822, -4.556349186104052151, 97.28125000409677625 ) ) ;
#54427=CARTESIAN_POINT ( 'NONE',  ( 6.742326029964707423, 8.814023156139338511, 117.4676415472669788 ) ) ;
#54447=CARTESIAN_POINT ( 'NONE',  ( -6.238412754330611322E-16, 10.18810118749999916, 106.6562500020483810 ) ) ;
#54456=CARTESIAN_POINT ( 'NONE',  ( 10.18810118750000093, -4.220049686691933033, 70.18750000204838102 ) ) ;
#54469=CARTESIAN_POINT ( 'NONE',  ( -7.204075437095965206, -7.204075437095968759, 116.2187500020483810 ) ) ;
#54470=( BOUNDED_CURVE ( )  B_SPLINE_CURVE ( 2, ( #63509, #5809, #58609, #17484, #70293, #52203, #535, #24254, #23515 ),
 .UNSPECIFIED., .F., .F. ) 
 B_SPLINE_CURVE_WITH_KNOTS ( ( 3, 2, 2, 2, 3 ),
 ( 0.1617647058823530326, 0.1654411764705883137, 0.1691176470588236225, 0.1727941176470589035, 0.1764705882352942123 ),
 .UNSPECIFIED. ) 
 CURVE ( )  GEOMETRIC_REPRESENTATION_ITEM ( )  RATIONAL_B_SPLINE_CURVE ( ( 0.9999999999999982236, 0.9238795325112885148, 1.000000000000000000, 0.9238795325112867385, 1.000000000000000000, 0.9238795325112867385, 1.000000000000000000, 0.9238795325112849621, 1.000000000000001776 ) ) 
 REPRESENTATION_ITEM ( '' )  );
#54473=ORIENTED_EDGE ( 'NONE', *, *, #70336, .T. ) ;
#54476=EDGE_CURVE ( 'NONE', #46843, #56876, #43262, .T. ) ;
#54481=CARTESIAN_POINT ( 'NONE',  ( 11.00000000000000000, 1.347111479062088405E-15, 103.7500000000000000 ) ) ;
#54483=ORIENTED_EDGE ( 'NONE', *, *, #73564, .T. ) ;
#54486=CARTESIAN_POINT ( 'NONE',  ( 7.204075437095968759, -7.204075437095966983, 114.7187500020483810 ) ) ;
#54498=CARTESIAN_POINT ( 'NONE',  ( 11.00000000000000000, 1.347111479062088405E-15, 87.43750000409677625 ) ) ;
#54500=DIRECTION ( 'NONE',  ( -0.000000000000000000, -0.000000000000000000, -1.000000000000000000 ) ) ;
#54502=DIRECTION ( 'NONE',  ( -1.000000000000000000, 0.000000000000000000, 0.000000000000000000 ) ) ;
#54504=CARTESIAN_POINT ( 'NONE',  ( 2.020667218593132706E-15, -11.00000000000000000, 89.87499999999998579 ) ) ;
#54523=DIRECTION ( 'NONE',  ( -0.000000000000000000, -0.000000000000000000, -1.000000000000000000 ) ) ;
#54532=CARTESIAN_POINT ( 'NONE',  ( -10.18810118749999738, -4.220049686691941915, 96.25000000204838102 ) ) ;
#54542=DIRECTION ( 'NONE',  ( -0.000000000000000000, -0.000000000000000000, -1.000000000000000000 ) ) ;
#54547=CARTESIAN_POINT ( 'NONE',  ( -7.204075437095967871, 7.204075437095967871, 90.34375000204838102 ) ) ;
#54553=CARTESIAN_POINT ( 'NONE',  ( 10.18810118749999916, 1.247682550866122264E-15, 71.78125000204838102 ) ) ;
#54561=CARTESIAN_POINT ( 'NONE',  ( 4.220049686691941027, -10.18810118749999738, 83.12500000204835260 ) ) ;
#54568=( BOUNDED_CURVE ( )  B_SPLINE_CURVE ( 2, ( #1861, #25957, #60300, #20684, #48236, #71244, #14268, #30894, #20302 ),
 .UNSPECIFIED., .F., .F. ) 
 B_SPLINE_CURVE_WITH_KNOTS ( ( 3, 2, 2, 2, 3 ),
 ( 0.8823529411764706731, 0.8860294117647059542, 0.8897058823529412352, 0.8933823529411766273, 0.8970588235294119084 ),
 .UNSPECIFIED. ) 
 CURVE ( )  GEOMETRIC_REPRESENTATION_ITEM ( )  RATIONAL_B_SPLINE_CURVE ( ( 0.9999999999999976685, 0.9238795325112890700, 1.000000000000000000, 0.9238795325112867385, 1.000000000000000000, 0.9238795325112867385, 1.000000000000000000, 0.9238795325112844070, 1.000000000000002220 ) ) 
 REPRESENTATION_ITEM ( '' )  );
#54597=CARTESIAN_POINT ( 'NONE',  ( -4.556349186104045934, 11.00000000000000000, 78.71874999999998579 ) ) ;
#54601=ORIENTED_EDGE ( 'NONE', *, *, #1411, .T. ) ;
#54602=LINE ( 'NONE', #36501, #4642 ) ;
#54606=CARTESIAN_POINT ( 'NONE',  ( 4.556349186104051263, -10.99999999999999822, 114.1562500040967763 ) ) ;
#54622=CARTESIAN_POINT ( 'NONE',  ( 10.18810118749999916, 1.247682550866122264E-15, 86.78125000204836681 ) ) ;
#54623=CARTESIAN_POINT ( 'NONE',  ( 1.871523826299183495E-15, -10.18810118749999916, 116.0312500020483810 ) ) ;
#54632=FACE_OUTER_BOUND ( 'NONE', #17448, .T. ) ;
#54635=CARTESIAN_POINT ( 'NONE',  ( 7.204075437095968759, -7.204075437095966983, 104.5937500020483810 ) ) ;
#54639=CARTESIAN_POINT ( 'NONE',  ( -11.00000000000000533, 0.000000000000000000, 41.99999999999999289 ) ) ;
#54647=ORIENTED_EDGE ( 'NONE', *, *, #11313, .F. ) ;
#54655=ADVANCED_FACE ( 'NONE', ( #49575 ), #32237, .T. ) ;
#54673=EDGE_CURVE ( 'NONE', #13626, #43538, #72593, .T. ) ;
#54676=CARTESIAN_POINT ( 'NONE',  ( -10.18810118749999916, 4.220049686691934809, 81.06250000204836681 ) ) ;
#54679=CARTESIAN_POINT ( 'NONE',  ( 7.778174593052021635, 7.778174593052023411, 96.43749999999998579 ) ) ;
#54707=CARTESIAN_POINT ( 'NONE',  ( 7.778174593052023411, -7.778174593052021635, 78.25000000409676204 ) ) ;
#54727=CARTESIAN_POINT ( 'NONE',  ( -7.204075437095965206, -7.204075437095968759, 78.34375000204838102 ) ) ;
#54729=CYLINDRICAL_SURFACE ( 'NONE', #53174, 11.00000000000000000 ) ;
#54735=CARTESIAN_POINT ( 'NONE',  ( -4.220049686691937474, -10.18810118749999738, 84.81250000204838102 ) ) ;
#54736=VERTEX_POINT ( 'NONE', #49951 ) ;
#54738=CARTESIAN_POINT ( 'NONE',  ( -11.00000000000000000, 0.000000000000000000, 109.1875000040967763 ) ) ;
#54740=CARTESIAN_POINT ( 'NONE',  ( 1.871523826299183495E-15, -10.18810118749999916, 96.53125000204838102 ) ) ;
#54748=CARTESIAN_POINT ( 'NONE',  ( 4.220049686691941027, -10.18810118749999738, 95.50000000204838102 ) ) ;
#54759=CARTESIAN_POINT ( 'NONE',  ( -11.00000000000000000, 0.000000000000000000, 99.99999999999998579 ) ) ;
#54764=CARTESIAN_POINT ( 'NONE',  ( -6.238412754330611322E-16, 10.18810118749999916, 95.78125000204836681 ) ) ;
#54782=CARTESIAN_POINT ( 'NONE',  ( -6.735557395310442023E-16, 11.00000000000000000, 116.1249999999999858 ) ) ;
#54795=CARTESIAN_POINT ( 'NONE',  ( 4.556349186104045934, 11.00000000000000000, 99.71875000409676204 ) ) ;
#54796=CARTESIAN_POINT ( 'NONE',  ( -7.778174593052020747, -7.778174593052023411, 106.3750000040967763 ) ) ;
#54820=CARTESIAN_POINT ( 'NONE',  ( -10.99999999999999822, -4.556349186104053040, 70.28125000409676204 ) ) ;
#54822=CARTESIAN_POINT ( 'NONE',  ( 4.220049686691934809, 10.18810118749999916, 106.5625000020483668 ) ) ;
#54829=CARTESIAN_POINT ( 'NONE',  ( 7.204075437095968759, -7.204075437095966983, 71.59375000204836681 ) ) ;
#54838=CYLINDRICAL_SURFACE ( 'NONE', #44937, 11.00000000000000000 ) ;
#54841=CARTESIAN_POINT ( 'NONE',  ( -6.238412754330611322E-16, 10.18810118749999916, 117.1562500020483810 ) ) ;
#54851=VERTEX_POINT ( 'NONE', #52193 ) ;
#54854=CARTESIAN_POINT ( 'NONE',  ( -10.18810118749999916, 0.000000000000000000, 114.1562500020483810 ) ) ;
#54855=CARTESIAN_POINT ( 'NONE',  ( 7.778174593052023411, -7.778174593052021635, 84.25000000409677625 ) ) ;
#54861=CIRCLE ( 'NONE', #28369, 11.00000000000000000 ) ;
#54869=FACE_OUTER_BOUND ( 'NONE', #65808, .T. ) ;
#54871=CARTESIAN_POINT ( 'NONE',  ( 11.00000000000000000, 1.347111479062088405E-15, 118.0000000000000000 ) ) ;
#54876=CARTESIAN_POINT ( 'NONE',  ( -11.00000000000000000, 0.000000000000000000, 89.50000000000000000 ) ) ;
#54906=CARTESIAN_POINT ( 'NONE',  ( 4.220049686691934809, 10.18810118749999916, 92.68750000204838102 ) ) ;
#54920=CARTESIAN_POINT ( 'NONE',  ( -10.18810118749999738, -4.220049686691941915, 90.62500000204836681 ) ) ;
#54935=CARTESIAN_POINT ( 'NONE',  ( 1.871523826299183495E-15, -10.18810118749999916, 86.03125000204836681 ) ) ;
#54948=CARTESIAN_POINT ( 'NONE',  ( 2.020667218593132706E-15, -11.00000000000000000, 76.37499999999998579 ) ) ;
#54960=CARTESIAN_POINT ( 'NONE',  ( 4.556349186104052151, -10.99999999999999822, 92.96875000000000000 ) ) ;
#54964=CARTESIAN_POINT ( 'NONE',  ( 2.020667218593132706E-15, -11.00000000000000000, 115.5625000040967763 ) ) ;
#54965=CARTESIAN_POINT ( 'NONE',  ( 7.778174593052021635, 7.778174593052023411, 114.4375000000000000 ) ) ;
#54969=CARTESIAN_POINT ( 'NONE',  ( -6.735557395310442023E-16, 11.00000000000000000, 69.62499999999998579 ) ) ;
#54973=EDGE_LOOP ( 'NONE', ( #24566, #35928, #68185, #53625 ) ) ;
#54975=ADVANCED_FACE ( 'NONE', ( #46519 ), #69163, .T. ) ;
#54981=CARTESIAN_POINT ( 'NONE',  ( -10.99999999999999822, -4.556349186104052151, 113.7812500040967763 ) ) ;
#54997=ORIENTED_EDGE ( 'NONE', *, *, #12435, .F. ) ;
#54998=CARTESIAN_POINT ( 'NONE',  ( 10.18810118749999916, 1.247682550866122264E-15, 89.78125000204836681 ) ) ;
#54999=CARTESIAN_POINT ( 'NONE',  ( -10.18810118749999916, 0.000000000000000000, 112.6562500020483810 ) ) ;
#55012=CARTESIAN_POINT ( 'NONE',  ( 4.220049686691934809, 10.18810118749999916, 108.0625000020483810 ) ) ;
#55049=CARTESIAN_POINT ( 'NONE',  ( -7.204075437095965206, -7.204075437095968759, 82.84375000204838102 ) ) ;
#55052=CARTESIAN_POINT ( 'NONE',  ( 11.00000000000000355, -4.556349186104045046, 90.15625000000000000 ) ) ;
#55068=LINE ( 'NONE', #3377, #47196 ) ;
#55075=CARTESIAN_POINT ( 'NONE',  ( 10.99999999999989697, -4.556349186104149851, 72.15624999999998579 ) ) ;
#55081=CARTESIAN_POINT ( 'NONE',  ( -4.556349186104047710, -10.99999999999999822, 82.46875000409677625 ) ) ;
#55096=CARTESIAN_POINT ( 'NONE',  ( 11.00000000000000000, 1.347111479062088405E-15, 100.7499999999999858 ) ) ;
#55100=CARTESIAN_POINT ( 'NONE',  ( 7.204075437095968759, -7.204075437095966983, 80.21875000204836681 ) ) ;
#55108=CARTESIAN_POINT ( 'NONE',  ( -10.18810118749999916, 0.000000000000000000, 83.03125000204838102 ) ) ;
#55112=CARTESIAN_POINT ( 'NONE',  ( 11.00000000000000000, 1.347111479062088405E-15, 90.43750000409676204 ) ) ;
#55115=CARTESIAN_POINT ( 'NONE',  ( 1.871523826299183495E-15, -10.18810118749999916, 95.03125000204836681 ) ) ;
#55122=CARTESIAN_POINT ( 'NONE',  ( -10.18810118749999738, -4.220049686691941915, 93.62500000204838102 ) ) ;
#55140=CARTESIAN_POINT ( 'NONE',  ( 7.204075437095968759, -7.204075437095966983, 101.2187500020483668 ) ) ;
#55161=CARTESIAN_POINT ( 'NONE',  ( 7.778174593052023411, -7.778174593052021635, 111.0625000000000000 ) ) ;
#55167=CARTESIAN_POINT ( 'NONE',  ( 0.000000000000000000, 0.000000000000000000, 118.0000000000000000 ) ) ;
#55170=LINE ( 'NONE', #27218, #12166 ) ;
#55174=CARTESIAN_POINT ( 'NONE',  ( -11.00000000000000000, 4.556349186104045934, 97.09375000409679046 ) ) ;
#55177=CARTESIAN_POINT ( 'NONE',  ( 11.00000000000001066, 4.556349186104036164, 117.3437500000000142 ) ) ;
#55191=CYLINDRICAL_SURFACE ( 'NONE', #3767, 11.00000000000000000 ) ;
#55196=CARTESIAN_POINT ( 'NONE',  ( 4.556349186104045934, 11.00000000000000000, 69.53124999999998579 ) ) ;
#55198=CARTESIAN_POINT ( 'NONE',  ( 10.18810118749999916, 1.247682550866122264E-15, 103.2812500020483810 ) ) ;
#55204=CARTESIAN_POINT ( 'NONE',  ( -10.18810118749999916, 4.220049686691934809, 67.93750000204838102 ) ) ;
#55207=CARTESIAN_POINT ( 'NONE',  ( -10.18810118749999916, 0.000000000000000000, 112.6562500020483810 ) ) ;
#55217=CARTESIAN_POINT ( 'NONE',  ( 5.094050593753887135, 8.823154444699161658, 67.15552362291680311 ) ) ;
#55229=ORIENTED_EDGE ( 'NONE', *, *, #10905, .T. ) ;
#55251=CARTESIAN_POINT ( 'NONE',  ( -11.00000000000010303, -4.556349186103947346, 110.5937499999999716 ) ) ;
#55277=ORIENTED_EDGE ( 'NONE', *, *, #38998, .T. ) ;
#55284=CARTESIAN_POINT ( 'NONE',  ( -10.18810118749999916, 0.000000000000000000, 96.15625000204838102 ) ) ;
#55295=CARTESIAN_POINT ( 'NONE',  ( -6.238412754330611322E-16, 10.18810118749999916, 82.65625000204838102 ) ) ;
#55300=CARTESIAN_POINT ( 'NONE',  ( 11.00000000000000000, 1.347111479062088405E-15, 112.9375000040967763 ) ) ;
#55308=CARTESIAN_POINT ( 'NONE',  ( -10.18810118749999738, -4.220049686691941915, 85.75000000204838102 ) ) ;
#55311=CARTESIAN_POINT ( 'NONE',  ( -10.99999999999989342, 4.556349186104152515, 110.4062500000000142 ) ) ;
#55344=CARTESIAN_POINT ( 'NONE',  ( 4.556349186104045934, 11.00000000000000000, 71.03124999999998579 ) ) ;
#55355=CARTESIAN_POINT ( 'NONE',  ( 4.556349186104052151, -10.99999999999999822, 70.46874999999998579 ) ) ;
#55371=CARTESIAN_POINT ( 'NONE',  ( 10.18810118750000093, -4.220049686691933921, 113.3125000020483668 ) ) ;
#55385=CARTESIAN_POINT ( 'NONE',  ( -10.18810118749999738, -4.220049686691941915, 107.1250000020483810 ) ) ;
#55405=AXIS2_PLACEMENT_3D ( 'NONE', #3561, #26551, #8846 ) ;
#55423=CARTESIAN_POINT ( 'NONE',  ( -10.18810118749999916, 4.220049686691934809, 79.56250000204836681 ) ) ;
#55426=CARTESIAN_POINT ( 'NONE',  ( 11.00000000000000000, 4.556349186104045934, 87.34374999999998579 ) ) ;
#55430=CARTESIAN_POINT ( 'NONE',  ( 11.00000000000000000, 1.347111479062088405E-15, 84.24999999999998579 ) ) ;
#55449=VERTEX_POINT ( 'NONE', #64181 ) ;
#55453=CARTESIAN_POINT ( 'NONE',  ( -11.00000000000000000, 0.000000000000000000, 79.18750000409677625 ) ) ;
#55461=( BOUNDED_CURVE ( )  B_SPLINE_CURVE ( 2, ( #464, #41176, #13588, #63806, #12491, #35521, #29855, #52866, #49801 ),
 .UNSPECIFIED., .F., .F. ) 
 B_SPLINE_CURVE_WITH_KNOTS ( ( 3, 2, 2, 2, 3 ),
 ( 0.3382352941176470229, 0.3419117647058823040, 0.3455882352941175850, 0.3492647058823528661, 0.3529411764705882026 ),
 .UNSPECIFIED. ) 
 CURVE ( )  GEOMETRIC_REPRESENTATION_ITEM ( )  RATIONAL_B_SPLINE_CURVE ( ( 1.000000000000001110, 0.9238795325112856283, 1.000000000000000000, 0.9238795325112867385, 1.000000000000000000, 0.9238795325112867385, 1.000000000000000000, 0.9238795325112878487, 0.9999999999999988898 ) ) 
 REPRESENTATION_ITEM ( '' )  );
#55469=CARTESIAN_POINT ( 'NONE',  ( 7.204075437095966983, 7.204075437095967871, 79.09375000204838102 ) ) ;
#55471=FACE_OUTER_BOUND ( 'NONE', #21053, .T. ) ;
#55480=CARTESIAN_POINT ( 'NONE',  ( 7.204075437095966983, 7.204075437095967871, 86.96875000204836681 ) ) ;
#55485=CARTESIAN_POINT ( 'NONE',  ( -10.18810118749999916, 0.000000000000000000, 97.65625000204838102 ) ) ;
#55495=CARTESIAN_POINT ( 'NONE',  ( 7.204075437095966983, 7.204075437095967871, 94.46875000204838102 ) ) ;
#55514=CARTESIAN_POINT ( 'NONE',  ( -10.18810118749999916, 0.000000000000000000, 99.15625000204838102 ) ) ;
#55517=CARTESIAN_POINT ( 'NONE',  ( -6.735557395310442023E-16, 11.00000000000000000, 110.1249999999999858 ) ) ;
#55521=VECTOR ( 'NONE', #50366, 1000.000000000000000 ) ;
#55527=DIRECTION ( 'NONE',  ( 0.000000000000000000, 0.000000000000000000, 1.000000000000000000 ) ) ;
#55529=EDGE_CURVE ( 'NONE', #2280, #37130, #22341, .T. ) ;
#55548=CARTESIAN_POINT ( 'NONE',  ( -11.00000000000000000, 0.000000000000000000, 97.18750000409677625 ) ) ;
#55569=CARTESIAN_POINT ( 'NONE',  ( 1.871523826299183495E-15, -10.18810118749999916, 102.9062500020483810 ) ) ;
#55577=VERTEX_POINT ( 'NONE', #28022 ) ;
#55578=CARTESIAN_POINT ( 'NONE',  ( -4.220049686691935698, 10.18810118749999916, 115.3750000020483810 ) ) ;
#55583=AXIS2_PLACEMENT_3D ( 'NONE', #18246, #41262, #41630 ) ;
#55587=CARTESIAN_POINT ( 'NONE',  ( 10.18810118750000093, -4.220049686691933921, 110.6875000020483952 ) ) ;
#55596=CARTESIAN_POINT ( 'NONE',  ( 10.18810118749999916, 1.247682550866122264E-15, 71.78125000204838102 ) ) ;
#55605=CARTESIAN_POINT ( 'NONE',  ( -4.220049686691935698, 10.18810118749999916, 116.8750000020483952 ) ) ;
#55606=CARTESIAN_POINT ( 'NONE',  ( -7.778174593052020747, -7.778174593052023411, 83.87500000409677625 ) ) ;
#55618=DIRECTION ( 'NONE',  ( -0.000000000000000000, -0.000000000000000000, -1.000000000000000000 ) ) ;
#55619=LINE ( 'NONE', #21264, #48316 ) ;
#55622=CARTESIAN_POINT ( 'NONE',  ( -11.00000000000000000, 0.000000000000000000, 107.6875000040967763 ) ) ;
#55658=CARTESIAN_POINT ( 'NONE',  ( 10.18810118750000093, -4.220049686691933921, 89.31250000204838102 ) ) ;
#55670=CARTESIAN_POINT ( 'NONE',  ( 10.18810118749999916, 1.247682550866122264E-15, 83.78125000204838102 ) ) ;
#55685=CARTESIAN_POINT ( 'NONE',  ( 4.220049686691941027, -10.18810118749999738, 78.62500000204838102 ) ) ;
#55688=CARTESIAN_POINT ( 'NONE',  ( -4.556349186104045934, 11.00000000000000000, 110.2187499999999858 ) ) ;
#55699=CARTESIAN_POINT ( 'NONE',  ( -4.556349186104048599, -10.99999999999999822, 73.46875000409677625 ) ) ;
#55719=CARTESIAN_POINT ( 'NONE',  ( -11.00000000000000000, 0.000000000000000000, 71.49999999999998579 ) ) ;
#55722=CARTESIAN_POINT ( 'NONE',  ( -7.778174593052023411, 7.778174593052023411, 110.5000000040967763 ) ) ;
#55729=DIRECTION ( 'NONE',  ( 0.000000000000000000, 0.000000000000000000, -1.000000000000000000 ) ) ;
#55745=CARTESIAN_POINT ( 'NONE',  ( 4.220049686691941027, -10.18810118749999738, 108.6250000020483668 ) ) ;
#55759=CARTESIAN_POINT ( 'NONE',  ( 1.871523826299183495E-15, -10.18810118749999916, 98.40625000204838102 ) ) ;
#55762=ORIENTED_EDGE ( 'NONE', *, *, #74133, .F. ) ;
#55778=CARTESIAN_POINT ( 'NONE',  ( -10.18810118749999916, 4.220049686691934809, 78.43750000204838102 ) ) ;
#55795=ORIENTED_EDGE ( 'NONE', *, *, #44504, .T. ) ;
#55796=( BOUNDED_CURVE ( )  B_SPLINE_CURVE ( 2, ( #65075, #42804, #31875, #37162, #53411, #30757, #71472, #1734, #48840 ),
 .UNSPECIFIED., .F., .F. ) 
 B_SPLINE_CURVE_WITH_KNOTS ( ( 3, 2, 2, 2, 3 ),
 ( 0.2205882352941175018, 0.2242647058823528106, 0.2279411764705880916, 0.2316176470588234004, 0.2352941176470586815 ),
 .UNSPECIFIED. ) 
 CURVE ( )  GEOMETRIC_REPRESENTATION_ITEM ( )  RATIONAL_B_SPLINE_CURVE ( ( 1.000000000000002887, 0.9238795325112838519, 1.000000000000000000, 0.9238795325112867385, 1.000000000000000000, 0.9238795325112867385, 1.000000000000000000, 0.9238795325112896251, 0.9999999999999971134 ) ) 
 REPRESENTATION_ITEM ( '' )  );
#55798=CARTESIAN_POINT ( 'NONE',  ( 7.204075437095966983, 7.204075437095967871, 71.59375000204836681 ) ) ;
#55800=CARTESIAN_POINT ( 'NONE',  ( 0.000000000000000000, 0.000000000000000000, 41.99999999999999289 ) ) ;
#55801=CARTESIAN_POINT ( 'NONE',  ( 2.020667218593132706E-15, -11.00000000000000000, 88.37499999999998579 ) ) ;
#55805=CARTESIAN_POINT ( 'NONE',  ( -11.00000000000000000, 0.000000000000000000, 83.49999999999998579 ) ) ;
#55808=EDGE_CURVE ( 'NONE', #36810, #73904, #1226, .T. ) ;
#55832=CARTESIAN_POINT ( 'NONE',  ( 4.556349186104051263, -10.99999999999999822, 79.65625000409677625 ) ) ;
#55849=CARTESIAN_POINT ( 'NONE',  ( -7.204075437095965206, -7.204075437095968759, 75.34375000204838102 ) ) ;
#55858=CARTESIAN_POINT ( 'NONE',  ( -4.220049686691935698, 10.18810118749999916, 87.25000000204838102 ) ) ;
#55860=CARTESIAN_POINT ( 'NONE',  ( -11.00000000000000000, 0.000000000000000000, 89.68750000409677625 ) ) ;
#55864=ORIENTED_EDGE ( 'NONE', *, *, #473, .F. ) ;
#55865=ORIENTED_EDGE ( 'NONE', *, *, #70130, .T. ) ;
#55870=CARTESIAN_POINT ( 'NONE',  ( 4.220049686691934809, 10.18810118749999916, 94.56250000204838102 ) ) ;
#55884=ORIENTED_EDGE ( 'NONE', *, *, #38998, .F. ) ;
#55886=CARTESIAN_POINT ( 'NONE',  ( 10.18810118749999916, 4.220049686691935698, 89.50000000204836681 ) ) ;
#55889=CARTESIAN_POINT ( 'NONE',  ( 7.778174593052023411, -7.778174593052021635, 106.5624999999999858 ) ) ;
#55919=EDGE_LOOP ( 'NONE', ( #38412, #56519, #51099, #3213 ) ) ;
#55924=CARTESIAN_POINT ( 'NONE',  ( -7.778174593052020747, -7.778174593052023411, 95.87500000409676204 ) ) ;
#55927=CARTESIAN_POINT ( 'NONE',  ( 7.778174593052021635, 7.778174593052023411, 117.4375000000000000 ) ) ;
#55937=ORIENTED_EDGE ( 'NONE', *, *, #65254, .T. ) ;
#55946=CARTESIAN_POINT ( 'NONE',  ( -7.204075437095967871, 7.204075437095967871, 100.8437500020483668 ) ) ;
#55955=CARTESIAN_POINT ( 'NONE',  ( -4.220049686691937474, -10.18810118749999738, 115.9375000020483668 ) ) ;
#55963=CARTESIAN_POINT ( 'NONE',  ( 10.18810118750000093, -4.220049686691933921, 109.1875000020483810 ) ) ;
#55971=CARTESIAN_POINT ( 'NONE',  ( 10.18810118749999916, 4.220049686691935698, 70.37500000204838102 ) ) ;
#55976=CARTESIAN_POINT ( 'NONE',  ( -11.00000000000000000, 0.000000000000000000, 91.00000000000000000 ) ) ;
#56025=CARTESIAN_POINT ( 'NONE',  ( -6.735557395310442023E-16, 11.00000000000000000, 95.12499999999998579 ) ) ;
#56029=CARTESIAN_POINT ( 'NONE',  ( -10.18810118749999916, 4.220049686691934809, 88.56250000204836681 ) ) ;
#56042=CARTESIAN_POINT ( 'NONE',  ( -7.204075437095965206, -7.204075437095968759, 83.21875000204836681 ) ) ;
#56055=CARTESIAN_POINT ( 'NONE',  ( 4.220049686691934809, 10.18810118749999916, 77.68750000204838102 ) ) ;
#56060=VERTEX_POINT ( 'NONE', #67658 ) ;
#56073=EDGE_CURVE ( 'NONE', #34562, #50500, #68888, .T. ) ;
#56076=ORIENTED_EDGE ( 'NONE', *, *, #14446, .T. ) ;
#56085=CARTESIAN_POINT ( 'NONE',  ( -7.778174593052020747, -7.778174593052023411, 115.3750000040967905 ) ) ;
#56090=CARTESIAN_POINT ( 'NONE',  ( -11.00000000000000000, 0.000000000000000000, 68.49999999999997158 ) ) ;
#56093=CARTESIAN_POINT ( 'NONE',  ( -10.99999999999993427, 4.556349186104110771, 110.5937500040967620 ) ) ;
#56096=CARTESIAN_POINT ( 'NONE',  ( 7.778174593052023411, -7.778174593052021635, 114.2500000040967763 ) ) ;
#56115=CARTESIAN_POINT ( 'NONE',  ( -4.220049686691937474, -10.18810118749999738, 109.9375000020483952 ) ) ;
#56119=CARTESIAN_POINT ( 'NONE',  ( 4.556349186104052151, -10.99999999999999822, 97.46874999999998579 ) ) ;
#56131=CARTESIAN_POINT ( 'NONE',  ( -10.18810118749999916, 4.220049686691934809, 102.4375000020483810 ) ) ;
#56135=LINE ( 'NONE', #61784, #313 ) ;
#56139=CARTESIAN_POINT ( 'NONE',  ( 7.778174593052023411, -7.778174593052021635, 72.25000000409677625 ) ) ;
#56146=VERTEX_POINT ( 'NONE', #62723 ) ;
#56149=CARTESIAN_POINT ( 'NONE',  ( 7.204075437095966983, 7.204075437095967871, 80.96875000204836681 ) ) ;
#56170=CARTESIAN_POINT ( 'NONE',  ( 10.18810118750000093, -4.220049686691933033, 72.81250000204838102 ) ) ;
#56173=CARTESIAN_POINT ( 'NONE',  ( 4.556349186104051263, -10.99999999999999822, 91.46874999999998579 ) ) ;
#56177=CARTESIAN_POINT ( 'NONE',  ( 7.778174593052021635, 7.778174593052023411, 88.93749999999998579 ) ) ;
#56195=CARTESIAN_POINT ( 'NONE',  ( -11.00000000000010303, -4.556349186103947346, 71.59374999999998579 ) ) ;
#56200=CARTESIAN_POINT ( 'NONE',  ( 7.778174593052023411, -7.778174593052021635, 76.75000000409676204 ) ) ;
#56216=CARTESIAN_POINT ( 'NONE',  ( 10.18810118749999916, 4.220049686691935698, 73.00000000204836681 ) ) ;
#56219=DIRECTION ( 'NONE',  ( -0.000000000000000000, -0.000000000000000000, -1.000000000000000000 ) ) ;
#56225=CARTESIAN_POINT ( 'NONE',  ( 4.220049686691941027, -10.18810118749999738, 79.00000000204838102 ) ) ;
#56229=( BOUNDED_CURVE ( )  B_SPLINE_CURVE ( 2, ( #21946, #57421, #62315, #5357, #56674, #17781, #74377, #57795, #52127 ),
 .UNSPECIFIED., .F., .F. ) 
 B_SPLINE_CURVE_WITH_KNOTS ( ( 3, 2, 2, 2, 3 ),
 ( 0.2647058823529410132, 0.2683823529411762943, 0.2720588235294115753, 0.2757352941176469674, 0.2794117647058822484 ),
 .UNSPECIFIED. ) 
 CURVE ( )  GEOMETRIC_REPRESENTATION_ITEM ( )  RATIONAL_B_SPLINE_CURVE ( ( 1.000000000000003553, 0.9238795325112832968, 1.000000000000000000, 0.9238795325112867385, 1.000000000000000000, 0.9238795325112867385, 1.000000000000000000, 0.9238795325112890700, 0.9999999999999976685 ) ) 
 REPRESENTATION_ITEM ( '' )  );
#56236=CARTESIAN_POINT ( 'NONE',  ( 7.204075437095968759, -7.204075437095966983, 92.59375000204838102 ) ) ;
#56252=CARTESIAN_POINT ( 'NONE',  ( -4.220049686691937474, -10.18810118749999738, 91.93750000204836681 ) ) ;
#56255=CARTESIAN_POINT ( 'NONE',  ( -4.556349186104045934, 11.00000000000000000, 107.2187500000000000 ) ) ;
#56284=CARTESIAN_POINT ( 'NONE',  ( -6.735557395310442023E-16, 11.00000000000000000, 92.31250000409677625 ) ) ;
#56306=CARTESIAN_POINT ( 'NONE',  ( 10.18810118749999916, 1.247682550866122264E-15, 97.28125000204838102 ) ) ;
#56316=CARTESIAN_POINT ( 'NONE',  ( 4.220049686691934809, 10.18810118749999916, 115.1875000020483668 ) ) ;
#56319=VECTOR ( 'NONE', #61640, 1000.000000000000000 ) ;
#56325=CARTESIAN_POINT ( 'NONE',  ( -7.204075437095965206, -7.204075437095968759, 111.7187500020483810 ) ) ;
#56342=ORIENTED_EDGE ( 'NONE', *, *, #51131, .F. ) ;
#56343=CARTESIAN_POINT ( 'NONE',  ( -7.204075437095967871, 7.204075437095967871, 107.9687500020483810 ) ) ;
#56365=CARTESIAN_POINT ( 'NONE',  ( -7.778174593052020747, -7.778174593052023411, 82.37500000409677625 ) ) ;
#56366=PLANE ( 'NONE',  #50290 ) ;
#56391=CARTESIAN_POINT ( 'NONE',  ( -10.18810118749999916, 0.000000000000000000, 88.65625000204838102 ) ) ;
#56393=AXIS2_PLACEMENT_3D ( 'NONE', #38924, #15148, #67223 ) ;
#56400=CARTESIAN_POINT ( 'NONE',  ( -6.735557395310442023E-16, 11.00000000000000000, 108.8125000040967763 ) ) ;
#56405=CARTESIAN_POINT ( 'NONE',  ( -6.238412754330611322E-16, 10.18810118749999916, 85.65625000204838102 ) ) ;
#56418=CARTESIAN_POINT ( 'NONE',  ( 10.18810118749999916, 1.247682550866122264E-15, 75.90625000204836681 ) ) ;
#56439=EDGE_CURVE ( 'NONE', #5598, #60666, #59205, .T. ) ;
#56450=( BOUNDED_CURVE ( )  B_SPLINE_CURVE ( 2, ( #21281, #26942, #49961, #44305, #67320, #15617, #38656, #8108, #25442 ),
 .UNSPECIFIED., .F., .F. ) 
 B_SPLINE_CURVE_WITH_KNOTS ( ( 3, 2, 2, 2, 3 ),
 ( 0.7500000000000000000, 0.7536764705882352811, 0.7573529411764705621, 0.7610294117647058432, 0.7647058823529411242 ),
 .UNSPECIFIED. ) 
 CURVE ( )  GEOMETRIC_REPRESENTATION_ITEM ( )  RATIONAL_B_SPLINE_CURVE ( ( 1.000000000000000000, 0.9238795325112867385, 1.000000000000000000, 0.9238795325112867385, 1.000000000000000000, 0.9238795325112867385, 1.000000000000000000, 0.9238795325112867385, 1.000000000000000000 ) ) 
 REPRESENTATION_ITEM ( '' )  );
#56455=DIRECTION ( 'NONE',  ( 0.000000000000000000, 0.000000000000000000, 1.000000000000000000 ) ) ;
#56458=CARTESIAN_POINT ( 'NONE',  ( -4.556349186104045934, 11.00000000000000000, 72.71874999999997158 ) ) ;
#56478=CARTESIAN_POINT ( 'NONE',  ( -7.778174593052023411, 7.778174593052023411, 81.81249999999998579 ) ) ;
#56485=CARTESIAN_POINT ( 'NONE',  ( 10.18810118750000093, -4.220049686691933921, 105.8125000020483952 ) ) ;
#56501=CARTESIAN_POINT ( 'NONE',  ( 10.18810118750000093, -4.220049686691933033, 100.1875000020483952 ) ) ;
#56503=ORIENTED_EDGE ( 'NONE', *, *, #69873, .T. ) ;
#56511=CARTESIAN_POINT ( 'NONE',  ( 11.00000000000000000, 1.347111479062088405E-15, 67.93750000409676204 ) ) ;
#56519=ORIENTED_EDGE ( 'NONE', *, *, #13144, .T. ) ;
#56523=CARTESIAN_POINT ( 'NONE',  ( -10.18810118749999916, 0.000000000000000000, 81.53125000204838102 ) ) ;
#56542=CARTESIAN_POINT ( 'NONE',  ( 4.220049686691941027, -10.18810118749999738, 77.12500000204838102 ) ) ;
#56545=CARTESIAN_POINT ( 'NONE',  ( -4.556349186104047710, -10.99999999999999822, 86.78124999999998579 ) ) ;
#56556=ORIENTED_EDGE ( 'NONE', *, *, #16396, .F. ) ;
#56574=CARTESIAN_POINT ( 'NONE',  ( -11.00000000000000000, 0.000000000000000000, 76.18750000409677625 ) ) ;
#56593=CARTESIAN_POINT ( 'NONE',  ( 4.220049686691934809, 10.18810118749999916, 68.68750000204836681 ) ) ;
#56603=CARTESIAN_POINT ( 'NONE',  ( -4.220049686691935698, 10.18810118749999916, 79.75000000204838102 ) ) ;
#56611=VERTEX_POINT ( 'NONE', #16702 ) ;
#56632=CARTESIAN_POINT ( 'NONE',  ( -10.18810118749999738, -4.220049686691941915, 93.25000000204838102 ) ) ;
#56635=CARTESIAN_POINT ( 'NONE',  ( -10.99999999999999822, -4.556349186104052151, 104.5937499999999716 ) ) ;
#56657=CARTESIAN_POINT ( 'NONE',  ( -4.556349186104048599, -10.99999999999999822, 88.28124999999998579 ) ) ;
#56660=AXIS2_PLACEMENT_3D ( 'NONE', #3291, #14962, #49298 ) ;
#56663=CARTESIAN_POINT ( 'NONE',  ( -4.556349186104047710, -10.99999999999999822, 91.46875000409676204 ) ) ;
#56674=CARTESIAN_POINT ( 'NONE',  ( -6.735557395310442023E-16, 11.00000000000000000, 102.8125000040967763 ) ) ;
#56685=CARTESIAN_POINT ( 'NONE',  ( -4.220049686691935698, 10.18810118749999916, 96.25000000204838102 ) ) ;
#56694=CARTESIAN_POINT ( 'NONE',  ( 4.220049686691934809, 10.18810118749999916, 113.6875000020483952 ) ) ;
#56704=CARTESIAN_POINT ( 'NONE',  ( 10.18810118749999916, 1.247682550866122264E-15, 107.7812500020483810 ) ) ;
#56719=CARTESIAN_POINT ( 'NONE',  ( -10.18810118749999916, 4.220049686691934809, 112.5625000020483810 ) ) ;
#56745=CARTESIAN_POINT ( 'NONE',  ( 7.778174593052023411, -7.778174593052021635, 112.7500000040967763 ) ) ;
#56760=LINE ( 'NONE', #34131, #42386 ) ;
#56766=EDGE_CURVE ( 'NONE', #10672, #62018, #57852, .T. ) ;
#56767=CARTESIAN_POINT ( 'NONE',  ( 4.220049686691941027, -10.18810118749999738, 90.62500000204836681 ) ) ;
#56772=CARTESIAN_POINT ( 'NONE',  ( -6.238412754330611322E-16, 10.18810118749999916, 114.1562500020483810 ) ) ;
#56779=CARTESIAN_POINT ( 'NONE',  ( 10.18810118749999916, 4.220049686691935698, 82.37500000204838102 ) ) ;
#56794=CARTESIAN_POINT ( 'NONE',  ( -10.18810118749999916, 0.000000000000000000, 75.15625000204836681 ) ) ;
#56814=CARTESIAN_POINT ( 'NONE',  ( -11.00000000000010658, 4.556349186103942017, 74.59375000409676204 ) ) ;
#56815=VERTEX_POINT ( 'NONE', #22742 ) ;
#56832=CARTESIAN_POINT ( 'NONE',  ( 10.99999999999989342, 4.556349186104152515, 84.53125000409679046 ) ) ;
#56834=ADVANCED_FACE ( 'NONE', ( #513 ), #51053, .T. ) ;
#56837=CARTESIAN_POINT ( 'NONE',  ( -4.556349186104048599, -10.99999999999999822, 112.4687500040967905 ) ) ;
#56856=EDGE_CURVE ( 'NONE', #22034, #37225, #66902, .T. ) ;
#56857=CARTESIAN_POINT ( 'NONE',  ( 4.220049686691934809, 10.18810118749999916, 104.6875000020483810 ) ) ;
#56874=CARTESIAN_POINT ( 'NONE',  ( 10.18810118749999916, 4.220049686691935698, 103.3750000020483952 ) ) ;
#56876=VERTEX_POINT ( 'NONE', #31002 ) ;
#56879=CARTESIAN_POINT ( 'NONE',  ( 0.000000000000000000, 0.000000000000000000, 41.99999999999999289 ) ) ;
#56887=CARTESIAN_POINT ( 'NONE',  ( -4.220049686691937474, -10.18810118749999738, 96.43750000204836681 ) ) ;
#56896=CARTESIAN_POINT ( 'NONE',  ( -6.238412754330611322E-16, 10.18810118749999916, 78.15625000204836681 ) ) ;
#56899=( BOUNDED_CURVE ( )  B_SPLINE_CURVE ( 2, ( #64700, #36036, #47700, #6259, #13362, #19774, #42045, #48443, #31094 ),
 .UNSPECIFIED., .F., .F. ) 
 B_SPLINE_CURVE_WITH_KNOTS ( ( 3, 2, 2, 2, 3 ),
 ( 0.000000000000000000, 0.003676470588235296235, 0.007352941176470592470, 0.01102941176470589001, 0.01470588235294118494 ),
 .UNSPECIFIED. ) 
 CURVE ( )  GEOMETRIC_REPRESENTATION_ITEM ( )  RATIONAL_B_SPLINE_CURVE ( ( 1.000000000000000000, 0.9238795325112867385, 1.000000000000000000, 0.9238795325112867385, 1.000000000000000000, 0.9238795325112867385, 1.000000000000000000, 0.9238795325112865164, 1.000000000000000222 ) ) 
 REPRESENTATION_ITEM ( '' )  );
#56915=ORIENTED_EDGE ( 'NONE', *, *, #49321, .T. ) ;
#56916=CARTESIAN_POINT ( 'NONE',  ( -7.204075437095965206, -7.204075437095968759, 72.34375000204836681 ) ) ;
#56919=CARTESIAN_POINT ( 'NONE',  ( -4.556349186104047710, -10.99999999999999822, 80.78124999999998579 ) ) ;
#56944=CARTESIAN_POINT ( 'NONE',  ( -6.735557395310442023E-16, 11.00000000000000000, 74.31250000409676204 ) ) ;
#56959=CARTESIAN_POINT ( 'NONE',  ( 10.18810118749999916, 1.247682550866122264E-15, 116.7812500020483810 ) ) ;
#56963=CARTESIAN_POINT ( 'NONE',  ( -10.18810118749999916, 0.000000000000000000, 72.15625000204836681 ) ) ;
#56974=ADVANCED_FACE ( 'NONE', ( #35938 ), #70628, .T. ) ;
#56977=EDGE_CURVE ( 'NONE', #17226, #32089, #2335, .T. ) ;
#56991=( BOUNDED_CURVE ( )  B_SPLINE_CURVE ( 2, ( #70002, #74536, #22847, #13365, #54504, #59417, #31481, #3186, #54876 ),
 .UNSPECIFIED., .F., .F. ) 
 B_SPLINE_CURVE_WITH_KNOTS ( ( 3, 2, 2, 2, 3 ),
 ( 0.5441176470588233727, 0.5477941176470587648, 0.5514705882352940458, 0.5551470588235293269, 0.5588235294117646079 ),
 .UNSPECIFIED. ) 
 CURVE ( )  GEOMETRIC_REPRESENTATION_ITEM ( )  RATIONAL_B_SPLINE_CURVE ( ( 1.000000000000002220, 0.9238795325112844070, 1.000000000000000000, 0.9238795325112867385, 1.000000000000000000, 0.9238795325112867385, 1.000000000000000000, 0.9238795325112890700, 0.9999999999999976685 ) ) 
 REPRESENTATION_ITEM ( '' )  );
#56999=CARTESIAN_POINT ( 'NONE',  ( -10.18810118749999916, 4.220049686691934809, 91.56250000204838102 ) ) ;
#57002=CARTESIAN_POINT ( 'NONE',  ( -11.00000000000000000, 0.000000000000000000, 108.9999999999999858 ) ) ;
#57004=CYLINDRICAL_SURFACE ( 'NONE', #57947, 11.00000000000000000 ) ;
#57031=ORIENTED_EDGE ( 'NONE', *, *, #69703, .T. ) ;
#57034=CARTESIAN_POINT ( 'NONE',  ( -4.556349186104047710, -10.99999999999999822, 89.96875000409677625 ) ) ;
#57056=CARTESIAN_POINT ( 'NONE',  ( -10.18810118749999738, -4.220049686691941915, 99.62500000204838102 ) ) ;
#57060=CARTESIAN_POINT ( 'NONE',  ( 11.00000000000000000, 1.347111479062088405E-15, 97.74999999999998579 ) ) ;
#57064=CARTESIAN_POINT ( 'NONE',  ( -4.220049686691937474, -10.18810118749999738, 106.9375000020483810 ) ) ;
#57067=AXIS2_PLACEMENT_3D ( 'NONE', #2633, #2256, #25249 ) ;
#57073=CARTESIAN_POINT ( 'NONE',  ( 4.220049686691941027, -10.18810118749999738, 106.0000000020483668 ) ) ;
#57078=ADVANCED_FACE ( 'NONE', ( #38167 ), #73239, .T. ) ;
#57084=ORIENTED_EDGE ( 'NONE', *, *, #51466, .T. ) ;
#57087=CARTESIAN_POINT ( 'NONE',  ( -4.220049686691937474, -10.18810118749999738, 112.9375000020483810 ) ) ;
#57096=CARTESIAN_POINT ( 'NONE',  ( 10.99999999999992006, -4.556349186104122317, 109.6562499999999858 ) ) ;
#57099=CARTESIAN_POINT ( 'NONE',  ( 2.020667218593132706E-15, -11.00000000000000000, 91.37499999999998579 ) ) ;
#57116=CARTESIAN_POINT ( 'NONE',  ( -10.99999999999999822, -4.556349186104052151, 112.2812500040967763 ) ) ;
#57118=CARTESIAN_POINT ( 'NONE',  ( -7.778174593052020747, -7.778174593052023411, 70.18749999999998579 ) ) ;
#57133=LINE ( 'NONE', #34882, #7373 ) ;
#57137=CARTESIAN_POINT ( 'NONE',  ( 7.204075437095966983, 7.204075437095967871, 91.09375000204838102 ) ) ;
#57142=CARTESIAN_POINT ( 'NONE',  ( -10.18810118749999738, -4.220049686691941915, 116.1250000020483810 ) ) ;
#57144=CARTESIAN_POINT ( 'NONE',  ( -10.99999999999991829, 4.556349186104124982, 109.0937500040967763 ) ) ;
#57150=CARTESIAN_POINT ( 'NONE',  ( -10.18810118749999916, 4.220049686691934809, 79.93750000204838102 ) ) ;
#57162=CARTESIAN_POINT ( 'NONE',  ( 10.18810118749999916, 1.247682550866122264E-15, 80.40625000204838102 ) ) ;
#57164=ADVANCED_FACE ( 'NONE', ( #3456 ), #15134, .T. ) ;
#57186=ORIENTED_EDGE ( 'NONE', *, *, #31714, .F. ) ;
#57227=CARTESIAN_POINT ( 'NONE',  ( -2.299997487996822354, 10.65384601377883023, 117.6108347966737426 ) ) ;
#57228=CARTESIAN_POINT ( 'NONE',  ( 7.204075437095968759, -7.204075437095966983, 107.2187500020483810 ) ) ;
#57238=( BOUNDED_CURVE ( )  B_SPLINE_CURVE ( 2, ( #55112, #27163, #3795, #49431, #2672, #72825, #32854, #72058, #55860 ),
 .UNSPECIFIED., .F., .F. ) 
 B_SPLINE_CURVE_WITH_KNOTS ( ( 3, 2, 2, 2, 3 ),
 ( 0.5147058823529412352, 0.5183823529411765163, 0.5220588235294116863, 0.5257352941176468564, 0.5294117647058820264 ),
 .UNSPECIFIED. ) 
 CURVE ( )  GEOMETRIC_REPRESENTATION_ITEM ( )  RATIONAL_B_SPLINE_CURVE ( ( 0.9999999999999976685, 0.9238795325112890700, 1.000000000000000000, 0.9238795325112867385, 1.000000000000000000, 0.9238795325112867385, 1.000000000000000000, 0.9238795325112936219, 0.9999999999999931166 ) ) 
 REPRESENTATION_ITEM ( '' )  );
#57245=CARTESIAN_POINT ( 'NONE',  ( 7.204075437095968759, -7.204075437095966983, 103.0937500020483668 ) ) ;
#57250=FACE_OUTER_BOUND ( 'NONE', #2138, .T. ) ;
#57255=AXIS2_PLACEMENT_3D ( 'NONE', #66204, #2094, #25827 ) ;
#57259=CARTESIAN_POINT ( 'NONE',  ( -4.220049686691937474, -10.18810118749999738, 93.43750000204836681 ) ) ;
#57269=CARTESIAN_POINT ( 'NONE',  ( -4.220049686691937474, -10.18810118749999738, 81.81250000204838102 ) ) ;
#57289=CARTESIAN_POINT ( 'NONE',  ( -10.18810118749999916, 4.220049686691934809, 72.06250000204836681 ) ) ;
#57292=CARTESIAN_POINT ( 'NONE',  ( -6.735557395310442023E-16, 11.00000000000000000, 83.12499999999998579 ) ) ;
#57295=FACE_OUTER_BOUND ( 'NONE', #55919, .T. ) ;
#57297=FACE_BOUND ( 'NONE', #40264, .T. ) ;
#57317=FACE_OUTER_BOUND ( 'NONE', #27712, .T. ) ;
#57318=CARTESIAN_POINT ( 'NONE',  ( 7.778174593052021635, 7.778174593052023411, 80.12500000409677625 ) ) ;
#57320=CARTESIAN_POINT ( 'NONE',  ( -4.556349186104045934, 11.00000000000000000, 77.40625000409676204 ) ) ;
#57337=CARTESIAN_POINT ( 'NONE',  ( 7.204075437095966983, 7.204075437095967871, 70.09375000204836681 ) ) ;
#57342=CARTESIAN_POINT ( 'NONE',  ( -7.778174593052020747, -7.778174593052023411, 79.37500000409677625 ) ) ;
#57354=AXIS2_PLACEMENT_3D ( 'NONE', #63097, #11422, #34459 ) ;
#57364=ORIENTED_EDGE ( 'NONE', *, *, #12875, .T. ) ;
#57374=CARTESIAN_POINT ( 'NONE',  ( 10.18810118750000093, -4.220049686691933033, 93.81250000204838102 ) ) ;
#57375=DIRECTION ( 'NONE',  ( -0.000000000000000000, -0.000000000000000000, -1.000000000000000000 ) ) ;
#57377=CARTESIAN_POINT ( 'NONE',  ( 11.00000000000000000, 1.347111479062088405E-15, 100.7499999999999858 ) ) ;
#57379=CARTESIAN_POINT ( 'NONE',  ( 2.020667218593132706E-15, -11.00000000000000000, 86.87499999999998579 ) ) ;
#57408=CARTESIAN_POINT ( 'NONE',  ( 4.556349186104051263, -10.99999999999999822, 93.15625000409676204 ) ) ;
#57421=CARTESIAN_POINT ( 'NONE',  ( -11.00000000000015810, 4.556349186103888727, 103.0937500040967905 ) ) ;
#57432=CARTESIAN_POINT ( 'NONE',  ( 7.204075437095968759, -7.204075437095966983, 98.59375000204836681 ) ) ;
#57434=AXIS2_PLACEMENT_3D ( 'NONE', #58098, #6410, #52793 ) ;
#57440=CARTESIAN_POINT ( 'NONE',  ( -10.18810118749999916, 0.000000000000000000, 106.6562500020483668 ) ) ;
#57448=ADVANCED_FACE ( 'NONE', ( #48257 ), #41137, .T. ) ;
#57449=( BOUNDED_CURVE ( )  B_SPLINE_CURVE ( 2, ( #5388, #33328, #28759, #40457, #5023, #63456, #62710, #23098, #29139 ),
 .UNSPECIFIED., .F., .F. ) 
 B_SPLINE_CURVE_WITH_KNOTS ( ( 3, 2, 2, 2, 3 ),
 ( 0.8235294117647058432, 0.8272058823529411242, 0.8308823529411766273, 0.8345588235294119084, 0.8382352941176471894 ),
 .UNSPECIFIED. ) 
 CURVE ( )  GEOMETRIC_REPRESENTATION_ITEM ( )  RATIONAL_B_SPLINE_CURVE ( ( 1.000000000000000000, 0.9238795325112867385, 1.000000000000000000, 0.9238795325112867385, 1.000000000000000000, 0.9238795325112867385, 1.000000000000000000, 0.9238795325112844070, 1.000000000000002220 ) ) 
 REPRESENTATION_ITEM ( '' )  );
#57450=CARTESIAN_POINT ( 'NONE',  ( -6.238412754330611322E-16, 10.18810118749999916, 103.6562500020483810 ) ) ;
#57454=DIRECTION ( 'NONE',  ( 0.000000000000000000, 0.000000000000000000, -1.000000000000000000 ) ) ;
#57457=CARTESIAN_POINT ( 'NONE',  ( 11.00000000000000000, 1.347111479062088405E-15, 81.24999999999998579 ) ) ;
#57469=CARTESIAN_POINT ( 'NONE',  ( 1.871523826299183495E-15, -10.18810118749999916, 108.5312500020483810 ) ) ;
#57489=CARTESIAN_POINT ( 'NONE',  ( 4.220049686691941027, -10.18810118749999738, 71.50000000204839523 ) ) ;
#57493=DIRECTION ( 'NONE',  ( -1.000000000000000000, 0.000000000000000000, 0.000000000000000000 ) ) ;
#57501=CARTESIAN_POINT ( 'NONE',  ( 11.00000000000000000, 4.556349186104045934, 113.0312500040967763 ) ) ;
#57522=CARTESIAN_POINT ( 'NONE',  ( -7.204075437095965206, -7.204075437095968759, 82.84375000204838102 ) ) ;
#57525=CARTESIAN_POINT ( 'NONE',  ( -6.735557395310442023E-16, 11.00000000000000000, 113.1249999999999858 ) ) ;
#57526=CARTESIAN_POINT ( 'NONE',  ( 7.204075437095968759, -7.204075437095966983, 116.5937500020483810 ) ) ;
#57533=CARTESIAN_POINT ( 'NONE',  ( -4.220049686691937474, -10.18810118749999738, 74.31250000204836681 ) ) ;
#57546=CARTESIAN_POINT ( 'NONE',  ( -6.238412754330611322E-16, 10.18810118749999916, 73.28125000204838102 ) ) ;
#57567=CARTESIAN_POINT ( 'NONE',  ( 11.00000000000000000, 4.556349186104045934, 74.03125000409677625 ) ) ;
#57583=CARTESIAN_POINT ( 'NONE',  ( -11.00000000000000000, 0.000000000000000000, 85.18750000409677625 ) ) ;
#57606=CARTESIAN_POINT ( 'NONE',  ( -10.18810118749999916, 0.000000000000000000, 102.1562500020483810 ) ) ;
#57622=CARTESIAN_POINT ( 'NONE',  ( 10.18810118750000093, -4.220049686691933033, 97.18750000204836681 ) ) ;
#57636=CARTESIAN_POINT ( 'NONE',  ( -7.204075437095967871, 7.204075437095967871, 86.96875000204836681 ) ) ;
#57647=CARTESIAN_POINT ( 'NONE',  ( 10.18810118749999916, 1.247682550866122264E-15, 76.28125000204836681 ) ) ;
#57664=CARTESIAN_POINT ( 'NONE',  ( -6.238412754330611322E-16, 10.18810118749999916, 67.28125000204838102 ) ) ;
#57667=CARTESIAN_POINT ( 'NONE',  ( -4.556349186104045934, 11.00000000000000000, 86.21874999999998579 ) ) ;
#57675=( BOUNDED_CURVE ( )  B_SPLINE_CURVE ( 2, ( #63828, #485, #23465, #69497, #40822, #39339, #62336, #10664, #61843 ),
 .UNSPECIFIED., .F., .F. ) 
 B_SPLINE_CURVE_WITH_KNOTS ( ( 3, 2, 2, 2, 3 ),
 ( 0.7794117647058822484, 0.7830882352941175295, 0.7867647058823528106, 0.7904411764705880916, 0.7941176470588233727 ),
 .UNSPECIFIED. ) 
 CURVE ( )  GEOMETRIC_REPRESENTATION_ITEM ( )  RATIONAL_B_SPLINE_CURVE ( ( 1.000000000000002220, 0.9238795325112844070, 1.000000000000000000, 0.9238795325112867385, 1.000000000000000000, 0.9238795325112867385, 1.000000000000000000, 0.9238795325112890700, 0.9999999999999976685 ) ) 
 REPRESENTATION_ITEM ( '' )  );
#57693=CARTESIAN_POINT ( 'NONE',  ( 4.556349186104052151, -10.99999999999999822, 116.9687500000000142 ) ) ;
#57696=CARTESIAN_POINT ( 'NONE',  ( 11.00000000000000355, -4.556349186104045046, 76.84375000409676204 ) ) ;
#57708=CARTESIAN_POINT ( 'NONE',  ( -7.204075437095967871, 7.204075437095967871, 111.3437500020483810 ) ) ;
#57712=CARTESIAN_POINT ( 'NONE',  ( 1.871523826299183495E-15, -10.18810118749999916, 72.53125000204838102 ) ) ;
#57720=CARTESIAN_POINT ( 'NONE',  ( 11.00000000000000000, 1.347111479062088405E-15, 75.24999999999998579 ) ) ;
#57726=ORIENTED_EDGE ( 'NONE', *, *, #30960, .F. ) ;
#57742=DIRECTION ( 'NONE',  ( -1.000000000000000000, 0.000000000000000000, 0.000000000000000000 ) ) ;
#57750=CARTESIAN_POINT ( 'NONE',  ( 7.204075437095968759, -7.204075437095966983, 84.71875000204836681 ) ) ;
#57753=CARTESIAN_POINT ( 'NONE',  ( 11.00000000000000000, 1.347111479062088405E-15, 102.2500000000000000 ) ) ;
#57784=CARTESIAN_POINT ( 'NONE',  ( 4.556349186104045934, 11.00000000000000000, 90.71875000409676204 ) ) ;
#57785=CARTESIAN_POINT ( 'NONE',  ( -11.00000000000000533, 11.00000000000000000, 41.99999999999999289 ) ) ;
#57795=CARTESIAN_POINT ( 'NONE',  ( 10.99999999999989342, 4.556349186104152515, 102.5312500040967763 ) ) ;
#57809=CARTESIAN_POINT ( 'NONE',  ( 1.871523826299183495E-15, -10.18810118749999916, 95.40625000204836681 ) ) ;
#57816=CARTESIAN_POINT ( 'NONE',  ( 4.220049686691941027, -10.18810118749999738, 108.6250000020483668 ) ) ;
#57826=CARTESIAN_POINT ( 'NONE',  ( 10.18810118750000093, -4.220049686691933921, 103.1875000020483810 ) ) ;
#57833=APPLICATION_CONTEXT ( 'automotive_design' ) ;
#57842=CARTESIAN_POINT ( 'NONE',  ( 10.18810118749999916, 4.220049686691935698, 107.5000000020483668 ) ) ;
#57852=LINE ( 'NONE', #18213, #67459 ) ;
#57859=CARTESIAN_POINT ( 'NONE',  ( -4.220049686691937474, -10.18810118749999738, 69.81250000204835260 ) ) ;
#57864=CARTESIAN_POINT ( 'NONE',  ( -11.00000000000000000, 0.000000000000000000, 97.18750000409677625 ) ) ;
#57866=FACE_OUTER_BOUND ( 'NONE', #69027, .T. ) ;
#57870=CARTESIAN_POINT ( 'NONE',  ( -11.00000000000000000, 4.556349186104045934, 109.0937500040967905 ) ) ;
#57884=ORIENTED_EDGE ( 'NONE', *, *, #41051, .F. ) ;
#57885=CARTESIAN_POINT ( 'NONE',  ( -7.778174593052023411, 7.778174593052023411, 116.3125000000000000 ) ) ;
#57891=CARTESIAN_POINT ( 'NONE',  ( -4.220049686691935698, 10.18810118749999916, 85.37500000204839523 ) ) ;
#57895=CARTESIAN_POINT ( 'NONE',  ( 4.220049686691934809, 10.18810118749999916, 117.0625000020483668 ) ) ;
#57904=CARTESIAN_POINT ( 'NONE',  ( 4.220049686691934809, 10.18810118749999916, 76.56250000204836681 ) ) ;
#57907=CARTESIAN_POINT ( 'NONE',  ( 4.556349186104052151, -10.99999999999999822, 94.65625000409680467 ) ) ;
#57912=AXIS2_PLACEMENT_3D ( 'NONE', #70670, #18987, #17881 ) ;
#57919=CARTESIAN_POINT ( 'NONE',  ( 7.204075437095966983, 7.204075437095967871, 73.09375000204838102 ) ) ;
#57932=CARTESIAN_POINT ( 'NONE',  ( -4.556349186104048599, -10.99999999999999822, 74.96875000409677625 ) ) ;
#57947=AXIS2_PLACEMENT_3D ( 'NONE', #29065, #39645, #45297 ) ;
#57961=CARTESIAN_POINT ( 'NONE',  ( 4.556349186104045934, 11.00000000000000000, 84.71875000409677625 ) ) ;
#57962=EDGE_CURVE ( 'NONE', #24773, #68143, #20622, .T. ) ;
#57979=ADVANCED_FACE ( 'NONE', ( #12066 ), #5306, .T. ) ;
#57988=CARTESIAN_POINT ( 'NONE',  ( 4.220049686691941027, -10.18810118749999738, 102.6250000020483810 ) ) ;
#58000=CARTESIAN_POINT ( 'NONE',  ( 4.556349186104045934, 11.00000000000000000, 99.71875000409677625 ) ) ;
#58005=CARTESIAN_POINT ( 'NONE',  ( 1.871523826299183495E-15, -10.18810118749999916, 93.90625000204836681 ) ) ;
#58011=CARTESIAN_POINT ( 'NONE',  ( 10.18810118749999916, 4.220049686691935698, 82.37500000204838102 ) ) ;
#58012=VECTOR ( 'NONE', #49568, 1000.000000000000000 ) ;
#58019=CARTESIAN_POINT ( 'NONE',  ( 7.204075437095968759, -7.204075437095966983, 92.21875000204838102 ) ) ;
#58027=CARTESIAN_POINT ( 'NONE',  ( 10.18810118749999916, 4.220049686691935698, 74.87500000204836681 ) ) ;
#58041=CARTESIAN_POINT ( 'NONE',  ( 7.204075437095968759, -7.204075437095966983, 71.21875000204836681 ) ) ;
#58044=CARTESIAN_POINT ( 'NONE',  ( 4.556349186104045934, 11.00000000000000000, 81.53125000000000000 ) ) ;
#58047=FACE_OUTER_BOUND ( 'NONE', #34465, .T. ) ;
#58051=CYLINDRICAL_SURFACE ( 'NONE', #61277, 11.00000000000000000 ) ;
#58065=EDGE_CURVE ( 'NONE', #72690, #6581, #36218, .T. ) ;
#58069=CARTESIAN_POINT ( 'NONE',  ( 7.778174593052023411, -7.778174593052021635, 75.06249999999997158 ) ) ;
#58072=CARTESIAN_POINT ( 'NONE',  ( -4.556349186104045934, 11.00000000000000000, 68.40625000409677625 ) ) ;
#58083=CARTESIAN_POINT ( 'NONE',  ( 7.204075437095968759, -7.204075437095966983, 113.5937500020483810 ) ) ;
#58087=CARTESIAN_POINT ( 'NONE',  ( 0.000000000000000000, 0.000000000000000000, 118.0000000000000000 ) ) ;
#58098=CARTESIAN_POINT ( 'NONE',  ( 0.000000000000000000, 0.000000000000000000, 41.99999999999999289 ) ) ;
#58111=DIRECTION ( 'NONE',  ( -1.000000000000000000, 0.000000000000000000, 0.000000000000000000 ) ) ;
#58115=ORIENTED_EDGE ( 'NONE', *, *, #38255, .F. ) ;
#58124=CARTESIAN_POINT ( 'NONE',  ( 7.204075437095968759, -7.204075437095966983, 86.21875000204836681 ) ) ;
#58127=CARTESIAN_POINT ( 'NONE',  ( -7.778174593052023411, 7.778174593052023411, 98.31250000000000000 ) ) ;
#58159=CARTESIAN_POINT ( 'NONE',  ( -6.735557395310442023E-16, 11.00000000000000000, 89.31250000409676204 ) ) ;
#58181=CARTESIAN_POINT ( 'NONE',  ( -7.778174593052023411, 7.778174593052023411, 91.00000000409677625 ) ) ;
#58183=CARTESIAN_POINT ( 'NONE',  ( 7.204075437095966983, 7.204075437095967871, 92.96875000204838102 ) ) ;
#58187=UNCERTAINTY_MEASURE_WITH_UNIT (LENGTH_MEASURE( 1.000000000000000082E-05 ), #51006, 'distance_accuracy_value', 'NONE');
#58190=CARTESIAN_POINT ( 'NONE',  ( 10.18810118750000093, -4.220049686691933921, 108.8125000020484094 ) ) ;
#58198=CARTESIAN_POINT ( 'NONE',  ( 1.871523826299183495E-15, -10.18810118749999916, 102.9062500020483810 ) ) ;
#58216=CARTESIAN_POINT ( 'NONE',  ( -10.18810118749999916, 0.000000000000000000, 103.6562500020483810 ) ) ;
#58236=CARTESIAN_POINT ( 'NONE',  ( 2.020667218593132706E-15, -11.00000000000000000, 116.8749999999999858 ) ) ;
#58242=CARTESIAN_POINT ( 'NONE',  ( 11.00000000000000000, 1.347111479062088405E-15, 97.93750000409677625 ) ) ;
#58247=CARTESIAN_POINT ( 'NONE',  ( 4.556349186104045934, 11.00000000000000000, 108.7187500040967763 ) ) ;
#58258=EDGE_LOOP ( 'NONE', ( #38212, #32028, #45221, #69606 ) ) ;
#58266=CARTESIAN_POINT ( 'NONE',  ( -10.18810118749999738, -4.220049686691941915, 85.75000000204838102 ) ) ;
#58270=CARTESIAN_POINT ( 'NONE',  ( -4.220049686691935698, 10.18810118749999916, 112.7500000020483810 ) ) ;
#58272=DIRECTION ( 'NONE',  ( 0.7071067811865401342, 8.659560562354842879E-17, -0.7071067811865549002 ) ) ;
#58277=CARTESIAN_POINT ( 'NONE',  ( -10.18810118749999916, 4.220049686691934809, 75.43750000204836681 ) ) ;
#58280=CARTESIAN_POINT ( 'NONE',  ( 11.00000000000000355, -4.556349186104044158, 94.84375000409677625 ) ) ;
#58288=APPLICATION_CONTEXT ( 'automotive_design' ) ;
#58289=CARTESIAN_POINT ( 'NONE',  ( -4.220049686691937474, -10.18810118749999738, 70.93750000204838102 ) ) ;
#58294=EDGE_CURVE ( 'NONE', #13320, #2612, #38525, .T. ) ;
#58299=CARTESIAN_POINT ( 'NONE',  ( 4.556349186104045934, 11.00000000000000000, 93.71875000409676204 ) ) ;
#58326=CARTESIAN_POINT ( 'NONE',  ( -11.00000000000000000, 0.000000000000000000, 107.4999999999999858 ) ) ;
#58352=CARTESIAN_POINT ( 'NONE',  ( -10.46351411367761486, 2.360032084838133759, 117.7839813612980038 ) ) ;
#58353=CARTESIAN_POINT ( 'NONE',  ( 7.204075437095966983, 7.204075437095967871, 100.0937500020483668 ) ) ;
#58369=CARTESIAN_POINT ( 'NONE',  ( 1.871523826299183495E-15, -10.18810118749999916, 96.90625000204838102 ) ) ;
#58372=CARTESIAN_POINT ( 'NONE',  ( 0.000000000000000000, 0.000000000000000000, 41.99999999999999289 ) ) ;
#58375=CARTESIAN_POINT ( 'NONE',  ( -4.220049686691937474, -10.18810118749999738, 81.81250000204838102 ) ) ;
#58381=CARTESIAN_POINT ( 'NONE',  ( 11.00000000000000000, 1.347111479062088405E-15, 88.93750000409677625 ) ) ;
#58383=CARTESIAN_POINT ( 'NONE',  ( -6.238412754330611322E-16, 10.18810118749999916, 91.28125000204836681 ) ) ;
#58392=CARTESIAN_POINT ( 'NONE',  ( 10.18810118750000093, -4.220049686691933921, 73.18750000204838102 ) ) ;
#58396=CARTESIAN_POINT ( 'NONE',  ( -7.778174593052020747, -7.778174593052023411, 112.1875000000000000 ) ) ;
#58408=CARTESIAN_POINT ( 'NONE',  ( 10.18810118750000093, -4.220049686691933033, 71.31250000204836681 ) ) ;
#58411=CARTESIAN_POINT ( 'NONE',  ( 4.556349186104051263, -10.99999999999999822, 85.46874999999998579 ) ) ;
#58414=DIRECTION ( 'NONE',  ( -0.000000000000000000, -0.000000000000000000, -1.000000000000000000 ) ) ;
#58435=CARTESIAN_POINT ( 'NONE',  ( 11.00000000000000355, -4.556349186104045046, 70.84375000409676204 ) ) ;
#58447=( BOUNDED_CURVE ( )  B_SPLINE_CURVE ( 2, ( #60137, #3935, #43912, #66922, #15227, #38259, #72957, #21263, #150 ),
 .UNSPECIFIED., .F., .F. ) 
 B_SPLINE_CURVE_WITH_KNOTS ( ( 3, 2, 2, 2, 3 ),
 ( 0.7794117647058823595, 0.7830882352941176405, 0.7867647058823529216, 0.7904411764705882026, 0.7941176470588234837 ),
 .UNSPECIFIED. ) 
 CURVE ( )  GEOMETRIC_REPRESENTATION_ITEM ( )  RATIONAL_B_SPLINE_CURVE ( ( 1.000000000000000000, 0.9238795325112867385, 1.000000000000000000, 0.9238795325112867385, 1.000000000000000000, 0.9238795325112867385, 1.000000000000000000, 0.9238795325112867385, 1.000000000000000000 ) ) 
 REPRESENTATION_ITEM ( '' )  );
#58448=CARTESIAN_POINT ( 'NONE',  ( -4.220049686691937474, -10.18810118749999738, 110.3125000020483810 ) ) ;
#58474=VERTEX_POINT ( 'NONE', #70263 ) ;
#58478=CARTESIAN_POINT ( 'NONE',  ( -11.00000000000000000, 0.000000000000000000, 98.49999999999998579 ) ) ;
#58482=CIRCLE ( 'NONE', #4257, 34.85072926314708752 ) ;
#58486=CARTESIAN_POINT ( 'NONE',  ( -7.204075437095965206, -7.204075437095968759, 88.84375000204838102 ) ) ;
#58489=CARTESIAN_POINT ( 'NONE',  ( 4.556349186104045934, 11.00000000000000000, 99.53125000000001421 ) ) ;
#58513=CARTESIAN_POINT ( 'NONE',  ( -6.735557395310442023E-16, 11.00000000000000000, 99.62499999999998579 ) ) ;
#58518=CARTESIAN_POINT ( 'NONE',  ( -4.556349186104045934, 11.00000000000000000, 86.40625000409677625 ) ) ;
#58521=CARTESIAN_POINT ( 'NONE',  ( 7.778174593052021635, 7.778174593052023411, 100.9374999999999858 ) ) ;
#58530=ORIENTED_EDGE ( 'NONE', *, *, #65207, .F. ) ;
#58539=( BOUNDED_CURVE ( )  B_SPLINE_CURVE ( 2, ( #20889, #8454, #15597, #43152, #38636, #31474, #72955, #61260, #54498 ),
 .UNSPECIFIED., .F., .F. ) 
 B_SPLINE_CURVE_WITH_KNOTS ( ( 3, 2, 2, 2, 3 ),
 ( 0.5588235294117644969, 0.5624999999999997780, 0.5661764705882350590, 0.5698529411764704511, 0.5735294117647057321 ),
 .UNSPECIFIED. ) 
 CURVE ( )  GEOMETRIC_REPRESENTATION_ITEM ( )  RATIONAL_B_SPLINE_CURVE ( ( 1.000000000000004663, 0.9238795325112821866, 1.000000000000000000, 0.9238795325112867385, 1.000000000000000000, 0.9238795325112867385, 1.000000000000000000, 0.9238795325112890700, 0.9999999999999976685 ) ) 
 REPRESENTATION_ITEM ( '' )  );
#58543=CARTESIAN_POINT ( 'NONE',  ( -10.18810118749999916, 4.220049686691934809, 93.43750000204836681 ) ) ;
#58551=CARTESIAN_POINT ( 'NONE',  ( -6.238412754330611322E-16, 10.18810118749999916, 104.7812500020483810 ) ) ;
#58553=ORIENTED_EDGE ( 'NONE', *, *, #49490, .T. ) ;
#58561=CARTESIAN_POINT ( 'NONE',  ( 1.871523826299183495E-15, -10.18810118749999916, 101.4062500020483810 ) ) ;
#58570=DIRECTION ( 'NONE',  ( -0.000000000000000000, -0.000000000000000000, -1.000000000000000000 ) ) ;
#58573=VERTEX_POINT ( 'NONE', #58950 ) ;
#58574=CARTESIAN_POINT ( 'NONE',  ( -4.220049686691937474, -10.18810118749999738, 106.9375000020483810 ) ) ;
#58593=CARTESIAN_POINT ( 'NONE',  ( -7.204075437095967871, 7.204075437095967871, 67.84375000204836681 ) ) ;
#58604=CARTESIAN_POINT ( 'NONE',  ( 11.00000000000000000, 1.347111479062088405E-15, 106.9375000040967763 ) ) ;
#58609=CARTESIAN_POINT ( 'NONE',  ( 7.778174593052023411, -7.778174593052021635, 108.2500000040967763 ) ) ;
#58616=CYLINDRICAL_SURFACE ( 'NONE', #32587, 11.00000000000000000 ) ;
#58620=ORIENTED_EDGE ( 'NONE', *, *, #71991, .T. ) ;
#58625=CARTESIAN_POINT ( 'NONE',  ( -4.220049686691937474, -10.18810118749999738, 85.93750000204839523 ) ) ;
#58628=CARTESIAN_POINT ( 'NONE',  ( 1.871523826299183495E-15, -10.18810118749999916, 111.9062500020483810 ) ) ;
#58635=CARTESIAN_POINT ( 'NONE',  ( -10.18810118749999738, -4.220049686691941915, 75.62500000204838102 ) ) ;
#58648=CARTESIAN_POINT ( 'NONE',  ( 7.204075437095968759, -7.204075437095966983, 69.71875000204836681 ) ) ;
#58685=CARTESIAN_POINT ( 'NONE',  ( -7.778174593052020747, -7.778174593052023411, 68.87500000409677625 ) ) ;
#58693=EDGE_LOOP ( 'NONE', ( #38613, #60432, #5034, #20433, #2177 ) ) ;
#58701=CARTESIAN_POINT ( 'NONE',  ( 11.00000000000000000, 1.347111479062088405E-15, 85.75000000000000000 ) ) ;
#58708=CARTESIAN_POINT ( 'NONE',  ( 2.020667218593132706E-15, -11.00000000000000000, 115.3749999999999858 ) ) ;
#58711=ORIENTED_EDGE ( 'NONE', *, *, #24212, .T. ) ;
#58714=CARTESIAN_POINT ( 'NONE',  ( 10.18810118750000093, -4.220049686691933921, 99.81250000204838102 ) ) ;
#58731=CARTESIAN_POINT ( 'NONE',  ( 1.871523826299183495E-15, -10.18810118749999916, 92.40625000204836681 ) ) ;
#58737=CARTESIAN_POINT ( 'NONE',  ( 1.871523826299183495E-15, -10.18810118749999916, 78.90625000204836681 ) ) ;
#58746=CARTESIAN_POINT ( 'NONE',  ( 10.18810118749999916, 4.220049686691935698, 89.50000000204836681 ) ) ;
#58755=CARTESIAN_POINT ( 'NONE',  ( -10.18810118749999916, 4.220049686691934809, 72.43750000204838102 ) ) ;
#58774=CARTESIAN_POINT ( 'NONE',  ( -10.18810118749999738, -4.220049686691941915, 67.75000000204836681 ) ) ;
#58777=CARTESIAN_POINT ( 'NONE',  ( 2.020667218593132706E-15, -11.00000000000000000, 76.37499999999998579 ) ) ;
#58802=CARTESIAN_POINT ( 'NONE',  ( -4.220049686691935698, 10.18810118749999916, 116.8750000020483668 ) ) ;
#58815=CARTESIAN_POINT ( 'NONE',  ( 10.18810118750000093, -4.220049686691933033, 112.1875000020483810 ) ) ;
#58832=ORIENTED_EDGE ( 'NONE', *, *, #1749, .F. ) ;
#58845=CARTESIAN_POINT ( 'NONE',  ( 7.778174593052023411, -7.778174593052021635, 99.06250000000000000 ) ) ;
#58854=CARTESIAN_POINT ( 'NONE',  ( -6.238412754330611322E-16, 10.18810118749999916, 83.78125000204836681 ) ) ;
#58856=CARTESIAN_POINT ( 'NONE',  ( 2.020667218593132706E-15, -11.00000000000000000, 101.8750000000000000 ) ) ;
#58857=DIRECTION ( 'NONE',  ( -0.000000000000000000, -0.000000000000000000, -1.000000000000000000 ) ) ;
#58889=CARTESIAN_POINT ( 'NONE',  ( -10.99999999999999822, -4.556349186104052151, 83.78125000409679046 ) ) ;
#58912=CYLINDRICAL_SURFACE ( 'NONE', #28553, 11.00000000000000000 ) ;
#58914=CARTESIAN_POINT ( 'NONE',  ( 4.220049686691941027, -10.18810118749999738, 89.50000000204836681 ) ) ;
#58922=CARTESIAN_POINT ( 'NONE',  ( 1.871523826299183495E-15, -10.18810118749999916, 101.0312500020483810 ) ) ;
#58931=CARTESIAN_POINT ( 'NONE',  ( 10.18810118749999916, 4.220049686691935698, 97.37500000204839523 ) ) ;
#58937=CARTESIAN_POINT ( 'NONE',  ( -11.00000000000000000, 0.000000000000000000, 80.49999999999998579 ) ) ;
#58942=CARTESIAN_POINT ( 'NONE',  ( -6.735557395310442023E-16, 11.00000000000000000, 68.12499999999998579 ) ) ;
#58946=CARTESIAN_POINT ( 'NONE',  ( -4.220049686691935698, 10.18810118749999916, 106.3750000020483668 ) ) ;
#58950=CARTESIAN_POINT ( 'NONE',  ( -11.00000000000000000, 0.000000000000000000, 67.18750000409676204 ) ) ;
#58955=ADVANCED_FACE ( 'NONE', ( #68311 ), #57004, .T. ) ;
#58956=CARTESIAN_POINT ( 'NONE',  ( -7.778174593052023411, 7.778174593052023411, 74.31249999999998579 ) ) ;
#58964=CARTESIAN_POINT ( 'NONE',  ( 7.204075437095968759, -7.204075437095966983, 70.09375000204836681 ) ) ;
#58976=CARTESIAN_POINT ( 'NONE',  ( -7.778174593052020747, -7.778174593052023411, 106.3750000040967763 ) ) ;
#58979=CARTESIAN_POINT ( 'NONE',  ( 4.556349186104045934, 11.00000000000000000, 71.03124999999998579 ) ) ;
#58980=CARTESIAN_POINT ( 'NONE',  ( 11.00000000000000000, 4.556349186104045934, 71.03125000409676204 ) ) ;
#58995=DIRECTION ( 'NONE',  ( -0.000000000000000000, -0.000000000000000000, -1.000000000000000000 ) ) ;
#59001=CARTESIAN_POINT ( 'NONE',  ( -10.18810118749999916, 0.000000000000000000, 111.5312500020483668 ) ) ;
#59009=CARTESIAN_POINT ( 'NONE',  ( -10.18810118749999916, 0.000000000000000000, 69.53125000204838102 ) ) ;
#59020=CARTESIAN_POINT ( 'NONE',  ( -10.18810118749999738, -4.220049686691941915, 73.75000000204836681 ) ) ;
#59075=CARTESIAN_POINT ( 'NONE',  ( -6.735557395310442023E-16, 11.00000000000000000, 101.3125000040967763 ) ) ;
#59085=CARTESIAN_POINT ( 'NONE',  ( 10.18810118749999916, 1.247682550866122264E-15, 99.90625000204838102 ) ) ;
#59094=ORIENTED_EDGE ( 'NONE', *, *, #65254, .F. ) ;
#59102=CARTESIAN_POINT ( 'NONE',  ( 10.18810118749999916, 4.220049686691935698, 92.87500000204838102 ) ) ;
#59107=CARTESIAN_POINT ( 'NONE',  ( -7.778174593052023411, 7.778174593052023411, 102.8124999999999858 ) ) ;
#59108=CARTESIAN_POINT ( 'NONE',  ( -6.238412754330611322E-16, 10.18810118749999916, 72.15625000204836681 ) ) ;
#59114=CARTESIAN_POINT ( 'NONE',  ( -10.18810118749999916, 4.220049686691934809, 90.06250000204838102 ) ) ;
#59125=CARTESIAN_POINT ( 'NONE',  ( 7.204075437095968759, -7.204075437095966983, 77.59375000204838102 ) ) ;
#59129=EDGE_CURVE ( 'NONE', #30692, #41579, #24581, .T. ) ;
#59144=CARTESIAN_POINT ( 'NONE',  ( -10.18810118749999916, 0.000000000000000000, 67.65625000204836681 ) ) ;
#59147=CARTESIAN_POINT ( 'NONE',  ( 4.556349186104045934, 11.00000000000000000, 75.53124999999998579 ) ) ;
#59161=CARTESIAN_POINT ( 'NONE',  ( 7.778174593052023411, -7.778174593052021635, 70.56249999999998579 ) ) ;
#59174=CARTESIAN_POINT ( 'NONE',  ( -4.556349186104045934, 11.00000000000000000, 71.40625000409677625 ) ) ;
#59179=EDGE_CURVE ( 'NONE', #29602, #72546, #30174, .T. ) ;
#59185=CARTESIAN_POINT ( 'NONE',  ( -10.18810118749999916, 4.220049686691934809, 111.4375000020483810 ) ) ;
#59196=AXIS2_PLACEMENT_3D ( 'NONE', #10646, #63068, #16654 ) ;
#59205=( BOUNDED_CURVE ( )  B_SPLINE_CURVE ( 2, ( #48613, #31270, #61063, #2610, #71619, #20692, #71995, #42950, #70893 ),
 .UNSPECIFIED., .F., .F. ) 
 B_SPLINE_CURVE_WITH_KNOTS ( ( 3, 2, 2, 2, 3 ),
 ( 0.6764705882352940458, 0.6801470588235293269, 0.6838235294117647189, 0.6875000000000000000, 0.6911764705882352811 ),
 .UNSPECIFIED. ) 
 CURVE ( )  GEOMETRIC_REPRESENTATION_ITEM ( )  RATIONAL_B_SPLINE_CURVE ( ( 1.000000000000002220, 0.9238795325112844070, 1.000000000000000000, 0.9238795325112867385, 1.000000000000000000, 0.9238795325112867385, 1.000000000000000000, 0.9238795325112867385, 1.000000000000000000 ) ) 
 REPRESENTATION_ITEM ( '' )  );
#59223=CARTESIAN_POINT ( 'NONE',  ( 1.871523826299183495E-15, -10.18810118749999916, 87.53125000204836681 ) ) ;
#59225=CARTESIAN_POINT ( 'NONE',  ( 4.556349186104045934, 11.00000000000000000, 93.53125000000000000 ) ) ;
#59250=CARTESIAN_POINT ( 'NONE',  ( 11.00000000000000000, 1.347111479062088405E-15, 118.0000000000000000 ) ) ;
#59255=CARTESIAN_POINT ( 'NONE',  ( 4.556349186104045934, 11.00000000000000000, 86.21875000409680467 ) ) ;
#59258=CARTESIAN_POINT ( 'NONE',  ( -4.556349186104045934, 11.00000000000000000, 101.2187500000000000 ) ) ;
#59277=AXIS2_PLACEMENT_3D ( 'NONE', #13660, #59712, #64985 ) ;
#59280=CARTESIAN_POINT ( 'NONE',  ( 1.871523826299183495E-15, -10.18810118749999916, 90.90625000204838102 ) ) ;
#59286=CARTESIAN_POINT ( 'NONE',  ( 7.204075437095966983, 7.204075437095967871, 101.5937500020483668 ) ) ;
#59288=ORIENTED_EDGE ( 'NONE', *, *, #123, .T. ) ;
#59293=CARTESIAN_POINT ( 'NONE',  ( -11.00000000000000000, 0.000000000000000000, 96.99999999999998579 ) ) ;
#59294=CARTESIAN_POINT ( 'NONE',  ( -7.204075437095965206, -7.204075437095968759, 99.71875000204838102 ) ) ;
#59303=EDGE_CURVE ( 'NONE', #49304, #12752, #41994, .T. ) ;
#59308=CARTESIAN_POINT ( 'NONE',  ( -11.00000000000000000, 0.000000000000000000, 68.49999999999997158 ) ) ;
#59310=ORIENTED_EDGE ( 'NONE', *, *, #6221, .T. ) ;
#59312=( BOUNDED_CURVE ( )  B_SPLINE_CURVE ( 2, ( #33942, #23711, #58069, #6001, #39952, #62577, #29002, #23339, #10909 ),
 .UNSPECIFIED., .F., .F. ) 
 B_SPLINE_CURVE_WITH_KNOTS ( ( 3, 2, 2, 2, 3 ),
 ( 0.8382352941176471894, 0.8419117647058824705, 0.8455882352941177516, 0.8492647058823530326, 0.8529411764705883137 ),
 .UNSPECIFIED. ) 
 CURVE ( )  GEOMETRIC_REPRESENTATION_ITEM ( )  RATIONAL_B_SPLINE_CURVE ( ( 0.9999999999999976685, 0.9238795325112890700, 1.000000000000000000, 0.9238795325112867385, 1.000000000000000000, 0.9238795325112867385, 1.000000000000000000, 0.9238795325112844070, 1.000000000000002220 ) ) 
 REPRESENTATION_ITEM ( '' )  );
#59315=CARTESIAN_POINT ( 'NONE',  ( 4.220049686691941027, -10.18810118749999738, 102.6250000020483810 ) ) ;
#59323=ORIENTED_EDGE ( 'NONE', *, *, #21984, .F. ) ;
#59330=CARTESIAN_POINT ( 'NONE',  ( -4.556349186104045934, 11.00000000000000000, 113.2187499999999858 ) ) ;
#59341=CARTESIAN_POINT ( 'NONE',  ( 4.556349186104045934, 11.00000000000000000, 102.7187500040967620 ) ) ;
#59363=CARTESIAN_POINT ( 'NONE',  ( -10.18810118749999916, 4.220049686691934809, 109.9375000020483952 ) ) ;
#59371=CARTESIAN_POINT ( 'NONE',  ( 7.204075437095966983, 7.204075437095967871, 71.96875000204836681 ) ) ;
#59373=EDGE_LOOP ( 'NONE', ( #21250, #19274, #44801 ) ) ;
#59383=CARTESIAN_POINT ( 'NONE',  ( -7.204075437095965206, -7.204075437095968759, 114.7187500020483810 ) ) ;
#59398=ORIENTED_EDGE ( 'NONE', *, *, #16196, .T. ) ;
#59414=CARTESIAN_POINT ( 'NONE',  ( 0.000000000000000000, 0.000000000000000000, 118.0000000000000000 ) ) ;
#59417=CARTESIAN_POINT ( 'NONE',  ( -4.556349186104048599, -10.99999999999999822, 89.78125000000000000 ) ) ;
#59420=CARTESIAN_POINT ( 'NONE',  ( -11.00000000000000000, 0.000000000000000000, 76.18750000409677625 ) ) ;
#59421=CARTESIAN_POINT ( 'NONE',  ( 11.00000000000000000, 1.347111479062088405E-15, 81.43750000409677625 ) ) ;
#59447=CARTESIAN_POINT ( 'NONE',  ( 3.748303087376534393, 10.32408853373171809, 117.5267128448309677 ) ) ;
#59448=CARTESIAN_POINT ( 'NONE',  ( -10.18810118749999916, 0.000000000000000000, 94.65625000204836681 ) ) ;
#59464=CARTESIAN_POINT ( 'NONE',  ( 4.220049686691934809, 10.18810118749999916, 91.56250000204838102 ) ) ;
#59469=CARTESIAN_POINT ( 'NONE',  ( -10.99999999999989164, -4.556349186104158733, 101.7812500040967763 ) ) ;
#59470=VECTOR ( 'NONE', #71465, 1000.000000000000000 ) ;
#59471=CARTESIAN_POINT ( 'NONE',  ( 7.204075437095966983, 7.204075437095967871, 73.46875000204838102 ) ) ;
#59479=CARTESIAN_POINT ( 'NONE',  ( 7.204075437095966983, 7.204075437095967871, 85.09375000204836681 ) ) ;
#59490=CARTESIAN_POINT ( 'NONE',  ( 10.18810118750000093, -4.220049686691933921, 68.68750000204836681 ) ) ;
#59508=CARTESIAN_POINT ( 'NONE',  ( -10.99999999999999822, -4.556349186104052151, 77.59374999999998579 ) ) ;
#59534=CARTESIAN_POINT ( 'NONE',  ( 7.204075437095966983, 7.204075437095967871, 83.96875000204836681 ) ) ;
#59535=CARTESIAN_POINT ( 'NONE',  ( 11.00000000000000000, 4.556349186104045934, 69.53125000409677625 ) ) ;
#59547=CARTESIAN_POINT ( 'NONE',  ( 1.871523826299183495E-15, -10.18810118749999916, 107.4062500020483668 ) ) ;
#59585=CARTESIAN_POINT ( 'NONE',  ( 10.18810118750000093, -4.220049686691933033, 78.81250000204838102 ) ) ;
#59587=CARTESIAN_POINT ( 'NONE',  ( -11.00000000000000000, 4.556349186104045934, 95.40624999999998579 ) ) ;
#59613=CARTESIAN_POINT ( 'NONE',  ( 7.778174593052021635, 7.778174593052023411, 104.1250000040967763 ) ) ;
#59616=CARTESIAN_POINT ( 'NONE',  ( 7.778174593052021635, 7.778174593052023411, 86.12500000409677625 ) ) ;
#59640=CARTESIAN_POINT ( 'NONE',  ( -7.204075437095965206, -7.204075437095968759, 89.21875000204838102 ) ) ;
#59646=CARTESIAN_POINT ( 'NONE',  ( -10.18810118749999738, -4.220049686691941915, 100.7500000020483526 ) ) ;
#59652=EDGE_CURVE ( 'NONE', #33983, #45292, #18870, .T. ) ;
#59656=CARTESIAN_POINT ( 'NONE',  ( -10.18810118749999916, 4.220049686691934809, 99.43750000204836681 ) ) ;
#59662=ORIENTED_EDGE ( 'NONE', *, *, #11517, .F. ) ;
#59671=CARTESIAN_POINT ( 'NONE',  ( -11.00000000000000000, 0.000000000000000000, 118.0000000000000000 ) ) ;
#59675=CARTESIAN_POINT ( 'NONE',  ( 7.204075437095968759, -7.204075437095966983, 105.7187500020483810 ) ) ;
#59693=CARTESIAN_POINT ( 'NONE',  ( 7.778174593052023411, -7.778174593052021635, 91.75000000409677625 ) ) ;
#59694=CARTESIAN_POINT ( 'NONE',  ( -10.99999999999999822, -4.556349186104052151, 110.5937499999999858 ) ) ;
#59706=CARTESIAN_POINT ( 'NONE',  ( -11.00000000000000000, 0.000000000000000000, 106.1875000040967620 ) ) ;
#59710=CARTESIAN_POINT ( 'NONE',  ( 11.00000000000000000, 1.347111479062088405E-15, 108.2499999999999858 ) ) ;
#59712=DIRECTION ( 'NONE',  ( -0.000000000000000000, -0.000000000000000000, -1.000000000000000000 ) ) ;
#59728=CARTESIAN_POINT ( 'NONE',  ( 10.18810118750000093, -4.220049686691933921, 109.1875000020483810 ) ) ;
#59731=CARTESIAN_POINT ( 'NONE',  ( -7.778174593052020747, -7.778174593052023411, 109.3750000040967763 ) ) ;
#59736=CARTESIAN_POINT ( 'NONE',  ( -7.204075437095965206, -7.204075437095968759, 68.21875000204836681 ) ) ;
#59748=CARTESIAN_POINT ( 'NONE',  ( -7.204075437095965206, -7.204075437095968759, 67.84375000204836681 ) ) ;
#59782=DIRECTION ( 'NONE',  ( -1.000000000000000000, 0.000000000000000000, 0.000000000000000000 ) ) ;
#59785=CARTESIAN_POINT ( 'NONE',  ( -11.00000000000000000, 0.000000000000000000, 68.68750000409676204 ) ) ;
#59789=LINE ( 'NONE', #3193, #39478 ) ;
#59807=CARTESIAN_POINT ( 'NONE',  ( 10.99999999999997691, -4.556349186104070803, 115.6562500000000000 ) ) ;
#59812=CARTESIAN_POINT ( 'NONE',  ( 7.204075437095966983, 7.204075437095967871, 92.59375000204838102 ) ) ;
#59826=CARTESIAN_POINT ( 'NONE',  ( -6.238412754330611322E-16, 10.18810118749999916, 91.65625000204836681 ) ) ;
#59827=ADVANCED_FACE ( 'NONE', ( #6449 ), #66365, .T. ) ;
#59833=CARTESIAN_POINT ( 'NONE',  ( 10.18810118749999916, 1.247682550866122264E-15, 76.28125000204836681 ) ) ;
#59840=CARTESIAN_POINT ( 'NONE',  ( -7.204075437095965206, -7.204075437095968759, 82.84375000204838102 ) ) ;
#59852=CARTESIAN_POINT ( 'NONE',  ( -6.238412754330611322E-16, 10.18810118749999916, 69.15625000204836681 ) ) ;
#59873=CARTESIAN_POINT ( 'NONE',  ( -4.556349186104045934, 11.00000000000000000, 77.21875000000001421 ) ) ;
#59883=CARTESIAN_POINT ( 'NONE',  ( 2.020667218593132706E-15, -11.00000000000000000, 115.5625000040967763 ) ) ;
#59892=ORIENTED_EDGE ( 'NONE', *, *, #21146, .F. ) ;
#59899=CARTESIAN_POINT ( 'NONE',  ( -6.238412754330611322E-16, 10.18810118749999916, 87.15625000204838102 ) ) ;
#59900=CARTESIAN_POINT ( 'NONE',  ( -7.204075437095965206, -7.204075437095968759, 111.3437500020483810 ) ) ;
#59906=EDGE_CURVE ( 'NONE', #1423, #68675, #32044, .T. ) ;
#59912=CARTESIAN_POINT ( 'NONE',  ( 10.18810118749999916, 4.220049686691935698, 104.8750000020483668 ) ) ;
#59940=EDGE_LOOP ( 'NONE', ( #38715, #13678, #37958, #43988 ) ) ;
#59944=( BOUNDED_CURVE ( )  B_SPLINE_CURVE ( 2, ( #7656, #64256, #30294, #35593, #53680, #71013, #6549, #19328, #42341 ),
 .UNSPECIFIED., .F., .F. ) 
 B_SPLINE_CURVE_WITH_KNOTS ( ( 3, 2, 2, 2, 3 ),
 ( 0.4117647058823528661, 0.4154411764705882026, 0.4191176470588234837, 0.4227941176470588203, 0.4264705882352941013 ),
 .UNSPECIFIED. ) 
 CURVE ( )  GEOMETRIC_REPRESENTATION_ITEM ( )  RATIONAL_B_SPLINE_CURVE ( ( 1.000000000000001110, 0.9238795325112856283, 1.000000000000000000, 0.9238795325112867385, 1.000000000000000000, 0.9238795325112867385, 1.000000000000000000, 0.9238795325112867385, 1.000000000000000000 ) ) 
 REPRESENTATION_ITEM ( '' )  );
#59946=CARTESIAN_POINT ( 'NONE',  ( -10.18810118749999916, 0.000000000000000000, 78.15625000204836681 ) ) ;
#59949=CARTESIAN_POINT ( 'NONE',  ( 4.556349186104045934, 11.00000000000000000, 98.03124999999997158 ) ) ;
#59950=CARTESIAN_POINT ( 'NONE',  ( -11.00000000000000000, 0.000000000000000000, 86.50000000000000000 ) ) ;
#59955=CARTESIAN_POINT ( 'NONE',  ( -11.00000000000000000, 0.000000000000000000, 91.00000000000000000 ) ) ;
#59976=CARTESIAN_POINT ( 'NONE',  ( 4.556349186104045934, 11.00000000000000000, 69.71875000409677625 ) ) ;
#59979=CARTESIAN_POINT ( 'NONE',  ( -4.556349186104045934, 11.00000000000000000, 83.40625000409676204 ) ) ;
#59987=VECTOR ( 'NONE', #29464, 1000.000000000000000 ) ;
#59990=ORIENTED_EDGE ( 'NONE', *, *, #57962, .F. ) ;
#59995=CARTESIAN_POINT ( 'NONE',  ( 1.871523826299183495E-15, -10.18810118749999916, 84.53125000204836681 ) ) ;
#60004=CARTESIAN_POINT ( 'NONE',  ( -6.238412754330611322E-16, 10.18810118749999916, 85.65625000204838102 ) ) ;
#60008=CARTESIAN_POINT ( 'NONE',  ( -7.204075437095965206, -7.204075437095968759, 99.34375000204836681 ) ) ;
#60016=CARTESIAN_POINT ( 'NONE',  ( 1.871523826299183495E-15, -10.18810118749999916, 96.90625000204838102 ) ) ;
#60031=CARTESIAN_POINT ( 'NONE',  ( 1.871523826299183495E-15, -10.18810118749999916, 98.03125000204838102 ) ) ;
#60048=CARTESIAN_POINT ( 'NONE',  ( -11.00000000000000000, 4.556349186104045934, 110.4062500000000000 ) ) ;
#60054=CARTESIAN_POINT ( 'NONE',  ( 11.00000000000000000, 1.347111479062088405E-15, 91.74999999999998579 ) ) ;
#60055=FACE_OUTER_BOUND ( 'NONE', #11496, .T. ) ;
#60056=PLANE ( 'NONE',  #27841 ) ;
#60061=CARTESIAN_POINT ( 'NONE',  ( 4.556349186104051263, -10.99999999999999822, 99.15625000409677625 ) ) ;
#60089=CARTESIAN_POINT ( 'NONE',  ( 7.204075437095966983, 7.204075437095967871, 107.9687500020483810 ) ) ;
#60096=CARTESIAN_POINT ( 'NONE',  ( 7.204075437095968759, -7.204075437095966983, 70.09375000204836681 ) ) ;
#60102=ORIENTED_EDGE ( 'NONE', *, *, #39301, .T. ) ;
#60108=CARTESIAN_POINT ( 'NONE',  ( 4.220049686691934809, 10.18810118749999916, 115.5625000020483810 ) ) ;
#60133=ORIENTED_EDGE ( 'NONE', *, *, #18609, .T. ) ;
#60135=CYLINDRICAL_SURFACE ( 'NONE', #53274, 11.00000000000000000 ) ;
#60137=CARTESIAN_POINT ( 'NONE',  ( 11.00000000000000000, 1.347111479062088405E-15, 78.24999999999998579 ) ) ;
#60152=CARTESIAN_POINT ( 'NONE',  ( -11.00000000000000000, 0.000000000000000000, 77.68750000409677625 ) ) ;
#60161=DIRECTION ( 'NONE',  ( -1.000000000000000000, 0.000000000000000000, 0.000000000000000000 ) ) ;
#60166=( BOUNDED_CURVE ( )  B_SPLINE_CURVE ( 2, ( #21689, #44715, #62060, #44344, #26222, #20571, #60944, #15279, #72258 ),
 .UNSPECIFIED., .F., .F. ) 
 B_SPLINE_CURVE_WITH_KNOTS ( ( 3, 2, 2, 2, 3 ),
 ( 0.6029411764705880916, 0.6066176470588233727, 0.6102941176470586537, 0.6139705882352939348, 0.6176470588235292158 ),
 .UNSPECIFIED. ) 
 CURVE ( )  GEOMETRIC_REPRESENTATION_ITEM ( )  RATIONAL_B_SPLINE_CURVE ( ( 1.000000000000002220, 0.9238795325112844070, 1.000000000000000000, 0.9238795325112867385, 1.000000000000000000, 0.9238795325112867385, 1.000000000000000000, 0.9238795325112912904, 0.9999999999999954481 ) ) 
 REPRESENTATION_ITEM ( '' )  );
#60172=CARTESIAN_POINT ( 'NONE',  ( -0.4325856884189893115, 10.91672922346751839, 117.5849391215780457 ) ) ;
#60173=CARTESIAN_POINT ( 'NONE',  ( -4.220049686691935698, 10.18810118749999916, 95.87500000204838102 ) ) ;
#60186=CARTESIAN_POINT ( 'NONE',  ( 4.220049686691941027, -10.18810118749999738, 91.00000000204836681 ) ) ;
#60193=CARTESIAN_POINT ( 'NONE',  ( -10.18810118749999738, -4.220049686691941915, 72.62500000204836681 ) ) ;
#60199=CARTESIAN_POINT ( 'NONE',  ( -10.18810118749999916, 4.220049686691934809, 84.06250000204838102 ) ) ;
#60211=ORIENTED_EDGE ( 'NONE', *, *, #8384, .T. ) ;
#60214=EDGE_CURVE ( 'NONE', #29969, #8618, #34324, .T. ) ;
#60222=ORIENTED_EDGE ( 'NONE', *, *, #5591, .F. ) ;
#60230=CARTESIAN_POINT ( 'NONE',  ( -6.735557395310442023E-16, 11.00000000000000000, 114.6249999999999858 ) ) ;
#60234=CARTESIAN_POINT ( 'NONE',  ( -11.00000000000000000, 4.556349186104045934, 74.40624999999998579 ) ) ;
#60243=CARTESIAN_POINT ( 'NONE',  ( 11.00000000000000000, 4.556349186104045934, 114.5312500040968047 ) ) ;
#60259=CARTESIAN_POINT ( 'NONE',  ( 4.220049686691941027, -10.18810118749999738, 86.50000000204838102 ) ) ;
#60260=CARTESIAN_POINT ( 'NONE',  ( -4.220049686691937474, -10.18810118749999738, 111.4375000020483810 ) ) ;
#60273=CARTESIAN_POINT ( 'NONE',  ( 4.220049686691934809, 10.18810118749999916, 106.5625000020483810 ) ) ;
#60300=CARTESIAN_POINT ( 'NONE',  ( -7.778174593052023411, 7.778174593052023411, 72.81249999999998579 ) ) ;
#60302=ADVANCED_FACE ( 'NONE', ( #39940 ), #13738, .T. ) ;
#60313=CARTESIAN_POINT ( 'NONE',  ( 7.204075437095966983, 7.204075437095967871, 82.09375000204838102 ) ) ;
#60316=CARTESIAN_POINT ( 'NONE',  ( 4.556349186104051263, -10.99999999999999822, 97.46874999999998579 ) ) ;
#60321=CARTESIAN_POINT ( 'NONE',  ( 4.556349186104052151, -10.99999999999999822, 83.96874999999997158 ) ) ;
#60333=CARTESIAN_POINT ( 'NONE',  ( -11.00000000000003730, -4.556349186104013960, 112.2812500040967905 ) ) ;
#60344=CARTESIAN_POINT ( 'NONE',  ( 4.556349186104045934, 11.00000000000000000, 81.71875000409677625 ) ) ;
#60362=FACE_OUTER_BOUND ( 'NONE', #58258, .T. ) ;
#60363=CARTESIAN_POINT ( 'NONE',  ( -4.220049686691935698, 10.18810118749999916, 74.87500000204836681 ) ) ;
#60372=CARTESIAN_POINT ( 'NONE',  ( 10.18810118749999916, 4.220049686691935698, 88.37500000204839523 ) ) ;
#60377=CARTESIAN_POINT ( 'NONE',  ( -7.204075437095965206, -7.204075437095968759, 102.3437500020483668 ) ) ;
#60385=CARTESIAN_POINT ( 'NONE',  ( -10.18810118749999916, 4.220049686691934809, 96.43750000204836681 ) ) ;
#60396=VECTOR ( 'NONE', #13672, 1000.000000000000000 ) ;
#60404=CARTESIAN_POINT ( 'NONE',  ( -7.204075437095967871, 7.204075437095967871, 100.4687500020483668 ) ) ;
#60417=ORIENTED_EDGE ( 'NONE', *, *, #25834, .F. ) ;
#60425=CARTESIAN_POINT ( 'NONE',  ( 7.778174593052021635, 7.778174593052023411, 115.9375000000000000 ) ) ;
#60431=CARTESIAN_POINT ( 'NONE',  ( 11.00000000000000000, 1.347111479062088405E-15, 114.4375000040967763 ) ) ;
#60432=ORIENTED_EDGE ( 'NONE', *, *, #37, .F. ) ;
#60435=CARTESIAN_POINT ( 'NONE',  ( -4.556349186104045934, 11.00000000000000000, 99.90625000409677625 ) ) ;
#60448=ORIENTED_EDGE ( 'NONE', *, *, #24136, .T. ) ;
#60452=DIRECTION ( 'NONE',  ( -1.000000000000000000, 0.000000000000000000, 0.000000000000000000 ) ) ;
#60458=CARTESIAN_POINT ( 'NONE',  ( -4.220049686691937474, -10.18810118749999738, 102.8125000020483952 ) ) ;
#60466=CARTESIAN_POINT ( 'NONE',  ( -10.18810118749999738, -4.220049686691941915, 69.62500000204836681 ) ) ;
#60469=CARTESIAN_POINT ( 'NONE',  ( 4.220049686691934809, 10.18810118749999916, 116.6875000020483952 ) ) ;
#60476=DIRECTION ( 'NONE',  ( -0.000000000000000000, -0.000000000000000000, -1.000000000000000000 ) ) ;
#60479=CARTESIAN_POINT ( 'NONE',  ( -6.238412754330611322E-16, 10.18810118749999916, 115.6562500020483810 ) ) ;
#60482=VERTEX_POINT ( 'NONE', #69356 ) ;
#60483=CIRCLE ( 'NONE', #5107, 11.00000000000000000 ) ;
#60515=CYLINDRICAL_SURFACE ( 'NONE', #71609, 11.00000000000000000 ) ;
#60525=DIRECTION ( 'NONE',  ( 1.000000000000000000, 1.991032627040250683E-16, 0.000000000000000000 ) ) ;
#60548=CARTESIAN_POINT ( 'NONE',  ( -4.220049686691937474, -10.18810118749999738, 94.93750000204838102 ) ) ;
#60562=CARTESIAN_POINT ( 'NONE',  ( -4.220049686691937474, -10.18810118749999738, 87.81250000204838102 ) ) ;
#60577=CARTESIAN_POINT ( 'NONE',  ( 4.220049686691934809, 10.18810118749999916, 83.68750000204836681 ) ) ;
#60611=CARTESIAN_POINT ( 'NONE',  ( 7.778174593052021635, 7.778174593052023411, 73.93749999999998579 ) ) ;
#60620=CARTESIAN_POINT ( 'NONE',  ( -6.735557395310442023E-16, 11.00000000000000000, 116.3125000040967763 ) ) ;
#60624=VECTOR ( 'NONE', #7397, 1000.000000000000000 ) ;
#60633=( BOUNDED_CURVE ( )  B_SPLINE_CURVE ( 2, ( #18405, #5609, #28607, #41420, #64432, #24784, #2162, #30466, #53483 ),
 .UNSPECIFIED., .F., .F. ) 
 B_SPLINE_CURVE_WITH_KNOTS ( ( 3, 2, 2, 2, 3 ),
 ( 0.07352941176470594031, 0.07720588235294123525, 0.08088235294117653018, 0.08455882352941182512, 0.08823529411764712005 ),
 .UNSPECIFIED. ) 
 CURVE ( )  GEOMETRIC_REPRESENTATION_ITEM ( )  RATIONAL_B_SPLINE_CURVE ( ( 0.9999999999999988898, 0.9238795325112878487, 1.000000000000000000, 0.9238795325112867385, 1.000000000000000000, 0.9238795325112867385, 1.000000000000000000, 0.9238795325112856283, 1.000000000000001110 ) ) 
 REPRESENTATION_ITEM ( '' )  );
#60634=CARTESIAN_POINT ( 'NONE',  ( -11.00000000000010658, 4.556349186103942017, 81.90625000000000000 ) ) ;
#60640=CARTESIAN_POINT ( 'NONE',  ( 4.220049686691941027, -10.18810118749999738, 85.00000000204838102 ) ) ;
#60641=CARTESIAN_POINT ( 'NONE',  ( -7.204075437095965206, -7.204075437095968759, 115.8437500020483810 ) ) ;
#60651=CYLINDRICAL_SURFACE ( 'NONE', #1501, 11.00000000000000000 ) ;
#60654=CARTESIAN_POINT ( 'NONE',  ( -4.220049686691937474, -10.18810118749999738, 104.3125000020483810 ) ) ;
#60666=VERTEX_POINT ( 'NONE', #72973 ) ;
#60667=EDGE_CURVE ( 'NONE', #1009, #67207, #37153, .T. ) ;
#60695=CARTESIAN_POINT ( 'NONE',  ( 10.18810118749999916, 1.247682550866122264E-15, 83.40625000204838102 ) ) ;
#60698=CARTESIAN_POINT ( 'NONE',  ( 7.778174593052023411, -7.778174593052021635, 94.56250000000000000 ) ) ;
#60714=CARTESIAN_POINT ( 'NONE',  ( 2.020667218593132706E-15, -11.00000000000000000, 112.5625000040967763 ) ) ;
#60723=CARTESIAN_POINT ( 'NONE',  ( -4.556349186104045934, 11.00000000000000000, 69.90625000409674783 ) ) ;
#60725=CARTESIAN_POINT ( 'NONE',  ( -10.99999999999999822, -4.556349186104052151, 80.78125000409680467 ) ) ;
#60744=CARTESIAN_POINT ( 'NONE',  ( -10.18810118749999738, -4.220049686691941915, 79.75000000204838102 ) ) ;
#60752=CARTESIAN_POINT ( 'NONE',  ( -7.204075437095965206, -7.204075437095968759, 87.71875000204836681 ) ) ;
#60753=ORIENTED_EDGE ( 'NONE', *, *, #41331, .F. ) ;
#60758=CARTESIAN_POINT ( 'NONE',  ( -7.204075437095967871, 7.204075437095967871, 97.46875000204838102 ) ) ;
#60761=ORIENTED_EDGE ( 'NONE', *, *, #43625, .T. ) ;
#60766=CARTESIAN_POINT ( 'NONE',  ( -4.220049686691937474, -10.18810118749999738, 93.81250000204839523 ) ) ;
#60781=CARTESIAN_POINT ( 'NONE',  ( -10.18810118749999916, 4.220049686691934809, 100.5625000020483668 ) ) ;
#60792=DIRECTION ( 'NONE',  ( -1.000000000000000000, 0.000000000000000000, 0.000000000000000000 ) ) ;
#60799=CARTESIAN_POINT ( 'NONE',  ( -7.778174593052020747, -7.778174593052023411, 115.1875000000000000 ) ) ;
#60812=CARTESIAN_POINT ( 'NONE',  ( 11.00000000000000000, 4.556349186104045934, 98.03125000409677625 ) ) ;
#60821=EDGE_CURVE ( 'NONE', #40560, #10364, #14444, .T. ) ;
#60835=CARTESIAN_POINT ( 'NONE',  ( -11.00000000000000000, 0.000000000000000000, 70.18750000409676204 ) ) ;
#60837=CARTESIAN_POINT ( 'NONE',  ( 10.18810118749999916, 4.220049686691935698, 101.8750000020483810 ) ) ;
#60849=CARTESIAN_POINT ( 'NONE',  ( -10.18810118749999738, -4.220049686691941915, 115.7500000020483668 ) ) ;
#60857=CARTESIAN_POINT ( 'NONE',  ( -10.18810118749999738, -4.220049686691941915, 113.1250000020483810 ) ) ;
#60860=ORIENTED_EDGE ( 'NONE', *, *, #61705, .F. ) ;
#60871=CARTESIAN_POINT ( 'NONE',  ( -10.99999999999978684, -4.556349186104264426, 83.78125000409680467 ) ) ;
#60886=LINE ( 'NONE', #37135, #15299 ) ;
#60891=CARTESIAN_POINT ( 'NONE',  ( 11.00000000000000000, 1.347111479062088405E-15, 105.4375000040967763 ) ) ;
#60919=ORIENTED_EDGE ( 'NONE', *, *, #9377, .F. ) ;
#60922=EDGE_CURVE ( 'NONE', #62018, #43963, #3392, .T. ) ;
#60923=CARTESIAN_POINT ( 'NONE',  ( -7.204075437095965206, -7.204075437095968759, 93.34375000204838102 ) ) ;
#60929=CARTESIAN_POINT ( 'NONE',  ( 2.020667218593132706E-15, -11.00000000000000000, 95.87499999999998579 ) ) ;
#60931=CARTESIAN_POINT ( 'NONE',  ( 4.556349186104045934, 11.00000000000000000, 77.03125000000000000 ) ) ;
#60936=CARTESIAN_POINT ( 'NONE',  ( -4.220049686691937474, -10.18810118749999738, 86.31250000204838102 ) ) ;
#60944=CARTESIAN_POINT ( 'NONE',  ( -7.778174593052020747, -7.778174593052023411, 85.37500000409677625 ) ) ;
#60947=AXIS2_PLACEMENT_3D ( 'NONE', #26125, #20467, #2023 ) ;
#60953=CARTESIAN_POINT ( 'NONE',  ( 10.18810118749999916, 1.247682550866122264E-15, 86.40625000204838102 ) ) ;
#60985=CARTESIAN_POINT ( 'NONE',  ( 11.00000000000000000, 1.347111479062088405E-15, 72.24999999999998579 ) ) ;
#60994=FACE_OUTER_BOUND ( 'NONE', #26952, .T. ) ;
#61009=ORIENTED_EDGE ( 'NONE', *, *, #38502, .F. ) ;
#61012=CARTESIAN_POINT ( 'NONE',  ( 10.18810118749999916, 1.247682550866122264E-15, 113.4062500020483810 ) ) ;
#61027=CARTESIAN_POINT ( 'NONE',  ( 10.18810118749999916, 4.220049686691935698, 106.3750000020483668 ) ) ;
#61063=CARTESIAN_POINT ( 'NONE',  ( -7.778174593052023411, 7.778174593052023411, 83.31249999999998579 ) ) ;
#61068=CARTESIAN_POINT ( 'NONE',  ( -7.204075437095965206, -7.204075437095968759, 79.84375000204838102 ) ) ;
#61071=CARTESIAN_POINT ( 'NONE',  ( -11.00000000000000000, 4.556349186104045934, 87.90624999999998579 ) ) ;
#61072=CARTESIAN_POINT ( 'NONE',  ( -11.00000000000000000, 0.000000000000000000, 104.5000000000000000 ) ) ;
#61075=CARTESIAN_POINT ( 'NONE',  ( -7.778174593052023411, 7.778174593052023411, 89.31249999999998579 ) ) ;
#61092=CARTESIAN_POINT ( 'NONE',  ( 7.778174593052023411, -7.778174593052021635, 72.06249999999998579 ) ) ;
#61095=CARTESIAN_POINT ( 'NONE',  ( 10.99999999999989342, 4.556349186104152515, 69.53125000409676204 ) ) ;
#61097=CARTESIAN_POINT ( 'NONE',  ( -4.556349186104047710, -10.99999999999999822, 80.96875000409676204 ) ) ;
#61099=CARTESIAN_POINT ( 'NONE',  ( -11.00000000000000533, 11.00000000000000000, 41.99999999999999289 ) ) ;
#61115=CARTESIAN_POINT ( 'NONE',  ( 7.204075437095968759, -7.204075437095966983, 75.71875000204836681 ) ) ;
#61117=FACE_OUTER_BOUND ( 'NONE', #61782, .T. ) ;
#61123=CARTESIAN_POINT ( 'NONE',  ( 7.204075437095968759, -7.204075437095966983, 86.59375000204836681 ) ) ;
#61129=CARTESIAN_POINT ( 'NONE',  ( -10.18810118749999738, -4.220049686691941915, 94.75000000204838102 ) ) ;
#61137=CARTESIAN_POINT ( 'NONE',  ( -7.204075437095965206, -7.204075437095968759, 93.71875000204838102 ) ) ;
#61154=ORIENTED_EDGE ( 'NONE', *, *, #18090, .F. ) ;
#61156=CARTESIAN_POINT ( 'NONE',  ( -10.18810118749999916, 4.220049686691934809, 99.06250000204836681 ) ) ;
#61159=CARTESIAN_POINT ( 'NONE',  ( 11.00000000000000000, 4.556349186104045934, 109.8437500000000000 ) ) ;
#61175=CARTESIAN_POINT ( 'NONE',  ( -6.735557395310442023E-16, 11.00000000000000000, 111.6249999999999858 ) ) ;
#61187=CARTESIAN_POINT ( 'NONE',  ( 0.000000000000000000, 0.000000000000000000, 117.4999999999999716 ) ) ;
#61192=CARTESIAN_POINT ( 'NONE',  ( -6.735557395310442023E-16, 11.00000000000000000, 98.31250000409677625 ) ) ;
#61214=VECTOR ( 'NONE', #19981, 1000.000000000000000 ) ;
#61215=CARTESIAN_POINT ( 'NONE',  ( -10.18810118749999916, 4.220049686691934809, 102.4375000020483810 ) ) ;
#61222=CARTESIAN_POINT ( 'NONE',  ( 2.729893485599592662, 10.18810118749999738, 67.59560438569886287 ) ) ;
#61225=CARTESIAN_POINT ( 'NONE',  ( -7.204075437095967871, 7.204075437095967871, 113.9687500020483810 ) ) ;
#61231=VECTOR ( 'NONE', #71372, 1000.000000000000000 ) ;
#61235=CARTESIAN_POINT ( 'NONE',  ( -10.18810118749999738, -4.220049686691941915, 107.1250000020483810 ) ) ;
#61259=VECTOR ( 'NONE', #44044, 1000.000000000000000 ) ;
#61260=CARTESIAN_POINT ( 'NONE',  ( 10.99999999999989342, 4.556349186104152515, 87.53125000409677625 ) ) ;
#61263=CARTESIAN_POINT ( 'NONE',  ( 4.556349186104052151, -10.99999999999999822, 94.46874999999998579 ) ) ;
#61268=CARTESIAN_POINT ( 'NONE',  ( 10.99999999999989697, -4.556349186104149851, 111.1562500000000142 ) ) ;
#61277=AXIS2_PLACEMENT_3D ( 'NONE', #11632, #5981, #52374 ) ;
#61303=CARTESIAN_POINT ( 'NONE',  ( 4.220049686691934809, 10.18810118749999916, 89.68750000204836681 ) ) ;
#61316=CARTESIAN_POINT ( 'NONE',  ( -10.18810118749999916, 0.000000000000000000, 84.53125000204836681 ) ) ;
#61322=CARTESIAN_POINT ( 'NONE',  ( -11.00000000000000000, 0.000000000000000000, 118.0000000000000000 ) ) ;
#61328=CARTESIAN_POINT ( 'NONE',  ( 4.220049686691934809, 10.18810118749999916, 79.18750000204836681 ) ) ;
#61342=CARTESIAN_POINT ( 'NONE',  ( -15.99999999999999645, -16.00000000000000711, 7.387219678533736733 ) ) ;
#61363=CARTESIAN_POINT ( 'NONE',  ( 4.556349186104051263, -10.99999999999999822, 68.96875000000000000 ) ) ;
#61387=ORIENTED_EDGE ( 'NONE', *, *, #14377, .F. ) ;
#61389=CARTESIAN_POINT ( 'NONE',  ( -10.18810118749999916, 0.000000000000000000, 109.6562500020483668 ) ) ;
#61398=( BOUNDED_CURVE ( )  B_SPLINE_CURVE ( 2, ( #36660, #23854, #47962, #35925, #25315, #48331, #47227, #71339, #19660 ),
 .UNSPECIFIED., .F., .F. ) 
 B_SPLINE_CURVE_WITH_KNOTS ( ( 3, 2, 2, 2, 3 ),
 ( 0.6470588235294116863, 0.6507352941176469674, 0.6544117647058822484, 0.6580882352941175295, 0.6617647058823528106 ),
 .UNSPECIFIED. ) 
 CURVE ( )  GEOMETRIC_REPRESENTATION_ITEM ( )  RATIONAL_B_SPLINE_CURVE ( ( 1.000000000000002220, 0.9238795325112844070, 1.000000000000000000, 0.9238795325112867385, 1.000000000000000000, 0.9238795325112867385, 1.000000000000000000, 0.9238795325112890700, 0.9999999999999976685 ) ) 
 REPRESENTATION_ITEM ( '' )  );
#61403=CARTESIAN_POINT ( 'NONE',  ( -10.18810118749999916, 4.220049686691934809, 99.43750000204836681 ) ) ;
#61425=CARTESIAN_POINT ( 'NONE',  ( -10.18810118749999738, -4.220049686691941915, 80.12500000204835260 ) ) ;
#61444=CARTESIAN_POINT ( 'NONE',  ( 4.220049686691934809, 10.18810118749999916, 73.18750000204838102 ) ) ;
#61447=CARTESIAN_POINT ( 'NONE',  ( -4.556349186104047710, -10.99999999999999822, 91.28125000000000000 ) ) ;
#61470=CARTESIAN_POINT ( 'NONE',  ( -11.00000000000000000, 0.000000000000000000, 71.49999999999998579 ) ) ;
#61475=CARTESIAN_POINT ( 'NONE',  ( -7.778174593052020747, -7.778174593052023411, 80.87500000409677625 ) ) ;
#61492=CARTESIAN_POINT ( 'NONE',  ( -6.238412754330611322E-16, 10.18810118749999916, 76.28125000204836681 ) ) ;
#61501=CARTESIAN_POINT ( 'NONE',  ( -10.18810118749999916, 4.220049686691934809, 87.43750000204838102 ) ) ;
#61507=CARTESIAN_POINT ( 'NONE',  ( 10.18810118750000093, -4.220049686691933921, 98.31250000204836681 ) ) ;
#61516=CARTESIAN_POINT ( 'NONE',  ( 7.204075437095966983, 7.204075437095967871, 89.96875000204838102 ) ) ;
#61533=CARTESIAN_POINT ( 'NONE',  ( 4.220049686691941027, -10.18810118749999738, 99.62500000204838102 ) ) ;
#61536=CARTESIAN_POINT ( 'NONE',  ( 11.00000000000000355, -4.556349186104045046, 105.1562499999999858 ) ) ;
#61562=DIRECTION ( 'NONE',  ( -0.000000000000000000, -0.000000000000000000, -1.000000000000000000 ) ) ;
#61568=CARTESIAN_POINT ( 'NONE',  ( -4.556349186104047710, -10.99999999999999822, 95.96875000409676204 ) ) ;
#61588=CARTESIAN_POINT ( 'NONE',  ( -10.18810118749999738, -4.220049686691941915, 101.1250000020483810 ) ) ;
#61594=CARTESIAN_POINT ( 'NONE',  ( -7.204075437095967871, 7.204075437095967871, 67.84375000204836681 ) ) ;
#61597=CARTESIAN_POINT ( 'NONE',  ( 7.204075437095966983, 7.204075437095967871, 113.5937500020483810 ) ) ;
#61605=CARTESIAN_POINT ( 'NONE',  ( 7.778174593052023411, -7.778174593052021635, 103.7500000040967763 ) ) ;
#61607=CARTESIAN_POINT ( 'NONE',  ( 7.204075437095966983, 7.204075437095967871, 109.4687500020483810 ) ) ;
#61608=( GEOMETRIC_REPRESENTATION_CONTEXT ( 3 ) GLOBAL_UNCERTAINTY_ASSIGNED_CONTEXT ( ( #58187 ) ) GLOBAL_UNIT_ASSIGNED_CONTEXT ( ( #51006, #34426, #69105 ) ) REPRESENTATION_CONTEXT ( 'NONE', 'WORKASPACE' ) );
#61619=CARTESIAN_POINT ( 'NONE',  ( -10.18810118749999738, -4.220049686691941915, 69.62500000204838102 ) ) ;
#61627=CARTESIAN_POINT ( 'NONE',  ( -6.238412754330611322E-16, 10.18810118749999916, 113.7812500020483810 ) ) ;
#61640=DIRECTION ( 'NONE',  ( -0.000000000000000000, -0.000000000000000000, -1.000000000000000000 ) ) ;
#61643=CARTESIAN_POINT ( 'NONE',  ( 7.778174593052021635, 7.778174593052023411, 107.1250000040967763 ) ) ;
#61652=DIRECTION ( 'NONE',  ( -1.000000000000000000, -2.168404344971008868E-16, -0.000000000000000000 ) ) ;
#61671=CARTESIAN_POINT ( 'NONE',  ( 7.778174593052021635, 7.778174593052023411, 81.62500000409677625 ) ) ;
#61674=ORIENTED_EDGE ( 'NONE', *, *, #50371, .T. ) ;
#61676=CARTESIAN_POINT ( 'NONE',  ( -10.18810118749999738, -4.220049686691941915, 87.25000000204838102 ) ) ;
#61677=CARTESIAN_POINT ( 'NONE',  ( -6.735557395310442023E-16, 11.00000000000000000, 93.62499999999998579 ) ) ;
#61684=CARTESIAN_POINT ( 'NONE',  ( 7.778174593052021635, 7.778174593052023411, 76.93749999999998579 ) ) ;
#61689=CARTESIAN_POINT ( 'NONE',  ( -4.220049686691935698, 10.18810118749999916, 82.75000000204838102 ) ) ;
#61695=CARTESIAN_POINT ( 'NONE',  ( 10.99999999999999645, -10.99999999999999645, 41.99999999999999289 ) ) ;
#61703=CARTESIAN_POINT ( 'NONE',  ( -7.204075437095965206, -7.204075437095968759, 79.84375000204838102 ) ) ;
#61705=EDGE_CURVE ( 'NONE', #72225, #42214, #72716, .T. ) ;
#61707=EDGE_LOOP ( 'NONE', ( #59662, #37763, #58553, #22297 ) ) ;
#61739=CARTESIAN_POINT ( 'NONE',  ( -4.556349186104047710, -10.99999999999999822, 68.78125000000001421 ) ) ;
#61765=CARTESIAN_POINT ( 'NONE',  ( -4.220049686691937474, -10.18810118749999738, 105.4375000020483668 ) ) ;
#61768=CARTESIAN_POINT ( 'NONE',  ( 11.00000000000000000, 1.347111479062088405E-15, 69.24999999999997158 ) ) ;
#61774=EDGE_CURVE ( 'NONE', #27901, #44494, #27450, .T. ) ;
#61780=CARTESIAN_POINT ( 'NONE',  ( 10.18810118749999916, 4.220049686691935698, 101.8750000020483810 ) ) ;
#61782=EDGE_LOOP ( 'NONE', ( #74602, #28210, #36602, #60222 ) ) ;
#61784=CARTESIAN_POINT ( 'NONE',  ( -11.00000000000000000, 0.000000000000000000, 118.0000000000000000 ) ) ;
#61799=CARTESIAN_POINT ( 'NONE',  ( -10.18810118749999916, 4.220049686691934809, 81.43750000204836681 ) ) ;
#61804=ORIENTED_EDGE ( 'NONE', *, *, #59906, .T. ) ;
#61816=CARTESIAN_POINT ( 'NONE',  ( -10.18810118749999738, -4.220049686691941915, 72.25000000204836681 ) ) ;
#61819=CARTESIAN_POINT ( 'NONE',  ( 11.00000000000000000, 1.347111479062088405E-15, 91.74999999999998579 ) ) ;
#61841=LINE ( 'NONE', #33939, #43602 ) ;
#61843=CARTESIAN_POINT ( 'NONE',  ( -11.00000000000000000, 0.000000000000000000, 76.18750000409677625 ) ) ;
#61848=CARTESIAN_POINT ( 'NONE',  ( 4.556349186104045934, 11.00000000000000000, 72.71875000409677625 ) ) ;
#61865=CARTESIAN_POINT ( 'NONE',  ( 4.220049686691941027, -10.18810118749999738, 78.62500000204838102 ) ) ;
#61875=CARTESIAN_POINT ( 'NONE',  ( 10.18810118749999916, 1.247682550866122264E-15, 79.28125000204836681 ) ) ;
#61886=CARTESIAN_POINT ( 'NONE',  ( -6.238412754330611322E-16, 10.18810118749999916, 94.65625000204836681 ) ) ;
#61899=ORIENTED_EDGE ( 'NONE', *, *, #35772, .T. ) ;
#61901=CARTESIAN_POINT ( 'NONE',  ( -10.18810118749999916, 4.220049686691934809, 93.06250000204838102 ) ) ;
#61904=CARTESIAN_POINT ( 'NONE',  ( 4.556349186104051263, -10.99999999999999822, 109.4687499999999858 ) ) ;
#61926=CARTESIAN_POINT ( 'NONE',  ( 0.000000000000000000, 0.000000000000000000, 118.0000000000000000 ) ) ;
#61927=CARTESIAN_POINT ( 'NONE',  ( -11.00000000000000000, 0.000000000000000000, 88.00000000000000000 ) ) ;
#61933=CARTESIAN_POINT ( 'NONE',  ( 11.00000000000000000, 1.347111479062088405E-15, 90.43750000409676204 ) ) ;
#61934=LINE ( 'NONE', #57785, #2207 ) ;
#61955=CARTESIAN_POINT ( 'NONE',  ( -10.18810118749999738, -4.220049686691941915, 96.62500000204838102 ) ) ;
#61964=CARTESIAN_POINT ( 'NONE',  ( 7.204075437095966983, 7.204075437095967871, 112.0937500020483810 ) ) ;
#61973=CARTESIAN_POINT ( 'NONE',  ( 4.220049686691941027, -10.18810118749999738, 109.0000000020483810 ) ) ;
#61991=CARTESIAN_POINT ( 'NONE',  ( 7.778174593052021635, 7.778174593052023411, 90.43749999999998579 ) ) ;
#61993=CARTESIAN_POINT ( 'NONE',  ( 7.204075437095968759, -7.204075437095966983, 108.7187500020483810 ) ) ;
#62018=VERTEX_POINT ( 'NONE', #42079 ) ;
#62041=CARTESIAN_POINT ( 'NONE',  ( 4.220049686691941027, -10.18810118749999738, 87.62500000204836681 ) ) ;
#62042=DIRECTION ( 'NONE',  ( -0.000000000000000000, -0.000000000000000000, -1.000000000000000000 ) ) ;
#62054=CARTESIAN_POINT ( 'NONE',  ( -10.18810118749999916, 0.000000000000000000, 83.03125000204838102 ) ) ;
#62060=CARTESIAN_POINT ( 'NONE',  ( 7.778174593052023411, -7.778174593052021635, 85.75000000409677625 ) ) ;
#62068=CARTESIAN_POINT ( 'NONE',  ( 10.18810118749999916, 4.220049686691935698, 79.00000000204838102 ) ) ;
#62081=EDGE_CURVE ( 'NONE', #73625, #8706, #48481, .T. ) ;
#62099=LINE ( 'NONE', #33452, #39456 ) ;
#62104=CARTESIAN_POINT ( 'NONE',  ( -7.778174593052020747, -7.778174593052023411, 73.18749999999998579 ) ) ;
#62129=CARTESIAN_POINT ( 'NONE',  ( -10.18810118749999916, 0.000000000000000000, 106.6562500020483668 ) ) ;
#62145=CARTESIAN_POINT ( 'NONE',  ( -10.18810118749999916, 4.220049686691934809, 103.9375000020483810 ) ) ;
#62153=CARTESIAN_POINT ( 'NONE',  ( -10.99999999999999822, -4.556349186104053040, 71.78125000409679046 ) ) ;
#62163=CARTESIAN_POINT ( 'NONE',  ( 4.220049686691934809, 10.18810118749999916, 81.06250000204836681 ) ) ;
#62169=ORIENTED_EDGE ( 'NONE', *, *, #66030, .T. ) ;
#62182=CARTESIAN_POINT ( 'NONE',  ( 4.220049686691934809, 10.18810118749999916, 76.18750000204838102 ) ) ;
#62184=CARTESIAN_POINT ( 'NONE',  ( -10.18810118749999916, 0.000000000000000000, 117.1562500020483810 ) ) ;
#62185=CARTESIAN_POINT ( 'NONE',  ( -4.556349186104045934, 11.00000000000000000, 92.21875000000000000 ) ) ;
#62213=CARTESIAN_POINT ( 'NONE',  ( -11.00000000000000000, 0.000000000000000000, 71.68750000409676204 ) ) ;
#62230=CARTESIAN_POINT ( 'NONE',  ( -7.204075437095965206, -7.204075437095968759, 69.34375000204836681 ) ) ;
#62236=CARTESIAN_POINT ( 'NONE',  ( -10.99999999999989164, -4.556349186104158733, 79.28125000409679046 ) ) ;
#62239=CARTESIAN_POINT ( 'NONE',  ( 4.220049686691941027, -10.18810118749999738, 80.50000000204839523 ) ) ;
#62268=CARTESIAN_POINT ( 'NONE',  ( -6.238412754330611322E-16, 10.18810118749999916, 91.28125000204836681 ) ) ;
#62271=CARTESIAN_POINT ( 'NONE',  ( -4.556349186104047710, -10.99999999999999822, 104.7812499999999858 ) ) ;
#62302=CARTESIAN_POINT ( 'NONE',  ( -10.99999999999999822, -4.556349186104052151, 91.28125000409676204 ) ) ;
#62315=CARTESIAN_POINT ( 'NONE',  ( -7.778174593052023411, 7.778174593052023411, 103.0000000040967763 ) ) ;
#62324=CARTESIAN_POINT ( 'NONE',  ( -4.220049686691937474, -10.18810118749999738, 96.81250000204839523 ) ) ;
#62327=CARTESIAN_POINT ( 'NONE',  ( -11.00000000000000000, 4.556349186104045934, 98.40625000000000000 ) ) ;
#62331=CARTESIAN_POINT ( 'NONE',  ( -10.18810118749999916, 4.220049686691934809, 111.0625000020483810 ) ) ;
#62336=CARTESIAN_POINT ( 'NONE',  ( -7.778174593052020747, -7.778174593052023411, 76.37500000409677625 ) ) ;
#62339=CARTESIAN_POINT ( 'NONE',  ( 7.204075437095966983, 7.204075437095967871, 107.9687500020483810 ) ) ;
#62341=VERTEX_POINT ( 'NONE', #15265 ) ;
#62353=CARTESIAN_POINT ( 'NONE',  ( 1.871523826299183495E-15, -10.18810118749999916, 110.0312500020483668 ) ) ;
#62382=CARTESIAN_POINT ( 'NONE',  ( 11.00000000000000000, 1.347111479062088405E-15, 109.9375000040967763 ) ) ;
#62385=VECTOR ( 'NONE', #71032, 1000.000000000000000 ) ;
#62397=VERTEX_POINT ( 'NONE', #74013 ) ;
#62398=DIRECTION ( 'NONE',  ( -0.000000000000000000, -0.000000000000000000, -1.000000000000000000 ) ) ;
#62401=CARTESIAN_POINT ( 'NONE',  ( -7.778174593052023411, 7.778174593052023411, 95.31250000000000000 ) ) ;
#62405=CARTESIAN_POINT ( 'NONE',  ( 10.18810118749999916, 4.220049686691935698, 86.50000000204838102 ) ) ;
#62411=CARTESIAN_POINT ( 'NONE',  ( 4.220049686691941027, -10.18810118749999738, 115.0000000020483668 ) ) ;
#62420=CARTESIAN_POINT ( 'NONE',  ( -4.220049686691937474, -10.18810118749999738, 83.31250000204836681 ) ) ;
#62432=CARTESIAN_POINT ( 'NONE',  ( 4.220049686691934809, 10.18810118749999916, 76.18750000204839523 ) ) ;
#62467=CARTESIAN_POINT ( 'NONE',  ( -6.735557395310442023E-16, 11.00000000000000000, 68.12499999999998579 ) ) ;
#62485=ORIENTED_EDGE ( 'NONE', *, *, #55808, .T. ) ;
#62492=ORIENTED_EDGE ( 'NONE', *, *, #37412, .F. ) ;
#62494=CARTESIAN_POINT ( 'NONE',  ( 10.18810118750000093, -4.220049686691933921, 107.3125000020483668 ) ) ;
#62504=( BOUNDED_CURVE ( )  B_SPLINE_CURVE ( 2, ( #71867, #30046, #25101, #70408, #53059, #71124, #41733, #48118, #30777 ),
 .UNSPECIFIED., .F., .F. ) 
 B_SPLINE_CURVE_WITH_KNOTS ( ( 3, 2, 2, 2, 3 ),
 ( 0.6470588235294115753, 0.6507352941176468564, 0.6544117647058821374, 0.6580882352941174185, 0.6617647058823526995 ),
 .UNSPECIFIED. ) 
 CURVE ( )  GEOMETRIC_REPRESENTATION_ITEM ( )  RATIONAL_B_SPLINE_CURVE ( ( 1.000000000000004663, 0.9238795325112821866, 1.000000000000000000, 0.9238795325112867385, 1.000000000000000000, 0.9238795325112867385, 1.000000000000000000, 0.9238795325112912904, 0.9999999999999954481 ) ) 
 REPRESENTATION_ITEM ( '' )  );
#62507=CARTESIAN_POINT ( 'NONE',  ( -15.99999999999999645, 15.99999999999999645, 7.387219678533736733 ) ) ;
#62514=CARTESIAN_POINT ( 'NONE',  ( 7.204075437095966983, 7.204075437095967871, 98.96875000204838102 ) ) ;
#62533=CARTESIAN_POINT ( 'NONE',  ( 1.871523826299183495E-15, -10.18810118749999916, 78.90625000204836681 ) ) ;
#62546=ORIENTED_EDGE ( 'NONE', *, *, #69346, .F. ) ;
#62551=CARTESIAN_POINT ( 'NONE',  ( 4.220049686691941027, -10.18810118749999738, 75.62500000204838102 ) ) ;
#62554=CARTESIAN_POINT ( 'NONE',  ( 2.020667218593132706E-15, -11.00000000000000000, 86.87499999999998579 ) ) ;
#62559=CARTESIAN_POINT ( 'NONE',  ( 5.094044972490348933, 8.823157690132404696, 67.53052377765949643 ) ) ;
#62577=CARTESIAN_POINT ( 'NONE',  ( -4.556349186104048599, -10.99999999999999822, 74.78125000000001421 ) ) ;
#62578=CARTESIAN_POINT ( 'NONE',  ( -4.556349186104048599, -10.99999999999999822, 80.96875000409677625 ) ) ;
#62580=CARTESIAN_POINT ( 'NONE',  ( -6.735557395310442023E-16, 11.00000000000000000, 72.81250000409677625 ) ) ;
#62595=CARTESIAN_POINT ( 'NONE',  ( 4.220049686691934809, 10.18810118749999916, 117.0625000020483668 ) ) ;
#62599=CARTESIAN_POINT ( 'NONE',  ( 10.18810118750000093, -4.220049686691933921, 68.31250000204838102 ) ) ;
#62609=CARTESIAN_POINT ( 'NONE',  ( 7.204075437095966983, 7.204075437095967871, 77.96875000204836681 ) ) ;
#62614=( BOUNDED_CURVE ( )  B_SPLINE_CURVE ( 2, ( #54183, #48867, #36456, #8514, #36088, #13778, #42095, #59469, #19825 ),
 .UNSPECIFIED., .F., .F. ) 
 B_SPLINE_CURVE_WITH_KNOTS ( ( 3, 2, 2, 2, 3 ),
 ( 0.2794117647058822484, 0.2830882352941175295, 0.2867647058823528106, 0.2904411764705881471, 0.2941176470588234282 ),
 .UNSPECIFIED. ) 
 CURVE ( )  GEOMETRIC_REPRESENTATION_ITEM ( )  RATIONAL_B_SPLINE_CURVE ( ( 1.000000000000002220, 0.9238795325112844070, 1.000000000000000000, 0.9238795325112867385, 1.000000000000000000, 0.9238795325112867385, 1.000000000000000000, 0.9238795325112890700, 0.9999999999999976685 ) ) 
 REPRESENTATION_ITEM ( '' )  );
#62637=CARTESIAN_POINT ( 'NONE',  ( 4.220049686691934809, 10.18810118749999916, 92.68750000204838102 ) ) ;
#62640=CARTESIAN_POINT ( 'NONE',  ( -7.778174593052023411, 7.778174593052023411, 108.8124999999999858 ) ) ;
#62649=AXIS2_PLACEMENT_3D ( 'NONE', #36307, #48346, #25331 ) ;
#62657=CARTESIAN_POINT ( 'NONE',  ( -11.00000000000010658, 4.556349186103942017, 86.40624999999998579 ) ) ;
#62669=CARTESIAN_POINT ( 'NONE',  ( -4.556349186104045934, 11.00000000000000000, 93.90625000409679046 ) ) ;
#62689=CARTESIAN_POINT ( 'NONE',  ( 4.220049686691941027, -10.18810118749999738, 97.00000000204836681 ) ) ;
#62692=EDGE_CURVE ( 'NONE', #49057, #69053, #55461, .T. ) ;
#62699=CARTESIAN_POINT ( 'NONE',  ( 7.204075437095966983, 7.204075437095967871, 104.5937500020483810 ) ) ;
#62708=CARTESIAN_POINT ( 'NONE',  ( -6.238412754330611322E-16, 10.18810118749999916, 111.1562500020483668 ) ) ;
#62710=CARTESIAN_POINT ( 'NONE',  ( 7.778174593052021635, 7.778174593052023411, 75.43749999999998579 ) ) ;
#62723=CARTESIAN_POINT ( 'NONE',  ( -11.00000000000000000, 0.000000000000000000, 93.99999999999998579 ) ) ;
#62725=CARTESIAN_POINT ( 'NONE',  ( 10.18810118749999916, 1.247682550866122264E-15, 111.9062500020483810 ) ) ;
#62744=DIRECTION ( 'NONE',  ( 0.000000000000000000, -1.000000000000000000, 0.000000000000000000 ) ) ;
#62746=ORIENTED_EDGE ( 'NONE', *, *, #19001, .T. ) ;
#62749=CARTESIAN_POINT ( 'NONE',  ( -4.556349186104047710, -10.99999999999999822, 110.9687500040967905 ) ) ;
#62764=ORIENTED_EDGE ( 'NONE', *, *, #24932, .T. ) ;
#62767=CARTESIAN_POINT ( 'NONE',  ( 7.778174593052021635, 7.778174593052023411, 103.9374999999999858 ) ) ;
#62771=CARTESIAN_POINT ( 'NONE',  ( -7.204075437095967871, 7.204075437095967871, 88.46875000204838102 ) ) ;
#62785=CARTESIAN_POINT ( 'NONE',  ( 4.220049686691941027, -10.18810118749999738, 76.00000000204835260 ) ) ;
#62801=CARTESIAN_POINT ( 'NONE',  ( -10.18810118749999916, 4.220049686691934809, 78.06250000204838102 ) ) ;
#62866=CARTESIAN_POINT ( 'NONE',  ( 4.220049686691934809, 10.18810118749999916, 109.1875000020483810 ) ) ;
#62869=CARTESIAN_POINT ( 'NONE',  ( -11.00000000000000000, 0.000000000000000000, 68.49999999999997158 ) ) ;
#62882=CARTESIAN_POINT ( 'NONE',  ( 4.220049686691941027, -10.18810118749999738, 100.0000000020483952 ) ) ;
#62896=CARTESIAN_POINT ( 'NONE',  ( -4.220049686691937474, -10.18810118749999738, 94.93750000204838102 ) ) ;
#62904=EDGE_CURVE ( 'NONE', #10364, #12665, #13948, .T. ) ;
#62909=CARTESIAN_POINT ( 'NONE',  ( -7.204075437095965206, -7.204075437095968759, 83.21875000204836681 ) ) ;
#62916=DIRECTION ( 'NONE',  ( 0.000000000000000000, -1.000000000000000000, 0.000000000000000000 ) ) ;
#62922=CARTESIAN_POINT ( 'NONE',  ( -7.778174593052020747, -7.778174593052023411, 88.37500000409677625 ) ) ;
#62925=EDGE_LOOP ( 'NONE', ( #61899, #9825, #33475, #9885 ) ) ;
#62931=CARTESIAN_POINT ( 'NONE',  ( 4.220049686691941027, -10.18810118749999738, 72.62500000204836681 ) ) ;
#62934=CARTESIAN_POINT ( 'NONE',  ( 7.778174593052021635, 7.778174593052023411, 84.43749999999998579 ) ) ;
#62960=CARTESIAN_POINT ( 'NONE',  ( -4.556349186104045934, 11.00000000000000000, 72.90625000409677625 ) ) ;
#62980=CARTESIAN_POINT ( 'NONE',  ( -10.18810118749999916, 4.220049686691934809, 69.06250000204839523 ) ) ;
#63014=CARTESIAN_POINT ( 'NONE',  ( 4.220049686691941027, -10.18810118749999738, 90.62500000204836681 ) ) ;
#63017=CARTESIAN_POINT ( 'NONE',  ( 2.020667218593132706E-15, -11.00000000000000000, 103.3750000000000000 ) ) ;
#63047=CARTESIAN_POINT ( 'NONE',  ( 2.020667218593132706E-15, -11.00000000000000000, 90.06250000409676204 ) ) ;
#63068=DIRECTION ( 'NONE',  ( 0.000000000000000000, 0.000000000000000000, 1.000000000000000000 ) ) ;
#63072=CARTESIAN_POINT ( 'NONE',  ( -7.204075437095967871, 7.204075437095967871, 97.84375000204836681 ) ) ;
#63075=CARTESIAN_POINT ( 'NONE',  ( 11.00000000000000000, 4.556349186104045934, 97.84375000000000000 ) ) ;
#63079=CARTESIAN_POINT ( 'NONE',  ( -10.18810118749999916, 4.220049686691934809, 108.0625000020483810 ) ) ;
#63088=CARTESIAN_POINT ( 'NONE',  ( 10.18810118749999916, 4.220049686691935698, 106.3750000020483668 ) ) ;
#63097=CARTESIAN_POINT ( 'NONE',  ( 0.000000000000000000, 0.000000000000000000, 0.000000000000000000 ) ) ;
#63104=CARTESIAN_POINT ( 'NONE',  ( -10.18810118749999916, 0.000000000000000000, 109.6562500020483668 ) ) ;
#63120=CARTESIAN_POINT ( 'NONE',  ( 7.204075437095968759, -7.204075437095966983, 68.59375000204836681 ) ) ;
#63132=CARTESIAN_POINT ( 'NONE',  ( -11.00000000000000000, 4.556349186104045934, 113.5937500040967763 ) ) ;
#63151=DIRECTION ( 'NONE',  ( -0.000000000000000000, -0.000000000000000000, -1.000000000000000000 ) ) ;
#63155=CARTESIAN_POINT ( 'NONE',  ( 10.18810118749999916, 1.247682550866122264E-15, 83.40625000204838102 ) ) ;
#63159=CARTESIAN_POINT ( 'NONE',  ( -10.18810118749999738, -4.220049686691941915, 113.1250000020483810 ) ) ;
#63168=CARTESIAN_POINT ( 'NONE',  ( 4.220049686691941027, -10.18810118749999738, 74.50000000204838102 ) ) ;
#63179=CARTESIAN_POINT ( 'NONE',  ( -6.238412754330611322E-16, 10.18810118749999916, 70.28125000204838102 ) ) ;
#63198=CARTESIAN_POINT ( 'NONE',  ( 11.00000000000000000, 1.347111479062088405E-15, 73.93750000409676204 ) ) ;
#63208=CARTESIAN_POINT ( 'NONE',  ( -11.00000000000000000, 0.000000000000000000, 80.49999999999998579 ) ) ;
#63239=CARTESIAN_POINT ( 'NONE',  ( 7.204075437095966983, 7.204075437095967871, 103.0937500020483668 ) ) ;
#63242=CARTESIAN_POINT ( 'NONE',  ( 2.020667218593132706E-15, -11.00000000000000000, 68.87499999999998579 ) ) ;
#63256=CARTESIAN_POINT ( 'NONE',  ( -7.204075437095967871, 7.204075437095967871, 97.84375000204836681 ) ) ;
#63258=ORIENTED_EDGE ( 'NONE', *, *, #69399, .F. ) ;
#63266=CARTESIAN_POINT ( 'NONE',  ( 7.778174593052021635, 7.778174593052023411, 89.12500000409677625 ) ) ;
#63268=CARTESIAN_POINT ( 'NONE',  ( 10.18810118749999916, 4.220049686691935698, 94.00000000204838102 ) ) ;
#63269=( BOUNDED_CURVE ( )  B_SPLINE_CURVE ( 2, ( #28046, #73696, #11811, #21635, #57099, #10330, #69155, #5414, #45390 ),
 .UNSPECIFIED., .F., .F. ) 
 B_SPLINE_CURVE_WITH_KNOTS ( ( 3, 2, 2, 2, 3 ),
 ( 0.5147058823529412352, 0.5183823529411765163, 0.5220588235294116863, 0.5257352941176469674, 0.5294117647058821374 ),
 .UNSPECIFIED. ) 
 CURVE ( )  GEOMETRIC_REPRESENTATION_ITEM ( )  RATIONAL_B_SPLINE_CURVE ( ( 0.9999999999999976685, 0.9238795325112890700, 1.000000000000000000, 0.9238795325112867385, 1.000000000000000000, 0.9238795325112867385, 1.000000000000000000, 0.9238795325112912904, 0.9999999999999954481 ) ) 
 REPRESENTATION_ITEM ( '' )  );
#63277=CARTESIAN_POINT ( 'NONE',  ( 1.871523826299183495E-15, -10.18810118749999916, 75.90625000204836681 ) ) ;
#63283=CARTESIAN_POINT ( 'NONE',  ( -11.00000000000004796, -4.556349186104000637, 92.78125000409677625 ) ) ;
#63295=CARTESIAN_POINT ( 'NONE',  ( -4.220049686691935698, 10.18810118749999916, 68.87500000204838102 ) ) ;
#63298=CARTESIAN_POINT ( 'NONE',  ( 7.778174593052023411, -7.778174593052021635, 82.56249999999998579 ) ) ;
#63302=EDGE_LOOP ( 'NONE', ( #69166, #28493, #20854, #13373 ) ) ;
#63305=FACE_OUTER_BOUND ( 'NONE', #42268, .T. ) ;
#63306=AXIS2_PLACEMENT_3D ( 'NONE', #43380, #48297, #9444 ) ;
#63309=EDGE_CURVE ( 'NONE', #11062, #32460, #73301, .T. ) ;
#63328=CARTESIAN_POINT ( 'NONE',  ( -11.00000000000000000, 0.000000000000000000, 73.18750000409676204 ) ) ;
#63340=CARTESIAN_POINT ( 'NONE',  ( -10.18810118749999738, -4.220049686691941915, 113.1250000020483810 ) ) ;
#63344=CARTESIAN_POINT ( 'NONE',  ( 4.220049686691934809, 10.18810118749999916, 73.18750000204838102 ) ) ;
#63369=ORIENTED_EDGE ( 'NONE', *, *, #55529, .T. ) ;
#63372=CARTESIAN_POINT ( 'NONE',  ( 10.99999999999989342, 4.556349186104152515, 78.53125000409677625 ) ) ;
#63375=ORIENTED_EDGE ( 'NONE', *, *, #22932, .F. ) ;
#63381=EDGE_LOOP ( 'NONE', ( #36717, #20584, #55795, #43136, #31036 ) ) ;
#63382=CARTESIAN_POINT ( 'NONE',  ( 4.220049686691934809, 10.18810118749999916, 89.68750000204838102 ) ) ;
#63385=CARTESIAN_POINT ( 'NONE',  ( -4.556349186104047710, -10.99999999999999822, 98.78125000000000000 ) ) ;
#63411=EDGE_LOOP ( 'NONE', ( #59310, #62485, #9009, #32964 ) ) ;
#63414=CARTESIAN_POINT ( 'NONE',  ( -7.778174593052023411, 7.778174593052023411, 91.00000000409677625 ) ) ;
#63438=CARTESIAN_POINT ( 'NONE',  ( -7.204075437095967871, 7.204075437095967871, 94.84375000204838102 ) ) ;
#63446=CARTESIAN_POINT ( 'NONE',  ( -7.204075437095967871, 7.204075437095967871, 106.4687500020483810 ) ) ;
#63455=CARTESIAN_POINT ( 'NONE',  ( 4.220049686691934809, 10.18810118749999916, 105.0625000020483810 ) ) ;
#63456=CARTESIAN_POINT ( 'NONE',  ( 4.556349186104045934, 11.00000000000000000, 75.53125000000000000 ) ) ;
#63460=VECTOR ( 'NONE', #48529, 1000.000000000000000 ) ;
#63475=CARTESIAN_POINT ( 'NONE',  ( 4.220049686691934809, 10.18810118749999916, 107.6875000020483810 ) ) ;
#63493=CARTESIAN_POINT ( 'NONE',  ( -10.18810118749999738, -4.220049686691941915, 68.12500000204838102 ) ) ;
#63499=CARTESIAN_POINT ( 'NONE',  ( 4.556349186104052151, -10.99999999999999822, 97.65625000409679046 ) ) ;
#63505=CARTESIAN_POINT ( 'NONE',  ( 4.556349186104045934, 11.00000000000000000, 113.2187500040967763 ) ) ;
#63509=CARTESIAN_POINT ( 'NONE',  ( 11.00000000000000000, 1.347111479062088405E-15, 108.4375000040967763 ) ) ;
#63518=ORIENTED_EDGE ( 'NONE', *, *, #43034, .T. ) ;
#63526=CARTESIAN_POINT ( 'NONE',  ( 4.220049686691941027, -10.18810118749999738, 81.62500000204836681 ) ) ;
#63537=CARTESIAN_POINT ( 'NONE',  ( 7.204075437095968759, -7.204075437095966983, 76.09375000204838102 ) ) ;
#63539=ORIENTED_EDGE ( 'NONE', *, *, #48682, .T. ) ;
#63550=CARTESIAN_POINT ( 'NONE',  ( -7.204075437095965206, -7.204075437095968759, 73.84375000204838102 ) ) ;
#63588=CARTESIAN_POINT ( 'NONE',  ( 11.00000000000000000, 1.347111479062088405E-15, 82.93750000409677625 ) ) ;
#63613=CARTESIAN_POINT ( 'NONE',  ( -4.220049686691935698, 10.18810118749999916, 100.3750000020484094 ) ) ;
#63624=CARTESIAN_POINT ( 'NONE',  ( -6.735557395310442023E-16, 11.00000000000000000, 99.81250000409677625 ) ) ;
#63628=CARTESIAN_POINT ( 'NONE',  ( -4.220049686691937474, -10.18810118749999738, 92.31250000204838102 ) ) ;
#63637=VERTEX_POINT ( 'NONE', #37956 ) ;
#63643=CARTESIAN_POINT ( 'NONE',  ( -7.204075437095967871, 7.204075437095967871, 89.96875000204838102 ) ) ;
#63655=CARTESIAN_POINT ( 'NONE',  ( -10.18810118749999916, 0.000000000000000000, 77.03125000204836681 ) ) ;
#63670=CARTESIAN_POINT ( 'NONE',  ( -6.238412754330611322E-16, 10.18810118749999916, 68.78125000204838102 ) ) ;
#63673=CARTESIAN_POINT ( 'NONE',  ( -10.99999999999999822, -4.556349186104052151, 82.09375000000000000 ) ) ;
#63693=CYLINDRICAL_SURFACE ( 'NONE', #71329, 11.00000000000000000 ) ;
#63696=EDGE_LOOP ( 'NONE', ( #61009, #20039, #43139, #61387 ) ) ;
#63701=CARTESIAN_POINT ( 'NONE',  ( 4.556349186104051263, -10.99999999999999822, 67.65625000409677625 ) ) ;
#63711=CARTESIAN_POINT ( 'NONE',  ( 11.00000000000000000, 1.347111479062088405E-15, 105.2500000000000000 ) ) ;
#63714=CARTESIAN_POINT ( 'NONE',  ( -10.18810118749999916, 4.220049686691934809, 115.9375000020483810 ) ) ;
#63727=ORIENTED_EDGE ( 'NONE', *, *, #62081, .F. ) ;
#63748=EDGE_CURVE ( 'NONE', #12665, #22034, #46400, .T. ) ;
#63749=CARTESIAN_POINT ( 'NONE',  ( -11.00000000000000000, 0.000000000000000000, 79.18750000409677625 ) ) ;
#63757=CARTESIAN_POINT ( 'NONE',  ( 1.871523826299183495E-15, -10.18810118749999916, 84.53125000204836681 ) ) ;
#63759=CARTESIAN_POINT ( 'NONE',  ( -11.00000000000000000, 4.556349186104045934, 102.9062499999999858 ) ) ;
#63789=CARTESIAN_POINT ( 'NONE',  ( -7.778174593052020747, -7.778174593052023411, 85.37500000409677625 ) ) ;
#63806=CARTESIAN_POINT ( 'NONE',  ( 4.556349186104052151, -10.99999999999999822, 100.4687500000000000 ) ) ;
#63816=CARTESIAN_POINT ( 'NONE',  ( -7.204075437095967871, 7.204075437095967871, 88.84375000204838102 ) ) ;
#63817=ORIENTED_EDGE ( 'NONE', *, *, #30960, .T. ) ;
#63822=CARTESIAN_POINT ( 'NONE',  ( -10.18810118749999916, 4.220049686691934809, 105.0625000020483810 ) ) ;
#63828=CARTESIAN_POINT ( 'NONE',  ( 11.00000000000000000, 1.347111479062088405E-15, 76.93750000409677625 ) ) ;
#63832=CARTESIAN_POINT ( 'NONE',  ( 1.871523826299183495E-15, -10.18810118749999916, 104.4062500020483810 ) ) ;
#63838=CARTESIAN_POINT ( 'NONE',  ( -4.556349186104048599, -10.99999999999999822, 80.78124999999998579 ) ) ;
#63850=CARTESIAN_POINT ( 'NONE',  ( -10.18810118749999738, -4.220049686691941915, 103.7500000020483668 ) ) ;
#63868=CARTESIAN_POINT ( 'NONE',  ( 1.871523826299183495E-15, -10.18810118749999916, 71.40625000204836681 ) ) ;
#63879=CARTESIAN_POINT ( 'NONE',  ( 4.556349186104045934, 11.00000000000000000, 111.7187500040967905 ) ) ;
#63894=CARTESIAN_POINT ( 'NONE',  ( 4.556349186104045934, 11.00000000000000000, 116.0312499999999858 ) ) ;
#63900=CARTESIAN_POINT ( 'NONE',  ( 4.220049686691934809, 10.18810118749999916, 80.68750000204836681 ) ) ;
#63913=CARTESIAN_POINT ( 'NONE',  ( -4.220049686691937474, -10.18810118749999738, 75.81250000204838102 ) ) ;
#63928=CARTESIAN_POINT ( 'NONE',  ( -4.220049686691937474, -10.18810118749999738, 72.43750000204838102 ) ) ;
#63946=( BOUNDED_CURVE ( )  B_SPLINE_CURVE ( 2, ( #21364, #56093, #55722, #4037, #16437, #26268, #49288, #27031, #67025 ),
 .UNSPECIFIED., .F., .F. ) 
 B_SPLINE_CURVE_WITH_KNOTS ( ( 3, 2, 2, 2, 3 ),
 ( 0.1176470588235294795, 0.1213235294117647745, 0.1250000000000000833, 0.1286764705882353643, 0.1323529411764706731 ),
 .UNSPECIFIED. ) 
 CURVE ( )  GEOMETRIC_REPRESENTATION_ITEM ( )  RATIONAL_B_SPLINE_CURVE ( ( 0.9999999999999985567, 0.9238795325112881818, 1.000000000000000000, 0.9238795325112867385, 1.000000000000000000, 0.9238795325112867385, 1.000000000000000000, 0.9238795325112849621, 1.000000000000001776 ) ) 
 REPRESENTATION_ITEM ( '' )  );
#63973=CYLINDRICAL_SURFACE ( 'NONE', #26041, 11.00000000000000000 ) ;
#63989=CARTESIAN_POINT ( 'NONE',  ( 4.556349186104045934, 11.00000000000000000, 81.71875000409677625 ) ) ;
#63992=ORIENTED_EDGE ( 'NONE', *, *, #66141, .F. ) ;
#63993=CARTESIAN_POINT ( 'NONE',  ( -10.66427519835108129, 0.9491272587611292444, 117.8040744609134265 ) ) ;
#63994=CARTESIAN_POINT ( 'NONE',  ( -10.18810118749999738, -4.220049686691941915, 102.2500000020483952 ) ) ;
#64011=CARTESIAN_POINT ( 'NONE',  ( 10.18810118749999916, 4.220049686691935698, 95.87500000204838102 ) ) ;
#64018=CARTESIAN_POINT ( 'NONE',  ( -10.18810118749999916, 0.000000000000000000, 77.03125000204836681 ) ) ;
#64026=CARTESIAN_POINT ( 'NONE',  ( -6.238412754330611322E-16, 10.18810118749999916, 88.28125000204836681 ) ) ;
#64036=CARTESIAN_POINT ( 'NONE',  ( 10.18810118750000093, -4.220049686691933921, 76.18750000204839523 ) ) ;
#64040=CARTESIAN_POINT ( 'NONE',  ( 4.556349186104052151, -10.99999999999999822, 112.4687499999999858 ) ) ;
#64052=CARTESIAN_POINT ( 'NONE',  ( 4.220049686691934809, 10.18810118749999916, 68.68750000204838102 ) ) ;
#64055=CARTESIAN_POINT ( 'NONE',  ( 11.00000000000000355, -4.556349186104045046, 82.65625000000001421 ) ) ;
#64065=ADVANCED_FACE ( 'NONE', ( #70338 ), #7330, .F. ) ;
#64083=CARTESIAN_POINT ( 'NONE',  ( -11.00000000000000000, 0.000000000000000000, 67.18750000409676204 ) ) ;
#64093=AXIS2_PLACEMENT_3D ( 'NONE', #40582, #56455, #11911 ) ;
#64095=CARTESIAN_POINT ( 'NONE',  ( 4.220049686691941027, -10.18810118749999738, 110.5000000020483810 ) ) ;
#64133=CARTESIAN_POINT ( 'NONE',  ( 1.871523826299183495E-15, -10.18810118749999916, 86.03125000204836681 ) ) ;
#64135=CARTESIAN_POINT ( 'NONE',  ( 7.778174593052023411, -7.778174593052021635, 100.5625000000000000 ) ) ;
#64163=PLANE ( 'NONE',  #27908 ) ;
#64170=CARTESIAN_POINT ( 'NONE',  ( 11.00000000000000000, 4.556349186104045934, 87.53125000409676204 ) ) ;
#64177=AXIS2_PLACEMENT_3D ( 'NONE', #66400, #31706, #44517 ) ;
#64181=CARTESIAN_POINT ( 'NONE',  ( -11.00000000000000000, 0.000000000000000000, 81.99999999999998579 ) ) ;
#64192=CARTESIAN_POINT ( 'NONE',  ( 11.00000000000000000, 1.347111479062088405E-15, 90.43750000409676204 ) ) ;
#64195=CARTESIAN_POINT ( 'NONE',  ( 10.18810118749999916, 1.247682550866122264E-15, 92.78125000204836681 ) ) ;
#64198=DIRECTION ( 'NONE',  ( -0.7071067811865401342, 0.000000000000000000, -0.7071067811865549002 ) ) ;
#64201=CARTESIAN_POINT ( 'NONE',  ( -4.220049686691937474, -10.18810118749999738, 105.4375000020483668 ) ) ;
#64209=CARTESIAN_POINT ( 'NONE',  ( 7.204075437095966983, 7.204075437095967871, 103.4687500020483668 ) ) ;
#64223=CARTESIAN_POINT ( 'NONE',  ( 1.871523826299183495E-15, -10.18810118749999916, 107.0312500020483810 ) ) ;
#64229=ADVANCED_FACE ( 'NONE', ( #12608 ), #53723, .T. ) ;
#64233=ORIENTED_EDGE ( 'NONE', *, *, #36248, .T. ) ;
#64240=CARTESIAN_POINT ( 'NONE',  ( -6.735557395310442023E-16, 11.00000000000000000, 72.81250000409677625 ) ) ;
#64241=CARTESIAN_POINT ( 'NONE',  ( 11.00000000000000000, 4.556349186104045934, 117.3437500000000000 ) ) ;
#64248=CARTESIAN_POINT ( 'NONE',  ( 10.99999999999999467, 11.00000000000000355, 41.99999999999999289 ) ) ;
#64254=CARTESIAN_POINT ( 'NONE',  ( 4.556349186104051263, -10.99999999999999822, 103.6562500040967905 ) ) ;
#64256=CARTESIAN_POINT ( 'NONE',  ( -11.00000000000005151, 4.556349186103993532, 95.59375000409677625 ) ) ;
#64266=CARTESIAN_POINT ( 'NONE',  ( -11.00000000000000000, 0.000000000000000000, 98.68750000409677625 ) ) ;
#64267=VERTEX_POINT ( 'NONE', #12968 ) ;
#64270=LINE ( 'NONE', #18983, #60396 ) ;
#64274=CARTESIAN_POINT ( 'NONE',  ( 10.18810118749999916, 4.220049686691935698, 80.50000000204839523 ) ) ;
#64279=CARTESIAN_POINT ( 'NONE',  ( 10.18810118749999916, 4.220049686691935698, 107.8750000020483668 ) ) ;
#64287=CARTESIAN_POINT ( 'NONE',  ( -10.18810118749999916, 4.220049686691934809, 76.93750000204838102 ) ) ;
#64299=CARTESIAN_POINT ( 'NONE',  ( 7.204075437095968759, -7.204075437095966983, 71.21875000204836681 ) ) ;
#64300=EDGE_CURVE ( 'NONE', #63637, #49057, #32582, .T. ) ;
#64349=VECTOR ( 'NONE', #8428, 1000.000000000000000 ) ;
#64363=EDGE_LOOP ( 'NONE', ( #71683, #19643, #32735, #69513 ) ) ;
#64365=CARTESIAN_POINT ( 'NONE',  ( 10.18810118749999916, 1.247682550866122264E-15, 102.9062500020483810 ) ) ;
#64374=ORIENTED_EDGE ( 'NONE', *, *, #44076, .F. ) ;
#64383=CARTESIAN_POINT ( 'NONE',  ( -4.220049686691937474, -10.18810118749999738, 93.81250000204838102 ) ) ;
#64386=EDGE_LOOP ( 'NONE', ( #46839, #69559, #64233, #34129 ) ) ;
#64390=CARTESIAN_POINT ( 'NONE',  ( 10.18810118749999916, 4.220049686691935698, 80.87500000204836681 ) ) ;
#64396=CARTESIAN_POINT ( 'NONE',  ( 4.556349186104045934, 11.00000000000000000, 89.21875000409679046 ) ) ;
#64398=CARTESIAN_POINT ( 'NONE',  ( -10.18810118749999916, 0.000000000000000000, 88.65625000204838102 ) ) ;
#64408=CARTESIAN_POINT ( 'NONE',  ( 10.18810118749999916, 4.220049686691935698, 73.37500000204838102 ) ) ;
#64413=CARTESIAN_POINT ( 'NONE',  ( 11.00000000000000355, -4.556349186104044158, 93.34375000409677625 ) ) ;
#64426=CARTESIAN_POINT ( 'NONE',  ( -4.220049686691937474, -10.18810118749999738, 67.93750000204838102 ) ) ;
#64429=CARTESIAN_POINT ( 'NONE',  ( 7.778174593052021635, 7.778174593052023411, 81.43750000000000000 ) ) ;
#64432=CARTESIAN_POINT ( 'NONE',  ( 2.020667218593132706E-15, -11.00000000000000000, 113.8749999999999858 ) ) ;
#64456=CARTESIAN_POINT ( 'NONE',  ( 2.020667218593132706E-15, -11.00000000000000000, 67.56250000409677625 ) ) ;
#64469=CARTESIAN_POINT ( 'NONE',  ( -6.238412754330611322E-16, 10.18810118749999916, 112.6562500020483810 ) ) ;
#64472=EDGE_CURVE ( 'NONE', #50184, #26210, #57449, .T. ) ;
#64474=FACE_OUTER_BOUND ( 'NONE', #26328, .T. ) ;
#64508=CARTESIAN_POINT ( 'NONE',  ( -6.238412754330611322E-16, 10.18810118749999916, 85.28125000204836681 ) ) ;
#64511=CARTESIAN_POINT ( 'NONE',  ( -11.00000000000000000, 0.000000000000000000, 99.99999999999998579 ) ) ;
#64538=CARTESIAN_POINT ( 'NONE',  ( -4.556349186104045934, 11.00000000000000000, 87.90625000409677625 ) ) ;
#64541=CARTESIAN_POINT ( 'NONE',  ( -11.00000000000000000, 0.000000000000000000, 101.5000000000000000 ) ) ;
#64564=CARTESIAN_POINT ( 'NONE',  ( 4.220049686691934809, 10.18810118749999916, 90.06250000204838102 ) ) ;
#64570=CARTESIAN_POINT ( 'NONE',  ( -10.18810118749999738, -4.220049686691941915, 99.25000000204838102 ) ) ;
#64573=ORIENTED_EDGE ( 'NONE', *, *, #3084, .F. ) ;
#64578=CARTESIAN_POINT ( 'NONE',  ( -4.220049686691935698, 10.18810118749999916, 106.7500000020483668 ) ) ;
#64591=CARTESIAN_POINT ( 'NONE',  ( -4.556349186104045934, 11.00000000000000000, 68.21875000000000000 ) ) ;
#64594=( BOUNDED_CURVE ( )  B_SPLINE_CURVE ( 2, ( #41233, #68781, #23129, #1257, #64240, #46141, #35578, #18588, #51805 ),
 .UNSPECIFIED., .F., .F. ) 
 B_SPLINE_CURVE_WITH_KNOTS ( ( 3, 2, 2, 2, 3 ),
 ( 0.8529411764705882026, 0.8566176470588234837, 0.8602941176470588758, 0.8639705882352941568, 0.8676470588235294379 ),
 .UNSPECIFIED. ) 
 CURVE ( )  GEOMETRIC_REPRESENTATION_ITEM ( )  RATIONAL_B_SPLINE_CURVE ( ( 1.000000000000000000, 0.9238795325112867385, 1.000000000000000000, 0.9238795325112867385, 1.000000000000000000, 0.9238795325112867385, 1.000000000000000000, 0.9238795325112867385, 1.000000000000000000 ) ) 
 REPRESENTATION_ITEM ( '' )  );
#64596=CARTESIAN_POINT ( 'NONE',  ( -10.18810118749999916, 0.000000000000000000, 106.6562500020483668 ) ) ;
#64615=CARTESIAN_POINT ( 'NONE',  ( -4.220049686691935698, 10.18810118749999916, 70.75000000204836681 ) ) ;
#64626=CARTESIAN_POINT ( 'NONE',  ( 4.556349186104045934, 11.00000000000000000, 107.2187500040967905 ) ) ;
#64629=CARTESIAN_POINT ( 'NONE',  ( 10.99999999999987033, -4.556349186104176496, 108.1562500000000000 ) ) ;
#64644=CARTESIAN_POINT ( 'NONE',  ( -10.18810118749999916, 4.220049686691934809, 84.06250000204838102 ) ) ;
#64648=CARTESIAN_POINT ( 'NONE',  ( -7.204075437095965206, -7.204075437095968759, 110.2187500020483810 ) ) ;
#64650=CARTESIAN_POINT ( 'NONE',  ( 11.00000000000000000, 1.347111479062088405E-15, 118.0000000000000000 ) ) ;
#64654=CARTESIAN_POINT ( 'NONE',  ( -4.220049686691935698, 10.18810118749999916, 70.75000000204836681 ) ) ;
#64665=CARTESIAN_POINT ( 'NONE',  ( -10.18810118749999916, 4.220049686691934809, 69.06250000204839523 ) ) ;
#64691=CARTESIAN_POINT ( 'NONE',  ( 16.00000000000000711, -16.00000000000000000, 20.00000000000000000 ) ) ;
#64700=CARTESIAN_POINT ( 'NONE',  ( -11.00000000000000000, 0.000000000000000000, 116.6875000040967763 ) ) ;
#64714=DIRECTION ( 'NONE',  ( -1.000000000000000000, 0.000000000000000000, 0.000000000000000000 ) ) ;
#64731=CARTESIAN_POINT ( 'NONE',  ( 1.917649949088270800, 10.81880817070227607, 117.5534000801073233 ) ) ;
#64732=CARTESIAN_POINT ( 'NONE',  ( 4.220049686691934809, 10.18810118749999916, 103.1875000020483810 ) ) ;
#64733=CARTESIAN_POINT ( 'NONE',  ( -6.735557395310442023E-16, 11.00000000000000000, 86.31250000409676204 ) ) ;
#64747=CARTESIAN_POINT ( 'NONE',  ( 10.18810118749999916, 1.247682550866122264E-15, 95.78125000204836681 ) ) ;
#64751=DIRECTION ( 'NONE',  ( -0.000000000000000000, -0.000000000000000000, -1.000000000000000000 ) ) ;
#64753=CARTESIAN_POINT ( 'NONE',  ( -6.238412754330611322E-16, 10.18810118749999916, 73.65625000204836681 ) ) ;
#64759=CARTESIAN_POINT ( 'NONE',  ( 10.18810118750000093, -4.220049686691933921, 90.81250000204838102 ) ) ;
#64767=EDGE_CURVE ( 'NONE', #62018, #3255, #4565, .T. ) ;
#64769=CARTESIAN_POINT ( 'NONE',  ( -4.220049686691935698, 10.18810118749999916, 75.25000000204836681 ) ) ;
#64787=CARTESIAN_POINT ( 'NONE',  ( -10.18810118749999916, 4.220049686691934809, 67.56250000204836681 ) ) ;
#64790=CARTESIAN_POINT ( 'NONE',  ( -6.735557395310442023E-16, 11.00000000000000000, 77.12499999999998579 ) ) ;
#64816=CARTESIAN_POINT ( 'NONE',  ( -11.00000000000000000, 4.556349186104045934, 68.59375000409677625 ) ) ;
#64827=CARTESIAN_POINT ( 'NONE',  ( 4.220049686691941027, -10.18810118749999738, 112.0000000020483810 ) ) ;
#64867=CARTESIAN_POINT ( 'NONE',  ( 7.204075437095966983, 7.204075437095967871, 86.59375000204836681 ) ) ;
#64869=CARTESIAN_POINT ( 'NONE',  ( -7.778174593052020747, -7.778174593052023411, 94.18750000000000000 ) ) ;
#64870=CARTESIAN_POINT ( 'NONE',  ( -10.99999999999989164, -4.556349186104158733, 104.5937500000000000 ) ) ;
#64875=CARTESIAN_POINT ( 'NONE',  ( 4.556349186104045934, 11.00000000000000000, 105.7187500040967763 ) ) ;
#64885=CYLINDRICAL_SURFACE ( 'NONE', #57067, 11.00000000000000000 ) ;
#64893=CARTESIAN_POINT ( 'NONE',  ( -7.778174593052023411, 7.778174593052023411, 99.81250000000000000 ) ) ;
#64898=CARTESIAN_POINT ( 'NONE',  ( -11.00000000000000000, 4.556349186104045934, 88.09375000409677625 ) ) ;
#64911=ORIENTED_EDGE ( 'NONE', *, *, #16525, .F. ) ;
#64919=CARTESIAN_POINT ( 'NONE',  ( 4.220049686691941027, -10.18810118749999738, 91.00000000204836681 ) ) ;
#64926=CARTESIAN_POINT ( 'NONE',  ( -6.238412754330611322E-16, 10.18810118749999916, 100.2812500020483810 ) ) ;
#64935=CARTESIAN_POINT ( 'NONE',  ( -10.18810118749999738, -4.220049686691941915, 95.12500000204836681 ) ) ;
#64950=CARTESIAN_POINT ( 'NONE',  ( -7.204075437095965206, -7.204075437095968759, 105.3437500020483810 ) ) ;
#64965=CARTESIAN_POINT ( 'NONE',  ( -11.00000000000000000, 4.556349186104045934, 113.4062500000000000 ) ) ;
#64979=CARTESIAN_POINT ( 'NONE',  ( -6.735557395310442023E-16, 11.00000000000000000, 102.8125000040967763 ) ) ;
#64982=CARTESIAN_POINT ( 'NONE',  ( -4.556349186104045934, 11.00000000000000000, 71.21875000000000000 ) ) ;
#64983=CARTESIAN_POINT ( 'NONE',  ( -6.735557395310442023E-16, 11.00000000000000000, 71.31250000409677625 ) ) ;
#64985=DIRECTION ( 'NONE',  ( -1.000000000000000000, 0.000000000000000000, 0.000000000000000000 ) ) ;
#64993=CARTESIAN_POINT ( 'NONE',  ( -4.556349186104048599, -10.99999999999999822, 67.46875000409677625 ) ) ;
#65002=CARTESIAN_POINT ( 'NONE',  ( -4.220049686691935698, 10.18810118749999916, 106.7500000020483668 ) ) ;
#65005=CARTESIAN_POINT ( 'NONE',  ( 11.00000000000000000, 1.347111479062088405E-15, 109.9375000040967763 ) ) ;
#65010=CARTESIAN_POINT ( 'NONE',  ( 10.18810118749999916, 1.247682550866122264E-15, 73.28125000204838102 ) ) ;
#65020=CARTESIAN_POINT ( 'NONE',  ( -10.18810118749999738, -4.220049686691941915, 114.6250000020483810 ) ) ;
#65052=FACE_OUTER_BOUND ( 'NONE', #54973, .T. ) ;
#65068=AXIS2_PLACEMENT_3D ( 'NONE', #72866, #55527, #33265 ) ;
#65075=CARTESIAN_POINT ( 'NONE',  ( 11.00000000000000000, 1.347111479062088405E-15, 105.4375000040967763 ) ) ;
#65086=CARTESIAN_POINT ( 'NONE',  ( 10.18810118750000093, -4.220049686691933921, 96.81250000204839523 ) ) ;
#65102=CARTESIAN_POINT ( 'NONE',  ( -7.204075437095965206, -7.204075437095968759, 90.71875000204838102 ) ) ;
#65108=CARTESIAN_POINT ( 'NONE',  ( -10.18810118749999738, -4.220049686691941915, 75.62500000204838102 ) ) ;
#65116=CARTESIAN_POINT ( 'NONE',  ( 4.220049686691941027, -10.18810118749999738, 87.62500000204836681 ) ) ;
#65128=CARTESIAN_POINT ( 'NONE',  ( 7.204075437095968759, -7.204075437095966983, 68.59375000204836681 ) ) ;
#65148=CARTESIAN_POINT ( 'NONE',  ( -11.00000000000000000, 0.000000000000000000, 75.99999999999998579 ) ) ;
#65158=CARTESIAN_POINT ( 'NONE',  ( -7.778174593052023411, 7.778174593052023411, 116.5000000040967905 ) ) ;
#65167=FACE_OUTER_BOUND ( 'NONE', #73125, .T. ) ;
#65172=ORIENTED_EDGE ( 'NONE', *, *, #69703, .F. ) ;
#65173=CARTESIAN_POINT ( 'NONE',  ( -10.18810118749999916, 0.000000000000000000, 84.53125000204836681 ) ) ;
#65175=CARTESIAN_POINT ( 'NONE',  ( -11.00000000000000000, 4.556349186104045934, 71.59375000409676204 ) ) ;
#65186=CARTESIAN_POINT ( 'NONE',  ( -4.220049686691935698, 10.18810118749999916, 109.7500000020483810 ) ) ;
#65198=EDGE_CURVE ( 'NONE', #3255, #74244, #35486, .T. ) ;
#65207=EDGE_CURVE ( 'NONE', #15625, #68592, #7418, .T. ) ;
#65223=ORIENTED_EDGE ( 'NONE', *, *, #50105, .F. ) ;
#65229=CARTESIAN_POINT ( 'NONE',  ( 10.18810118749999916, 1.247682550866122264E-15, 84.90625000204838102 ) ) ;
#65231=CARTESIAN_POINT ( 'NONE',  ( 11.00000000000000355, -4.556349186104045046, 96.15624999999998579 ) ) ;
#65238=CARTESIAN_POINT ( 'NONE',  ( -11.00000000000000000, 0.000000000000000000, 78.99999999999998579 ) ) ;
#65254=EDGE_CURVE ( 'NONE', #34878, #56876, #36661, .T. ) ;
#65263=CARTESIAN_POINT ( 'NONE',  ( -7.778174593052023411, 7.778174593052023411, 88.00000000409677625 ) ) ;
#65290=CARTESIAN_POINT ( 'NONE',  ( -6.238412754330611322E-16, 10.18810118749999916, 93.15625000204836681 ) ) ;
#65296=CARTESIAN_POINT ( 'NONE',  ( 1.871523826299183495E-15, -10.18810118749999916, 99.53125000204838102 ) ) ;
#65304=CARTESIAN_POINT ( 'NONE',  ( 10.18810118749999916, 4.220049686691935698, 98.87500000204836681 ) ) ;
#65322=CARTESIAN_POINT ( 'NONE',  ( 4.220049686691941027, -10.18810118749999738, 107.1250000020483810 ) ) ;
#65335=CARTESIAN_POINT ( 'NONE',  ( -6.735557395310442023E-16, 11.00000000000000000, 74.12500000000000000 ) ) ;
#65342=CARTESIAN_POINT ( 'NONE',  ( 11.00000000000000355, -4.556349186104045046, 111.1562499999999858 ) ) ;
#65355=CARTESIAN_POINT ( 'NONE',  ( 11.00000000000000355, -4.556349186104045046, 103.8437500040967763 ) ) ;
#65361=CYLINDRICAL_SURFACE ( 'NONE', #59277, 11.00000000000000000 ) ;
#65362=( BOUNDED_CURVE ( )  B_SPLINE_CURVE ( 2, ( #27134, #20723, #66755, #26760, #9795, #72794, #21102, #44125, #67133 ),
 .UNSPECIFIED., .F., .F. ) 
 B_SPLINE_CURVE_WITH_KNOTS ( ( 3, 2, 2, 2, 3 ),
 ( 0.08823529411764710617, 0.09191176470588241498, 0.09558823529411769604, 0.09926470588235300485, 0.1029411764705882998 ),
 .UNSPECIFIED. ) 
 CURVE ( )  GEOMETRIC_REPRESENTATION_ITEM ( )  RATIONAL_B_SPLINE_CURVE ( ( 0.9999999999999991118, 0.9238795325112876267, 1.000000000000000000, 0.9238795325112867385, 1.000000000000000000, 0.9238795325112867385, 1.000000000000000000, 0.9238795325112852952, 1.000000000000001332 ) ) 
 REPRESENTATION_ITEM ( '' )  );
#65377=CARTESIAN_POINT ( 'NONE',  ( 7.204075437095966983, 7.204075437095967871, 110.9687500020483810 ) ) ;
#65385=CARTESIAN_POINT ( 'NONE',  ( 10.18810118750000093, -4.220049686691933033, 71.68750000204838102 ) ) ;
#65398=CARTESIAN_POINT ( 'NONE',  ( 10.18810118749999916, 4.220049686691935698, 115.3750000020483810 ) ) ;
#65412=ORIENTED_EDGE ( 'NONE', *, *, #35325, .T. ) ;
#65459=CARTESIAN_POINT ( 'NONE',  ( -11.00000000000003730, -4.556349186104013960, 115.0937500000000142 ) ) ;
#65464=CARTESIAN_POINT ( 'NONE',  ( -7.204075437095967871, 7.204075437095967871, 92.96875000204838102 ) ) ;
#65465=CARTESIAN_POINT ( 'NONE',  ( 4.556349186104045934, 11.00000000000000000, 86.21875000409680467 ) ) ;
#65476=CARTESIAN_POINT ( 'NONE',  ( -11.00000000000000000, 0.000000000000000000, 75.99999999999998579 ) ) ;
#65480=CARTESIAN_POINT ( 'NONE',  ( -10.18810118749999738, -4.220049686691941915, 89.12500000204836681 ) ) ;
#65483=ORIENTED_EDGE ( 'NONE', *, *, #3618, .F. ) ;
#65487=CARTESIAN_POINT ( 'NONE',  ( 10.18810118749999916, 4.220049686691935698, 74.87500000204836681 ) ) ;
#65494=CARTESIAN_POINT ( 'NONE',  ( -4.220049686691937474, -10.18810118749999738, 82.93750000204838102 ) ) ;
#65499=AXIS2_PLACEMENT_3D ( 'NONE', #69472, #39318, #68354 ) ;
#65501=CARTESIAN_POINT ( 'NONE',  ( 11.00000000000000000, 1.347111479062088405E-15, 118.0000000000000000 ) ) ;
#65505=CARTESIAN_POINT ( 'NONE',  ( -6.238412754330611322E-16, 10.18810118749999916, 67.65625000204836681 ) ) ;
#65524=CARTESIAN_POINT ( 'NONE',  ( 4.556349186104045934, 11.00000000000000000, 114.5312500000000000 ) ) ;
#65528=CARTESIAN_POINT ( 'NONE',  ( 11.00000000000000000, 1.347111479062088405E-15, 76.74999999999998579 ) ) ;
#65538=CARTESIAN_POINT ( 'NONE',  ( 7.778174593052021635, 7.778174593052023411, 114.6250000040967763 ) ) ;
#65552=CARTESIAN_POINT ( 'NONE',  ( 7.204075437095966983, 7.204075437095967871, 88.46875000204838102 ) ) ;
#65553=CARTESIAN_POINT ( 'NONE',  ( -10.18810118749999916, 0.000000000000000000, 115.6562500020483810 ) ) ;
#65562=CARTESIAN_POINT ( 'NONE',  ( -11.00000000000000000, 0.000000000000000000, 118.0000000000000000 ) ) ;
#65564=CARTESIAN_POINT ( 'NONE',  ( -4.220049686691935698, 10.18810118749999916, 105.2500000020483810 ) ) ;
#65596=CARTESIAN_POINT ( 'NONE',  ( -7.778174593052020747, -7.778174593052023411, 98.68749999999998579 ) ) ;
#65604=CARTESIAN_POINT ( 'NONE',  ( -6.238412754330611322E-16, 10.18810118749999916, 79.28125000204836681 ) ) ;
#65606=CARTESIAN_POINT ( 'NONE',  ( 11.00000000000000000, 1.347111479062088405E-15, 94.74999999999998579 ) ) ;
#65614=ADVANCED_FACE ( 'NONE', ( #52803 ), #24493, .T. ) ;
#65636=CARTESIAN_POINT ( 'NONE',  ( -7.778174593052023411, 7.778174593052023411, 79.00000000409676204 ) ) ;
#65647=ORIENTED_EDGE ( 'NONE', *, *, #5325, .F. ) ;
#65659=CARTESIAN_POINT ( 'NONE',  ( -4.220049686691937474, -10.18810118749999738, 83.31250000204836681 ) ) ;
#65664=CARTESIAN_POINT ( 'NONE',  ( 7.204075437095968759, -7.204075437095966983, 101.2187500020483668 ) ) ;
#65673=CARTESIAN_POINT ( 'NONE',  ( 10.18810118750000093, -4.220049686691933921, 98.68750000204838102 ) ) ;
#65689=CARTESIAN_POINT ( 'NONE',  ( -4.220049686691937474, -10.18810118749999738, 96.43750000204836681 ) ) ;
#65706=CARTESIAN_POINT ( 'NONE',  ( 11.00000000000000355, -4.556349186104045046, 114.1562499999999716 ) ) ;
#65711=CARTESIAN_POINT ( 'NONE',  ( 11.00000000000005329, -4.556349186103991755, 102.1562499999999858 ) ) ;
#65716=ORIENTED_EDGE ( 'NONE', *, *, #25808, .T. ) ;
#65719=CARTESIAN_POINT ( 'NONE',  ( -11.00000000000000000, 4.556349186104045934, 103.0937500040968047 ) ) ;
#65720=VECTOR ( 'NONE', #51957, 1000.000000000000000 ) ;
#65724=CARTESIAN_POINT ( 'NONE',  ( -11.00000000000000000, 0.000000000000000000, 71.68750000409676204 ) ) ;
#65730=EDGE_CURVE ( 'NONE', #26634, #39873, #19934, .T. ) ;
#65738=EDGE_CURVE ( 'NONE', #62341, #68592, #54568, .T. ) ;
#65745=CARTESIAN_POINT ( 'NONE',  ( 2.020667218593132706E-15, -11.00000000000000000, 70.56250000409677625 ) ) ;
#65746=CARTESIAN_POINT ( 'NONE',  ( -6.238412754330611322E-16, 10.18810118749999916, 112.6562500020483810 ) ) ;
#65752=DIRECTION ( 'NONE',  ( -0.000000000000000000, -0.000000000000000000, -1.000000000000000000 ) ) ;
#65753=CARTESIAN_POINT ( 'NONE',  ( -10.18810118749999738, -4.220049686691941915, 71.12500000204836681 ) ) ;
#65767=CARTESIAN_POINT ( 'NONE',  ( 7.204075437095966983, 7.204075437095967871, 113.9687500020483810 ) ) ;
#65782=CARTESIAN_POINT ( 'NONE',  ( -6.238412754330611322E-16, 10.18810118749999916, 116.7812500020483810 ) ) ;
#65792=( BOUNDED_CURVE ( )  B_SPLINE_CURVE ( 2, ( #6192, #16737, #57885, #22775, #23156, #63894, #5080, #52213, #17120 ),
 .UNSPECIFIED., .F., .F. ) 
 B_SPLINE_CURVE_WITH_KNOTS ( ( 3, 2, 2, 2, 3 ),
 ( 0.02941176470588237335, 0.03308823529411766828, 0.03676470588235296322, 0.04044117647058826509, 0.04411764705882356002 ),
 .UNSPECIFIED. ) 
 CURVE ( )  GEOMETRIC_REPRESENTATION_ITEM ( )  RATIONAL_B_SPLINE_CURVE ( ( 0.9999999999999995559, 0.9238795325112871826, 1.000000000000000000, 0.9238795325112867385, 1.000000000000000000, 0.9238795325112867385, 1.000000000000000000, 0.9238795325112861834, 1.000000000000000666 ) ) 
 REPRESENTATION_ITEM ( '' )  );
#65796=CARTESIAN_POINT ( 'NONE',  ( 0.000000000000000000, 0.000000000000000000, 118.0000000000000000 ) ) ;
#65799=DIRECTION ( 'NONE',  ( -0.000000000000000000, -0.000000000000000000, -1.000000000000000000 ) ) ;
#65808=EDGE_LOOP ( 'NONE', ( #43215, #49126, #34660, #42762 ) ) ;
#65829=CARTESIAN_POINT ( 'NONE',  ( 7.204075437095968759, -7.204075437095966983, 98.21875000204838102 ) ) ;
#65830=CYLINDRICAL_SURFACE ( 'NONE', #74260, 11.00000000000000000 ) ;
#65844=CARTESIAN_POINT ( 'NONE',  ( -6.238412754330611322E-16, 10.18810118749999916, 87.15625000204838102 ) ) ;
#65850=CARTESIAN_POINT ( 'NONE',  ( 1.871523826299183495E-15, -10.18810118749999916, 72.90625000204836681 ) ) ;
#65859=CARTESIAN_POINT ( 'NONE',  ( 7.204075437095968759, -7.204075437095966983, 84.71875000204836681 ) ) ;
#65869=CARTESIAN_POINT ( 'NONE',  ( -7.204075437095965206, -7.204075437095968759, 69.71875000204836681 ) ) ;
#65886=( BOUNDED_CURVE ( )  B_SPLINE_CURVE ( 2, ( #58701, #24711, #47723, #7012, #19062, #25076, #53775, #2084, #19422 ),
 .UNSPECIFIED., .F., .F. ) 
 B_SPLINE_CURVE_WITH_KNOTS ( ( 3, 2, 2, 2, 3 ),
 ( 0.6323529411764704511, 0.6360294117647057321, 0.6397058823529410132, 0.6433823529411764053, 0.6470588235294116863 ),
 .UNSPECIFIED. ) 
 CURVE ( )  GEOMETRIC_REPRESENTATION_ITEM ( )  RATIONAL_B_SPLINE_CURVE ( ( 1.000000000000002220, 0.9238795325112844070, 1.000000000000000000, 0.9238795325112867385, 1.000000000000000000, 0.9238795325112867385, 1.000000000000000000, 0.9238795325112890700, 0.9999999999999976685 ) ) 
 REPRESENTATION_ITEM ( '' )  );
#65893=CARTESIAN_POINT ( 'NONE',  ( 2.020667218593132706E-15, -11.00000000000000000, 74.87499999999998579 ) ) ;
#65903=CARTESIAN_POINT ( 'NONE',  ( -7.778174593052020747, -7.778174593052023411, 115.3750000040967905 ) ) ;
#65906=LINE ( 'NONE', #37250, #54281 ) ;
#65912=ORIENTED_EDGE ( 'NONE', *, *, #35772, .F. ) ;
#65914=( BOUNDED_CURVE ( )  B_SPLINE_CURVE ( 2, ( #5502, #56814, #45112, #69615, #40196, #51511, #74150, #57567, #63198 ),
 .UNSPECIFIED., .F., .F. ) 
 B_SPLINE_CURVE_WITH_KNOTS ( ( 3, 2, 2, 2, 3 ),
 ( 0.8235294117647057321, 0.8272058823529410132, 0.8308823529411764053, 0.8345588235294117974, 0.8382352941176470784 ),
 .UNSPECIFIED. ) 
 CURVE ( )  GEOMETRIC_REPRESENTATION_ITEM ( )  RATIONAL_B_SPLINE_CURVE ( ( 1.000000000000002220, 0.9238795325112844070, 1.000000000000000000, 0.9238795325112867385, 1.000000000000000000, 0.9238795325112867385, 1.000000000000000000, 0.9238795325112867385, 1.000000000000000000 ) ) 
 REPRESENTATION_ITEM ( '' )  );
#65920=CARTESIAN_POINT ( 'NONE',  ( -7.204075437095965206, -7.204075437095968759, 87.71875000204836681 ) ) ;
#65921=CARTESIAN_POINT ( 'NONE',  ( -10.18810118749999916, 4.220049686691934809, 115.5625000020483810 ) ) ;
#65929=EDGE_CURVE ( 'NONE', #33088, #24157, #27461, .T. ) ;
#65935=CARTESIAN_POINT ( 'NONE',  ( -10.18810118749999738, -4.220049686691941915, 110.1250000020483810 ) ) ;
#65948=CARTESIAN_POINT ( 'NONE',  ( 11.00000000000000000, 1.347111479062088405E-15, 118.0000000000000000 ) ) ;
#65974=CARTESIAN_POINT ( 'NONE',  ( 7.204075437095966983, 7.204075437095967871, 77.59375000204838102 ) ) ;
#65977=CARTESIAN_POINT ( 'NONE',  ( -7.778174593052023411, 7.778174593052023411, 92.31249999999998579 ) ) ;
#65978=CARTESIAN_POINT ( 'NONE',  ( -7.778174593052020747, -7.778174593052023411, 86.68749999999998579 ) ) ;
#65984=VECTOR ( 'NONE', #54542, 1000.000000000000000 ) ;
#66006=CARTESIAN_POINT ( 'NONE',  ( -6.735557395310442023E-16, 11.00000000000000000, 80.31250000409677625 ) ) ;
#66023=CARTESIAN_POINT ( 'NONE',  ( 7.204075437095968759, -7.204075437095966983, 77.21875000204836681 ) ) ;
#66030=EDGE_CURVE ( 'NONE', #43963, #1423, #21797, .T. ) ;
#66033=CARTESIAN_POINT ( 'NONE',  ( 10.18810118750000093, -4.220049686691933921, 83.68750000204836681 ) ) ;
#66035=ADVANCED_FACE ( 'NONE', ( #10494 ), #33529, .T. ) ;
#66039=CARTESIAN_POINT ( 'NONE',  ( -4.220049686691935698, 10.18810118749999916, 101.8750000020483810 ) ) ;
#66048=CARTESIAN_POINT ( 'NONE',  ( 7.204075437095968759, -7.204075437095966983, 100.0937500020483668 ) ) ;
#66061=ORIENTED_EDGE ( 'NONE', *, *, #10652, .F. ) ;
#66063=CARTESIAN_POINT ( 'NONE',  ( 4.220049686691941027, -10.18810118749999738, 98.12500000204838102 ) ) ;
#66073=ORIENTED_EDGE ( 'NONE', *, *, #61774, .T. ) ;
#66080=CARTESIAN_POINT ( 'NONE',  ( -7.778174593052020747, -7.778174593052023411, 91.37500000409677625 ) ) ;
#66081=CARTESIAN_POINT ( 'NONE',  ( 4.556349186104051263, -10.99999999999999822, 113.9687500000000142 ) ) ;
#66094=CARTESIAN_POINT ( 'NONE',  ( -4.556349186104045934, 11.00000000000000000, 101.4062500040967763 ) ) ;
#66097=CARTESIAN_POINT ( 'NONE',  ( -11.00000000000000000, 0.000000000000000000, 89.50000000000000000 ) ) ;
#66102=VECTOR ( 'NONE', #8297, 1000.000000000000000 ) ;
#66110=ORIENTED_EDGE ( 'NONE', *, *, #13996, .F. ) ;
#66117=CARTESIAN_POINT ( 'NONE',  ( 0.000000000000000000, 0.000000000000000000, 118.0000000000000000 ) ) ;
#66118=CARTESIAN_POINT ( 'NONE',  ( 4.220049686691941027, -10.18810118749999738, 106.0000000020483668 ) ) ;
#66125=CARTESIAN_POINT ( 'NONE',  ( -4.220049686691937474, -10.18810118749999738, 71.31250000204836681 ) ) ;
#66127=( BOUNDED_CURVE ( )  B_SPLINE_CURVE ( 2, ( #51046, #21996, #39357, #10316, #74056, #40100, #9946, #51788, #22355 ),
 .UNSPECIFIED., .F., .F. ) 
 B_SPLINE_CURVE_WITH_KNOTS ( ( 3, 2, 2, 2, 3 ),
 ( 0.3823529411764705621, 0.3860294117647058987, 0.3897058823529411242, 0.3933823529411764053, 0.3970588235294116863 ),
 .UNSPECIFIED. ) 
 CURVE ( )  GEOMETRIC_REPRESENTATION_ITEM ( )  RATIONAL_B_SPLINE_CURVE ( ( 1.000000000000000000, 0.9238795325112867385, 1.000000000000000000, 0.9238795325112867385, 1.000000000000000000, 0.9238795325112867385, 1.000000000000000000, 0.9238795325112878487, 0.9999999999999988898 ) ) 
 REPRESENTATION_ITEM ( '' )  );
#66129=CARTESIAN_POINT ( 'NONE',  ( -4.220049686691935698, 10.18810118749999916, 116.8750000020483668 ) ) ;
#66140=CARTESIAN_POINT ( 'NONE',  ( 4.220049686691934809, 10.18810118749999916, 117.0625000020483668 ) ) ;
#66141=EDGE_CURVE ( 'NONE', #18846, #22788, #171, .T. ) ;
#66165=CARTESIAN_POINT ( 'NONE',  ( 4.556349186104045934, 11.00000000000000000, 113.2187500040967763 ) ) ;
#66203=VERTEX_POINT ( 'NONE', #68953 ) ;
#66204=CARTESIAN_POINT ( 'NONE',  ( 0.000000000000000000, 0.000000000000000000, 118.0000000000000000 ) ) ;
#66205=CARTESIAN_POINT ( 'NONE',  ( 4.220049686691934809, 10.18810118749999916, 95.68750000204838102 ) ) ;
#66219=CARTESIAN_POINT ( 'NONE',  ( -4.220049686691935698, 10.18810118749999916, 91.75000000204836681 ) ) ;
#66222=CARTESIAN_POINT ( 'NONE',  ( 16.00000000000000711, -16.00000000000000000, 20.00000000000000000 ) ) ;
#66226=( BOUNDED_CURVE ( )  B_SPLINE_CURVE ( 2, ( #6002, #18427, #30118, #34686, #18800, #40322, #5629 ),
 .UNSPECIFIED., .F., .F. ) 
 B_SPLINE_CURVE_WITH_KNOTS ( ( 3, 2, 2, 3 ),
 ( 0.9705882352941177516, 0.9742647058823530326, 0.9779411764705882026, 0.9803851205147093850 ),
 .UNSPECIFIED. ) 
 CURVE ( )  GEOMETRIC_REPRESENTATION_ITEM ( )  RATIONAL_B_SPLINE_CURVE ( ( 0.9999999999999976685, 0.9238795325112890700, 1.000000000000000000, 0.9238795325112867385, 1.000000000000000000, 0.9493987076219048138, 0.9660721148037704209 ) ) 
 REPRESENTATION_ITEM ( '' )  );
#66235=CARTESIAN_POINT ( 'NONE',  ( 4.220049686691941027, -10.18810118749999738, 86.12500000204836681 ) ) ;
#66269=CARTESIAN_POINT ( 'NONE',  ( 4.556349186104051263, -10.99999999999999822, 70.46874999999998579 ) ) ;
#66274=EDGE_CURVE ( 'NONE', #53484, #36433, #69991, .T. ) ;
#66296=CARTESIAN_POINT ( 'NONE',  ( 7.204075437095968759, -7.204075437095966983, 85.09375000204836681 ) ) ;
#66297=CARTESIAN_POINT ( 'NONE',  ( 7.204075437095966983, 7.204075437095967871, 115.0937500020483810 ) ) ;
#66301=CARTESIAN_POINT ( 'NONE',  ( 7.778174593052023411, -7.778174593052021635, 106.5624999999999858 ) ) ;
#66311=CARTESIAN_POINT ( 'NONE',  ( -6.238412754330611322E-16, 10.18810118749999916, 106.6562500020483810 ) ) ;
#66331=( BOUNDED_CURVE ( )  B_SPLINE_CURVE ( 2, ( #50720, #46178, #74479, #49325, #57525, #72340, #73736, #68084, #16373 ),
 .UNSPECIFIED., .F., .F. ) 
 B_SPLINE_CURVE_WITH_KNOTS ( ( 3, 2, 2, 2, 3 ),
 ( 0.08823529411764712005, 0.09191176470588241498, 0.09558823529411770992, 0.09926470588235300485, 0.1029411764705883137 ),
 .UNSPECIFIED. ) 
 CURVE ( )  GEOMETRIC_REPRESENTATION_ITEM ( )  RATIONAL_B_SPLINE_CURVE ( ( 0.9999999999999988898, 0.9238795325112878487, 1.000000000000000000, 0.9238795325112867385, 1.000000000000000000, 0.9238795325112867385, 1.000000000000000000, 0.9238795325112849621, 1.000000000000001776 ) ) 
 REPRESENTATION_ITEM ( '' )  );
#66336=ORIENTED_EDGE ( 'NONE', *, *, #49321, .F. ) ;
#66350=CARTESIAN_POINT ( 'NONE',  ( 4.220049686691934809, 10.18810118749999916, 82.18750000204836681 ) ) ;
#66353=CARTESIAN_POINT ( 'NONE',  ( 4.556349186104045934, 11.00000000000000000, 96.53125000000000000 ) ) ;
#66365=SPHERICAL_SURFACE ( 'NONE', #72073, 38.34805510287551300 ) ;
#66377=CARTESIAN_POINT ( 'NONE',  ( 11.00000000000000000, 1.347111479062088405E-15, 69.43750000409676204 ) ) ;
#66379=CARTESIAN_POINT ( 'NONE',  ( -11.00000000000000000, 4.556349186104045934, 80.59375000409677625 ) ) ;
#66392=ORIENTED_EDGE ( 'NONE', *, *, #33134, .F. ) ;
#66398=CARTESIAN_POINT ( 'NONE',  ( -4.220049686691935698, 10.18810118749999916, 79.37500000204838102 ) ) ;
#66400=CARTESIAN_POINT ( 'NONE',  ( 0.000000000000000000, 0.000000000000000000, 118.0000000000000000 ) ) ;
#66406=CARTESIAN_POINT ( 'NONE',  ( 10.18810118750000093, -4.220049686691933921, 88.18750000204838102 ) ) ;
#66410=CARTESIAN_POINT ( 'NONE',  ( -10.18810118749999738, -4.220049686691941915, 93.25000000204838102 ) ) ;
#66418=CARTESIAN_POINT ( 'NONE',  ( 4.220049686691934809, 10.18810118749999916, 99.06250000204836681 ) ) ;
#66433=EDGE_LOOP ( 'NONE', ( #52696, #22209, #50025, #64911 ) ) ;
#66435=CARTESIAN_POINT ( 'NONE',  ( 10.18810118749999916, 4.220049686691935698, 95.50000000204838102 ) ) ;
#66436=CARTESIAN_POINT ( 'NONE',  ( 7.778174593052021635, 7.778174593052023411, 114.6250000040967763 ) ) ;
#66443=EDGE_CURVE ( 'NONE', #15013, #68586, #2993, .T. ) ;
#66456=CARTESIAN_POINT ( 'NONE',  ( -11.00000000000000000, 4.556349186104045934, 111.9062500000000000 ) ) ;
#66468=CARTESIAN_POINT ( 'NONE',  ( -6.735557395310442023E-16, 11.00000000000000000, 101.3125000040967763 ) ) ;
#66469=CARTESIAN_POINT ( 'NONE',  ( -11.00000000000000000, 0.000000000000000000, 89.68750000409677625 ) ) ;
#66490=CARTESIAN_POINT ( 'NONE',  ( -4.220049686691935698, 10.18810118749999916, 105.2500000020483952 ) ) ;
#66499=CARTESIAN_POINT ( 'NONE',  ( -10.18810118749999916, 4.220049686691934809, 112.5625000020483810 ) ) ;
#66507=CARTESIAN_POINT ( 'NONE',  ( -7.204075437095965206, -7.204075437095968759, 113.2187500020483810 ) ) ;
#66523=CARTESIAN_POINT ( 'NONE',  ( 4.220049686691941027, -10.18810118749999738, 116.1250000020483810 ) ) ;
#66556=CARTESIAN_POINT ( 'NONE',  ( 0.000000000000000000, 0.000000000000000000, 118.0000000000000000 ) ) ;
#66566=LINE ( 'NONE', #48839, #43121 ) ;
#66570=( BOUNDED_CURVE ( )  B_SPLINE_CURVE ( 2, ( #27323, #73361, #42807, #2832, #72616, #3968, #38290, #43183, #26198 ),
 .UNSPECIFIED., .F., .F. ) 
 B_SPLINE_CURVE_WITH_KNOTS ( ( 3, 2, 2, 2, 3 ),
 ( 0.6911764705882352811, 0.6948529411764705621, 0.6985294117647058432, 0.7022058823529410132, 0.7058823529411764053 ),
 .UNSPECIFIED. ) 
 CURVE ( )  GEOMETRIC_REPRESENTATION_ITEM ( )  RATIONAL_B_SPLINE_CURVE ( ( 1.000000000000000000, 0.9238795325112867385, 1.000000000000000000, 0.9238795325112867385, 1.000000000000000000, 0.9238795325112867385, 1.000000000000000000, 0.9238795325112890700, 0.9999999999999976685 ) ) 
 REPRESENTATION_ITEM ( '' )  );
#66580=CARTESIAN_POINT ( 'NONE',  ( 4.220049686691941027, -10.18810118749999738, 95.12500000204836681 ) ) ;
#66586=CARTESIAN_POINT ( 'NONE',  ( 11.00000000000000000, 1.347111479062088405E-15, 99.24999999999998579 ) ) ;
#66587=ORIENTED_EDGE ( 'NONE', *, *, #67182, .F. ) ;
#66594=CARTESIAN_POINT ( 'NONE',  ( 4.220049686691941027, -10.18810118749999738, 88.00000000204836681 ) ) ;
#66607=CARTESIAN_POINT ( 'NONE',  ( -4.220049686691937474, -10.18810118749999738, 81.43750000204836681 ) ) ;
#66641=CARTESIAN_POINT ( 'NONE',  ( 4.556349186104051263, -10.99999999999999822, 73.46875000000000000 ) ) ;
#66651=CARTESIAN_POINT ( 'NONE',  ( 11.00000000000000000, 4.556349186104045934, 116.0312500040967763 ) ) ;
#66663=CARTESIAN_POINT ( 'NONE',  ( 4.556349186104045934, 11.00000000000000000, 81.53125000000000000 ) ) ;
#66670=CARTESIAN_POINT ( 'NONE',  ( -7.204075437095965206, -7.204075437095968759, 84.71875000204836681 ) ) ;
#66671=CARTESIAN_POINT ( 'NONE',  ( 10.18810118749999916, 4.220049686691935698, 115.0000000020483668 ) ) ;
#66675=DIRECTION ( 'NONE',  ( -0.000000000000000000, -0.000000000000000000, -1.000000000000000000 ) ) ;
#66686=CARTESIAN_POINT ( 'NONE',  ( -10.18810118749999916, 4.220049686691934809, 108.4375000020483952 ) ) ;
#66709=AXIS2_PLACEMENT_3D ( 'NONE', #1680, #6958, #29600 ) ;
#66710=EDGE_LOOP ( 'NONE', ( #35299, #56076, #35784, #46408 ) ) ;
#66729=CARTESIAN_POINT ( 'NONE',  ( 10.18810118750000093, -4.220049686691933033, 80.31250000204836681 ) ) ;
#66731=CARTESIAN_POINT ( 'NONE',  ( 7.778174593052023411, -7.778174593052021635, 88.56249999999998579 ) ) ;
#66736=CARTESIAN_POINT ( 'NONE',  ( -4.556349186104045934, 11.00000000000000000, 89.21874999999998579 ) ) ;
#66745=CARTESIAN_POINT ( 'NONE',  ( 11.00000000000000000, 1.347111479062088405E-15, 118.0000000000000000 ) ) ;
#66755=CARTESIAN_POINT ( 'NONE',  ( -7.778174593052023411, 7.778174593052023411, 112.0000000040967763 ) ) ;
#66760=CARTESIAN_POINT ( 'NONE',  ( 4.556349186104045934, 11.00000000000000000, 83.21875000409679046 ) ) ;
#66777=CARTESIAN_POINT ( 'NONE',  ( 4.220049686691934809, 10.18810118749999916, 76.18750000204839523 ) ) ;
#66785=CARTESIAN_POINT ( 'NONE',  ( -10.18810118749999916, 0.000000000000000000, 86.03125000204836681 ) ) ;
#66792=CARTESIAN_POINT ( 'NONE',  ( 4.220049686691934809, 10.18810118749999916, 97.18750000204836681 ) ) ;
#66802=CARTESIAN_POINT ( 'NONE',  ( -6.238412754330611322E-16, 10.18810118749999916, 93.15625000204836681 ) ) ;
#66821=CARTESIAN_POINT ( 'NONE',  ( -4.220049686691935698, 10.18810118749999916, 95.87500000204838102 ) ) ;
#66824=CARTESIAN_POINT ( 'NONE',  ( -4.556349186104047710, -10.99999999999999822, 106.2812500000000000 ) ) ;
#66853=CARTESIAN_POINT ( 'NONE',  ( -6.735557395310442023E-16, 11.00000000000000000, 96.81250000409677625 ) ) ;
#66872=AXIS2_PLACEMENT_3D ( 'NONE', #31128, #37170, #48475 ) ;
#66873=CARTESIAN_POINT ( 'NONE',  ( 1.871523826299183495E-15, -10.18810118749999916, 101.4062500020483810 ) ) ;
#66885=CARTESIAN_POINT ( 'NONE',  ( 10.18810118749999916, 1.247682550866122264E-15, 114.9062500020483810 ) ) ;
#66894=CARTESIAN_POINT ( 'NONE',  ( -7.204075437095965206, -7.204075437095968759, 107.2187500020483810 ) ) ;
#66902=( BOUNDED_CURVE ( )  B_SPLINE_CURVE ( 2, ( #11073, #57096, #54404, #53658, #24228, #2711, #13637, #1251, #6892 ),
 .UNSPECIFIED., .F., .F. ) 
 B_SPLINE_CURVE_WITH_KNOTS ( ( 3, 2, 2, 2, 3 ),
 ( 0.1617647058823530326, 0.1654411764705883137, 0.1691176470588236502, 0.1727941176470589313, 0.1764705882352942401 ),
 .UNSPECIFIED. ) 
 CURVE ( )  GEOMETRIC_REPRESENTATION_ITEM ( )  RATIONAL_B_SPLINE_CURVE ( ( 0.9999999999999982236, 0.9238795325112885148, 1.000000000000000000, 0.9238795325112867385, 1.000000000000000000, 0.9238795325112867385, 1.000000000000000000, 0.9238795325112844070, 1.000000000000002220 ) ) 
 REPRESENTATION_ITEM ( '' )  );
#66909=CARTESIAN_POINT ( 'NONE',  ( 10.18810118749999916, 1.247682550866122264E-15, 114.9062500020483810 ) ) ;
#66922=CARTESIAN_POINT ( 'NONE',  ( 4.556349186104052151, -10.99999999999999822, 77.96874999999998579 ) ) ;
#66952=CARTESIAN_POINT ( 'NONE',  ( 10.99999999999989342, 4.556349186104152515, 81.53125000409677625 ) ) ;
#66958=CARTESIAN_POINT ( 'NONE',  ( -4.220049686691937474, -10.18810118749999738, 90.43750000204836681 ) ) ;
#66970=CARTESIAN_POINT ( 'NONE',  ( 10.18810118749999916, 1.247682550866122264E-15, 80.78125000204838102 ) ) ;
#66984=EDGE_CURVE ( 'NONE', #50500, #24157, #56991, .T. ) ;
#66986=CARTESIAN_POINT ( 'NONE',  ( -6.238412754330611322E-16, 10.18810118749999916, 77.78125000204836681 ) ) ;
#67001=CARTESIAN_POINT ( 'NONE',  ( -11.00000000000000000, 0.000000000000000000, 73.18750000409676204 ) ) ;
#67011=CARTESIAN_POINT ( 'NONE',  ( -4.556349186104048599, -10.99999999999999822, 92.78124999999998579 ) ) ;
#67018=( BOUNDED_CURVE ( )  B_SPLINE_CURVE ( 2, ( #26553, #21644, #51064, #38648, #74077, #49577, #56365, #27681, #50687 ),
 .UNSPECIFIED., .F., .F. ) 
 B_SPLINE_CURVE_WITH_KNOTS ( ( 3, 2, 2, 2, 3 ),
 ( 0.6617647058823526995, 0.6654411764705879806, 0.6691176470588232617, 0.6727941176470586537, 0.6764705882352939348 ),
 .UNSPECIFIED. ) 
 CURVE ( )  GEOMETRIC_REPRESENTATION_ITEM ( )  RATIONAL_B_SPLINE_CURVE ( ( 1.000000000000004663, 0.9238795325112821866, 1.000000000000000000, 0.9238795325112867385, 1.000000000000000000, 0.9238795325112867385, 1.000000000000000000, 0.9238795325112912904, 0.9999999999999954481 ) ) 
 REPRESENTATION_ITEM ( '' )  );
#67022=CARTESIAN_POINT ( 'NONE',  ( 11.00000000000000355, -4.556349186104045046, 73.65625000000000000 ) ) ;
#67025=CARTESIAN_POINT ( 'NONE',  ( 11.00000000000000000, 1.347111479062088405E-15, 109.9375000040967763 ) ) ;
#67026=ORIENTED_EDGE ( 'NONE', *, *, #1759, .F. ) ;
#67028=( GEOMETRIC_REPRESENTATION_CONTEXT ( 3 ) GLOBAL_UNCERTAINTY_ASSIGNED_CONTEXT ( ( #1150 ) ) GLOBAL_UNIT_ASSIGNED_CONTEXT ( ( #27939, #35, #50947 ) ) REPRESENTATION_CONTEXT ( 'NONE', 'WORKASPACE' ) );
#67032=CARTESIAN_POINT ( 'NONE',  ( 7.778174593052021635, 7.778174593052023411, 111.6250000040967763 ) ) ;
#67050=CARTESIAN_POINT ( 'NONE',  ( 7.204075437095966983, 7.204075437095967871, 113.5937500020483810 ) ) ;
#67065=CARTESIAN_POINT ( 'NONE',  ( -4.220049686691937474, -10.18810118749999738, 99.81250000204838102 ) ) ;
#67082=AXIS2_PLACEMENT_3D ( 'NONE', #28684, #57375, #70813 ) ;
#67087=EDGE_CURVE ( 'NONE', #71006, #21157, #2437, .T. ) ;
#67106=CARTESIAN_POINT ( 'NONE',  ( -4.220049686691935698, 10.18810118749999916, 71.87500000204836681 ) ) ;
#67109=CARTESIAN_POINT ( 'NONE',  ( 11.00000000000000000, 1.347111479062088405E-15, 87.25000000000000000 ) ) ;
#67113=( BOUNDED_CURVE ( )  B_SPLINE_CURVE ( 2, ( #26260, #15693, #16062, #15314, #54964, #21725, #56085, #50406, #44755 ),
 .UNSPECIFIED., .F., .F. ) 
 B_SPLINE_CURVE_WITH_KNOTS ( ( 3, 2, 2, 2, 3 ),
 ( 0.01470588235294118494, 0.01838235294117648161, 0.02205882352941178001, 0.02573529411764707148, 0.02941176470588236988 ),
 .UNSPECIFIED. ) 
 CURVE ( )  GEOMETRIC_REPRESENTATION_ITEM ( )  RATIONAL_B_SPLINE_CURVE ( ( 0.9999999999999998890, 0.9238795325112869605, 1.000000000000000000, 0.9238795325112867385, 1.000000000000000000, 0.9238795325112867385, 1.000000000000000000, 0.9238795325112864054, 1.000000000000000444 ) ) 
 REPRESENTATION_ITEM ( '' )  );
#67133=CARTESIAN_POINT ( 'NONE',  ( 11.00000000000000000, 1.347111479062088405E-15, 111.4375000040967763 ) ) ;
#67140=CARTESIAN_POINT ( 'NONE',  ( 11.00000000000000000, 4.556349186104045934, 78.53125000409677625 ) ) ;
#67148=CARTESIAN_POINT ( 'NONE',  ( -6.735557395310442023E-16, 11.00000000000000000, 98.31250000409677625 ) ) ;
#67159=CARTESIAN_POINT ( 'NONE',  ( -10.18810118749999738, -4.220049686691941915, 78.25000000204836681 ) ) ;
#67167=CARTESIAN_POINT ( 'NONE',  ( 10.18810118749999916, 1.247682550866122264E-15, 83.78125000204838102 ) ) ;
#67173=CARTESIAN_POINT ( 'NONE',  ( -7.204075437095967871, 7.204075437095967871, 92.96875000204838102 ) ) ;
#67180=CARTESIAN_POINT ( 'NONE',  ( -6.238412754330611322E-16, 10.18810118749999916, 90.15625000204838102 ) ) ;
#67182=EDGE_CURVE ( 'NONE', #8028, #12665, #33886, .T. ) ;
#67197=CARTESIAN_POINT ( 'NONE',  ( 1.871523826299183495E-15, -10.18810118749999916, 101.0312500020483810 ) ) ;
#67200=CARTESIAN_POINT ( 'NONE',  ( 7.778174593052021635, 7.778174593052023411, 105.4374999999999858 ) ) ;
#67207=VERTEX_POINT ( 'NONE', #9597 ) ;
#67223=DIRECTION ( 'NONE',  ( -1.000000000000000000, 0.000000000000000000, 0.000000000000000000 ) ) ;
#67231=CARTESIAN_POINT ( 'NONE',  ( 7.778174593052023411, -7.778174593052021635, 99.25000000409679046 ) ) ;
#67232=CARTESIAN_POINT ( 'NONE',  ( 7.778174593052023411, -7.778174593052021635, 106.7500000040967763 ) ) ;
#67255=CARTESIAN_POINT ( 'NONE',  ( 10.18810118749999916, 4.220049686691935698, 103.3750000020484094 ) ) ;
#67264=CARTESIAN_POINT ( 'NONE',  ( 10.18810118750000093, -4.220049686691933921, 116.3125000020483668 ) ) ;
#67274=CARTESIAN_POINT ( 'NONE',  ( 1.871523826299183495E-15, -10.18810118749999916, 111.9062500020483810 ) ) ;
#67280=CARTESIAN_POINT ( 'NONE',  ( 4.220049686691941027, -10.18810118749999738, 71.50000000204839523 ) ) ;
#67283=VERTEX_POINT ( 'NONE', #60891 ) ;
#67286=CARTESIAN_POINT ( 'NONE',  ( -4.220049686691937474, -10.18810118749999738, 114.4375000020483668 ) ) ;
#67309=CARTESIAN_POINT ( 'NONE',  ( -11.00000000000000000, 0.000000000000000000, 118.0000000000000000 ) ) ;
#67317=CARTESIAN_POINT ( 'NONE',  ( 10.99999999999989342, 4.556349186104152515, 77.03125000409679046 ) ) ;
#67320=CARTESIAN_POINT ( 'NONE',  ( 2.020667218593132706E-15, -11.00000000000000000, 79.37499999999998579 ) ) ;
#67337=CARTESIAN_POINT ( 'NONE',  ( 4.220049686691941027, -10.18810118749999738, 92.12500000204836681 ) ) ;
#67348=CARTESIAN_POINT ( 'NONE',  ( -10.18810118749999738, -4.220049686691941915, 84.62500000204836681 ) ) ;
#67362=CARTESIAN_POINT ( 'NONE',  ( 7.204075437095968759, -7.204075437095966983, 75.71875000204836681 ) ) ;
#67396=CARTESIAN_POINT ( 'NONE',  ( 2.020667218593132706E-15, -11.00000000000000000, 71.87500000000000000 ) ) ;
#67407=VECTOR ( 'NONE', #5761, 1000.000000000000000 ) ;
#67417=CARTESIAN_POINT ( 'NONE',  ( -4.556349186104045934, 11.00000000000000000, 81.71874999999998579 ) ) ;
#67425=CARTESIAN_POINT ( 'NONE',  ( -7.204075437095965206, -7.204075437095968759, 109.8437500020483810 ) ) ;
#67428=CARTESIAN_POINT ( 'NONE',  ( -15.99999999999999645, -16.00000000000000355, 20.00000000000000000 ) ) ;
#67430=LINE ( 'NONE', #37270, #9933 ) ;
#67440=CARTESIAN_POINT ( 'NONE',  ( -10.18810118749999738, -4.220049686691941915, 102.6250000020483810 ) ) ;
#67459=VECTOR ( 'NONE', #23869, 1000.000000000000000 ) ;
#67460=CARTESIAN_POINT ( 'NONE',  ( -7.204075437095965206, -7.204075437095968759, 78.71875000204836681 ) ) ;
#67469=CARTESIAN_POINT ( 'NONE',  ( -11.00000000000000533, 11.00000000000000000, 20.00000000000000000 ) ) ;
#67480=CARTESIAN_POINT ( 'NONE',  ( 1.871523826299183495E-15, -10.18810118749999916, 72.53125000204838102 ) ) ;
#67483=CARTESIAN_POINT ( 'NONE',  ( 11.00000000000000355, -4.556349186104045046, 87.15624999999998579 ) ) ;
#67506=CARTESIAN_POINT ( 'NONE',  ( -7.778174593052020747, -7.778174593052023411, 71.68749999999998579 ) ) ;
#67511=CARTESIAN_POINT ( 'NONE',  ( 11.00000000000000355, -4.556349186104045046, 73.84375000409676204 ) ) ;
#67526=CARTESIAN_POINT ( 'NONE',  ( -11.00000000000000000, 0.000000000000000000, 95.68750000409677625 ) ) ;
#67527=CARTESIAN_POINT ( 'NONE',  ( 10.18810118749999916, 1.247682550866122264E-15, 77.40625000204836681 ) ) ;
#67529=CARTESIAN_POINT ( 'NONE',  ( -11.00000000000000000, 0.000000000000000000, 115.1875000040967763 ) ) ;
#67532=ADVANCED_FACE ( 'NONE', ( #48692 ), #8336, .T. ) ;
#67533=EDGE_CURVE ( 'NONE', #25230, #46843, #58482, .T. ) ;
#67538=CARTESIAN_POINT ( 'NONE',  ( -10.18810118749999738, -4.220049686691941915, 78.62500000204838102 ) ) ;
#67544=ORIENTED_EDGE ( 'NONE', *, *, #47131, .F. ) ;
#67551=CARTESIAN_POINT ( 'NONE',  ( 7.204075437095966983, 7.204075437095967871, 92.96875000204838102 ) ) ;
#67569=CARTESIAN_POINT ( 'NONE',  ( -7.204075437095965206, -7.204075437095968759, 91.84375000204838102 ) ) ;
#67572=CARTESIAN_POINT ( 'NONE',  ( 4.556349186104051263, -10.99999999999999822, 104.9687500000000000 ) ) ;
#67588=CARTESIAN_POINT ( 'NONE',  ( -4.556349186104045934, 11.00000000000000000, 111.7187499999999858 ) ) ;
#67597=FACE_OUTER_BOUND ( 'NONE', #50433, .T. ) ;
#67603=CARTESIAN_POINT ( 'NONE',  ( 4.556349186104051263, -10.99999999999999822, 100.6562500040967905 ) ) ;
#67626=CARTESIAN_POINT ( 'NONE',  ( 10.18810118750000093, -4.220049686691933921, 104.6875000020483810 ) ) ;
#67630=CARTESIAN_POINT ( 'NONE',  ( -7.778174593052023411, 7.778174593052023411, 98.31250000000000000 ) ) ;
#67636=CARTESIAN_POINT ( 'NONE',  ( -6.238412754330611322E-16, 10.18810118749999916, 112.2812500020483810 ) ) ;
#67643=CARTESIAN_POINT ( 'NONE',  ( -10.18810118749999916, 0.000000000000000000, 110.0312500020483668 ) ) ;
#67658=CARTESIAN_POINT ( 'NONE',  ( 11.00000000000000000, 1.347111479062088405E-15, 106.7500000000000000 ) ) ;
#67660=CARTESIAN_POINT ( 'NONE',  ( 7.204075437095966983, 7.204075437095967871, 110.5937500020483810 ) ) ;
#67674=DIRECTION ( 'NONE',  ( -0.000000000000000000, -0.000000000000000000, -1.000000000000000000 ) ) ;
#67676=CARTESIAN_POINT ( 'NONE',  ( -4.556349186104045934, 11.00000000000000000, 107.4062500040967620 ) ) ;
#67688=ORIENTED_EDGE ( 'NONE', *, *, #21984, .T. ) ;
#67707=CARTESIAN_POINT ( 'NONE',  ( 4.556349186104045934, 11.00000000000000000, 95.03124999999998579 ) ) ;
#67711=CARTESIAN_POINT ( 'NONE',  ( 7.204075437095966983, 7.204075437095967871, 88.09375000204836681 ) ) ;
#67712=CARTESIAN_POINT ( 'NONE',  ( 0.000000000000000000, 0.000000000000000000, 118.0000000000000000 ) ) ;
#67723=CARTESIAN_POINT ( 'NONE',  ( -10.18810118749999916, 4.220049686691934809, 85.93750000204839523 ) ) ;
#67739=CARTESIAN_POINT ( 'NONE',  ( -10.18810118749999916, 0.000000000000000000, 76.65625000204836681 ) ) ;
#67773=CARTESIAN_POINT ( 'NONE',  ( -6.735557395310442023E-16, 11.00000000000000000, 72.62500000000000000 ) ) ;
#67799=CARTESIAN_POINT ( 'NONE',  ( -6.238412754330611322E-16, 10.18810118749999916, 106.2812500020483810 ) ) ;
#67803=CARTESIAN_POINT ( 'NONE',  ( -4.556349186104048599, -10.99999999999999822, 97.28124999999998579 ) ) ;
#67812=CARTESIAN_POINT ( 'NONE',  ( -10.18810118749999916, 0.000000000000000000, 99.53125000204838102 ) ) ;
#67831=CARTESIAN_POINT ( 'NONE',  ( -4.220049686691935698, 10.18810118749999916, 79.75000000204838102 ) ) ;
#67843=ORIENTED_EDGE ( 'NONE', *, *, #3468, .F. ) ;
#67847=ORIENTED_EDGE ( 'NONE', *, *, #33019, .T. ) ;
#67848=CARTESIAN_POINT ( 'NONE',  ( -7.204075437095965206, -7.204075437095968759, 75.34375000204838102 ) ) ;
#67851=CARTESIAN_POINT ( 'NONE',  ( -6.735557395310442023E-16, 11.00000000000000000, 87.62499999999998579 ) ) ;
#67856=CARTESIAN_POINT ( 'NONE',  ( 1.959434878635765526E-15, -16.00000000000000711, 3.497325839728428143 ) ) ;
#67877=CARTESIAN_POINT ( 'NONE',  ( 7.778174593052023411, -7.778174593052021635, 81.25000000409676204 ) ) ;
#67879=CARTESIAN_POINT ( 'NONE',  ( -7.778174593052020747, -7.778174593052023411, 71.87500000409677625 ) ) ;
#67895=ORIENTED_EDGE ( 'NONE', *, *, #32420, .T. ) ;
#67897=CARTESIAN_POINT ( 'NONE',  ( 10.18810118749999916, 1.247682550866122264E-15, 69.90625000204836681 ) ) ;
#67906=CARTESIAN_POINT ( 'NONE',  ( -4.220049686691935698, 10.18810118749999916, 78.25000000204836681 ) ) ;
#67919=CARTESIAN_POINT ( 'NONE',  ( 4.220049686691934809, 10.18810118749999916, 90.06250000204838102 ) ) ;
#67935=ORIENTED_EDGE ( 'NONE', *, *, #33134, .T. ) ;
#67936=ORIENTED_EDGE ( 'NONE', *, *, #56856, .F. ) ;
#67937=CARTESIAN_POINT ( 'NONE',  ( 4.220049686691941027, -10.18810118749999738, 95.12500000204838102 ) ) ;
#67940=CARTESIAN_POINT ( 'NONE',  ( 4.556349186104051263, -10.99999999999999822, 106.4687499999999716 ) ) ;
#67969=CARTESIAN_POINT ( 'NONE',  ( 7.778174593052023411, -7.778174593052021635, 91.75000000409677625 ) ) ;
#67990=CARTESIAN_POINT ( 'NONE',  ( 10.18810118749999916, 4.220049686691935698, 98.87500000204836681 ) ) ;
#67998=CARTESIAN_POINT ( 'NONE',  ( 4.220049686691941027, -10.18810118749999738, 111.6250000020483810 ) ) ;
#68007=CARTESIAN_POINT ( 'NONE',  ( -4.220049686691935698, 10.18810118749999916, 108.2500000020483810 ) ) ;
#68010=VECTOR ( 'NONE', #48141, 1000.000000000000000 ) ;
#68018=( BOUNDED_CURVE ( )  B_SPLINE_CURVE ( 2, ( #12127, #35166, #58181, #13225, #1203, #7587, #24914, #42275, #64192 ),
 .UNSPECIFIED., .F., .F. ) 
 B_SPLINE_CURVE_WITH_KNOTS ( ( 3, 2, 2, 2, 3 ),
 ( 0.5000000000000000000, 0.5036764705882352811, 0.5073529411764705621, 0.5110294117647059542, 0.5147058823529412352 ),
 .UNSPECIFIED. ) 
 CURVE ( )  GEOMETRIC_REPRESENTATION_ITEM ( )  RATIONAL_B_SPLINE_CURVE ( ( 1.000000000000000000, 0.9238795325112867385, 1.000000000000000000, 0.9238795325112867385, 1.000000000000000000, 0.9238795325112867385, 1.000000000000000000, 0.9238795325112844070, 1.000000000000002220 ) ) 
 REPRESENTATION_ITEM ( '' )  );
#68023=ORIENTED_EDGE ( 'NONE', *, *, #18185, .F. ) ;
#68027=CARTESIAN_POINT ( 'NONE',  ( 4.220049686691941027, -10.18810118749999738, 113.1250000020483810 ) ) ;
#68045=EDGE_CURVE ( 'NONE', #69783, #22824, #28572, .T. ) ;
#68080=CARTESIAN_POINT ( 'NONE',  ( -4.220049686691935698, 10.18810118749999916, 88.37500000204839523 ) ) ;
#68084=CARTESIAN_POINT ( 'NONE',  ( 11.00000000000007994, 4.556349186103967774, 112.8437500000000000 ) ) ;
#68086=CARTESIAN_POINT ( 'NONE',  ( -10.18810118749999916, 4.220049686691934809, 115.9375000020483668 ) ) ;
#68093=CARTESIAN_POINT ( 'NONE',  ( -10.18810118749999738, -4.220049686691941915, 86.12500000204836681 ) ) ;
#68097=CARTESIAN_POINT ( 'NONE',  ( 11.00000000000000000, 1.347111479062088405E-15, 84.24999999999998579 ) ) ;
#68105=CARTESIAN_POINT ( 'NONE',  ( -6.238412754330611322E-16, 10.18810118749999916, 76.28125000204836681 ) ) ;
#68116=( BOUNDED_CURVE ( )  B_SPLINE_CURVE ( 2, ( #59293, #41923, #53259, #34818, #41199, #18554, #6502, #17808, #46107 ),
 .UNSPECIFIED., .F., .F. ) 
 B_SPLINE_CURVE_WITH_KNOTS ( ( 3, 2, 2, 2, 3 ),
 ( 0.4117647058823529216, 0.4154411764705882582, 0.4191176470588235947, 0.4227941176470588758, 0.4264705882352941568 ),
 .UNSPECIFIED. ) 
 CURVE ( )  GEOMETRIC_REPRESENTATION_ITEM ( )  RATIONAL_B_SPLINE_CURVE ( ( 1.000000000000000000, 0.9238795325112867385, 1.000000000000000000, 0.9238795325112867385, 1.000000000000000000, 0.9238795325112867385, 1.000000000000000000, 0.9238795325112856283, 1.000000000000001110 ) ) 
 REPRESENTATION_ITEM ( '' )  );
#68134=CARTESIAN_POINT ( 'NONE',  ( 11.00000000000000000, 4.556349186104045934, 79.84374999999998579 ) ) ;
#68143=VERTEX_POINT ( 'NONE', #29243 ) ;
#68163=CARTESIAN_POINT ( 'NONE',  ( -10.18810118749999738, -4.220049686691941915, 109.7500000020483810 ) ) ;
#68167=CARTESIAN_POINT ( 'NONE',  ( -11.00000000000000000, 0.000000000000000000, 96.99999999999998579 ) ) ;
#68172=EDGE_CURVE ( 'NONE', #30135, #18846, #43983, .T. ) ;
#68182=CARTESIAN_POINT ( 'NONE',  ( 1.871523826299183495E-15, -10.18810118749999916, 99.90625000204838102 ) ) ;
#68185=ORIENTED_EDGE ( 'NONE', *, *, #24555, .F. ) ;
#68201=CARTESIAN_POINT ( 'NONE',  ( 10.18810118749999916, 4.220049686691935698, 82.37500000204838102 ) ) ;
#68202=VERTEX_POINT ( 'NONE', #54481 ) ;
#68208=VECTOR ( 'NONE', #27648, 1000.000000000000000 ) ;
#68220=CARTESIAN_POINT ( 'NONE',  ( -10.18810118749999738, -4.220049686691941915, 73.75000000204836681 ) ) ;
#68223=CARTESIAN_POINT ( 'NONE',  ( 4.556349186104051263, -10.99999999999999822, 88.46874999999998579 ) ) ;
#68249=CARTESIAN_POINT ( 'NONE',  ( -11.00000000000000000, 0.000000000000000000, 114.9999999999999858 ) ) ;
#68252=CARTESIAN_POINT ( 'NONE',  ( 11.00000000000000000, 1.347111479062088405E-15, 73.93750000409676204 ) ) ;
#68265=CARTESIAN_POINT ( 'NONE',  ( -6.238412754330611322E-16, 10.18810118749999916, 117.1562500020483810 ) ) ;
#68269=CARTESIAN_POINT ( 'NONE',  ( 10.18810118749999916, 1.247682550866122264E-15, 68.40625000204836681 ) ) ;
#68278=EDGE_CURVE ( 'NONE', #47406, #34562, #70700, .T. ) ;
#68279=CARTESIAN_POINT ( 'NONE',  ( 1.871523826299183495E-15, -10.18810118749999916, 81.90625000204838102 ) ) ;
#68305=CARTESIAN_POINT ( 'NONE',  ( -10.18810118749999916, 0.000000000000000000, 94.65625000204836681 ) ) ;
#68308=CARTESIAN_POINT ( 'NONE',  ( -11.00000000000000000, 4.556349186104045934, 105.9062499999999858 ) ) ;
#68311=FACE_OUTER_BOUND ( 'NONE', #42948, .T. ) ;
#68341=CARTESIAN_POINT ( 'NONE',  ( -11.00000000000000000, 4.556349186104045934, 91.09375000409677625 ) ) ;
#68354=DIRECTION ( 'NONE',  ( -1.000000000000000000, 0.000000000000000000, 0.000000000000000000 ) ) ;
#68363=CARTESIAN_POINT ( 'NONE',  ( 7.204075437095966983, 7.204075437095967871, 98.96875000204838102 ) ) ;
#68370=CARTESIAN_POINT ( 'NONE',  ( -4.220049686691935698, 10.18810118749999916, 104.8750000020483668 ) ) ;
#68379=CARTESIAN_POINT ( 'NONE',  ( -7.204075437095967871, 7.204075437095967871, 112.8437500020483810 ) ) ;
#68394=CARTESIAN_POINT ( 'NONE',  ( 7.204075437095968759, -7.204075437095966983, 113.2187500020483810 ) ) ;
#68403=CARTESIAN_POINT ( 'NONE',  ( 0.000000000000000000, 0.000000000000000000, 118.0000000000000000 ) ) ;
#68420=CARTESIAN_POINT ( 'NONE',  ( -6.735557395310442023E-16, 11.00000000000000000, 113.3125000040967763 ) ) ;
#68432=ORIENTED_EDGE ( 'NONE', *, *, #38255, .T. ) ;
#68440=CARTESIAN_POINT ( 'NONE',  ( 4.220049686691934809, 10.18810118749999916, 88.18750000204838102 ) ) ;
#68446=CARTESIAN_POINT ( 'NONE',  ( -4.220049686691937474, -10.18810118749999738, 113.3125000020483668 ) ) ;
#68456=CARTESIAN_POINT ( 'NONE',  ( 10.18810118750000093, -4.220049686691933033, 85.18750000204838102 ) ) ;
#68469=CARTESIAN_POINT ( 'NONE',  ( 4.220049686691934809, 10.18810118749999916, 74.68750000204836681 ) ) ;
#68478=CARTESIAN_POINT ( 'NONE',  ( 2.020667218593132706E-15, -11.00000000000000000, 75.06250000409676204 ) ) ;
#68507=CARTESIAN_POINT ( 'NONE',  ( -6.735557395310442023E-16, 11.00000000000000000, 107.1250000000000000 ) ) ;
#68510=CARTESIAN_POINT ( 'NONE',  ( -11.00000000000021139, 4.556349186103834548, 85.09375000409677625 ) ) ;
#68533=CARTESIAN_POINT ( 'NONE',  ( 4.220049686691941027, -10.18810118749999738, 107.1250000020483810 ) ) ;
#68547=FACE_OUTER_BOUND ( 'NONE', #70024, .T. ) ;
#68551=CARTESIAN_POINT ( 'NONE',  ( 4.220049686691934809, 10.18810118749999916, 99.06250000204836681 ) ) ;
#68564=CARTESIAN_POINT ( 'NONE',  ( 7.204075437095968759, -7.204075437095966983, 95.21875000204838102 ) ) ;
#68573=CARTESIAN_POINT ( 'NONE',  ( 4.220049686691941027, -10.18810118749999738, 83.50000000204840944 ) ) ;
#68586=VERTEX_POINT ( 'NONE', #72567 ) ;
#68592=VERTEX_POINT ( 'NONE', #15954 ) ;
#68593=CARTESIAN_POINT ( 'NONE',  ( 1.871523826299183495E-15, -10.18810118749999916, 75.53125000204836681 ) ) ;
#68595=CARTESIAN_POINT ( 'NONE',  ( 7.778174593052023411, -7.778174593052021635, 84.06249999999998579 ) ) ;
#68619=CYLINDRICAL_SURFACE ( 'NONE', #32653, 11.00000000000000000 ) ;
#68622=CARTESIAN_POINT ( 'NONE',  ( -7.778174593052023411, 7.778174593052023411, 76.00000000409676204 ) ) ;
#68640=CARTESIAN_POINT ( 'NONE',  ( 10.18810118749999916, 4.220049686691935698, 70.00000000204836681 ) ) ;
#68646=CARTESIAN_POINT ( 'NONE',  ( 7.778174593052023411, -7.778174593052021635, 79.75000000409676204 ) ) ;
#68650=VECTOR ( 'NONE', #57454, 1000.000000000000000 ) ;
#68654=( BOUNDED_CURVE ( )  B_SPLINE_CURVE ( 2, ( #52728, #41039, #23303, #69331, #28967, #11616, #62922, #52357, #46317 ),
 .UNSPECIFIED., .F., .F. ) 
 B_SPLINE_CURVE_WITH_KNOTS ( ( 3, 2, 2, 2, 3 ),
 ( 0.5441176470588233727, 0.5477941176470587648, 0.5514705882352939348, 0.5551470588235292158, 0.5588235294117644969 ),
 .UNSPECIFIED. ) 
 CURVE ( )  GEOMETRIC_REPRESENTATION_ITEM ( )  RATIONAL_B_SPLINE_CURVE ( ( 1.000000000000002220, 0.9238795325112844070, 1.000000000000000000, 0.9238795325112867385, 1.000000000000000000, 0.9238795325112867385, 1.000000000000000000, 0.9238795325112912904, 0.9999999999999954481 ) ) 
 REPRESENTATION_ITEM ( '' )  );
#68665=ORIENTED_EDGE ( 'NONE', *, *, #29166, .F. ) ;
#68669=DIRECTION ( 'NONE',  ( -0.000000000000000000, -0.000000000000000000, -1.000000000000000000 ) ) ;
#68671=( BOUNDED_CURVE ( )  B_SPLINE_CURVE ( 2, ( #42043, #13723, #36768, #61263, #38260, #3553, #26168, #22008, #27295 ),
 .UNSPECIFIED., .F., .F. ) 
 B_SPLINE_CURVE_WITH_KNOTS ( ( 3, 2, 2, 2, 3 ),
 ( 0.4558823529411765163, 0.4595588235294117974, 0.4632352941176471894, 0.4669117647058824705, 0.4705882352941177516 ),
 .UNSPECIFIED. ) 
 CURVE ( )  GEOMETRIC_REPRESENTATION_ITEM ( )  RATIONAL_B_SPLINE_CURVE ( ( 0.9999999999999988898, 0.9238795325112878487, 1.000000000000000000, 0.9238795325112867385, 1.000000000000000000, 0.9238795325112867385, 1.000000000000000000, 0.9238795325112844070, 1.000000000000002220 ) ) 
 REPRESENTATION_ITEM ( '' )  );
#68675=VERTEX_POINT ( 'NONE', #45015 ) ;
#68676=CARTESIAN_POINT ( 'NONE',  ( 7.204075437095966983, 7.204075437095967871, 92.59375000204838102 ) ) ;
#68679=CARTESIAN_POINT ( 'NONE',  ( -6.735557395310442023E-16, 11.00000000000000000, 102.6250000000000000 ) ) ;
#68685=CARTESIAN_POINT ( 'NONE',  ( -7.778174593052020747, -7.778174593052023411, 86.87500000409677625 ) ) ;
#68708=CARTESIAN_POINT ( 'NONE',  ( 11.00000000000000000, 1.347111479062088405E-15, 93.43750000409677625 ) ) ;
#68709=CARTESIAN_POINT ( 'NONE',  ( 11.00000000000000000, 1.347111479062088405E-15, 117.2500000000000000 ) ) ;
#68729=CARTESIAN_POINT ( 'NONE',  ( 10.18810118750000093, -4.220049686691933921, 98.68750000204838102 ) ) ;
#68731=VECTOR ( 'NONE', #19390, 1000.000000000000000 ) ;
#68739=CARTESIAN_POINT ( 'NONE',  ( 7.204075437095968759, -7.204075437095966983, 110.2187500020483810 ) ) ;
#68747=CARTESIAN_POINT ( 'NONE',  ( 10.18810118749999916, 1.247682550866122264E-15, 106.2812500020483810 ) ) ;
#68759=CARTESIAN_POINT ( 'NONE',  ( 11.00000000000000000, 1.347111479062088405E-15, 118.0000000000000000 ) ) ;
#68766=CARTESIAN_POINT ( 'NONE',  ( 7.204075437095966983, 7.204075437095967871, 109.0937500020483810 ) ) ;
#68781=CARTESIAN_POINT ( 'NONE',  ( -11.00000000000000000, 4.556349186104045934, 73.09375000409676204 ) ) ;
#68782=CARTESIAN_POINT ( 'NONE',  ( -10.18810118749999916, 0.000000000000000000, 69.53125000204838102 ) ) ;
#68788=CARTESIAN_POINT ( 'NONE',  ( -7.778174593052020747, -7.778174593052023411, 97.37500000409676204 ) ) ;
#68793=CARTESIAN_POINT ( 'NONE',  ( -11.00000000000000000, 0.000000000000000000, 109.1875000040967763 ) ) ;
#68813=CARTESIAN_POINT ( 'NONE',  ( -7.204075437095967871, 7.204075437095967871, 83.96875000204836681 ) ) ;
#68818=CARTESIAN_POINT ( 'NONE',  ( 7.204075437095968759, -7.204075437095966983, 113.5937500020483810 ) ) ;
#68826=CARTESIAN_POINT ( 'NONE',  ( 10.18810118749999916, 1.247682550866122264E-15, 77.78125000204836681 ) ) ;
#68828=ORIENTED_EDGE ( 'NONE', *, *, #6585, .T. ) ;
#68837=CARTESIAN_POINT ( 'NONE',  ( -11.00000000000000000, 0.000000000000000000, 118.0000000000000000 ) ) ;
#68842=CARTESIAN_POINT ( 'NONE',  ( 4.220049686691941027, -10.18810118749999738, 74.12500000204836681 ) ) ;
#68847=AXIS2_PLACEMENT_3D ( 'NONE', #13479, #42534, #19152 ) ;
#68858=CARTESIAN_POINT ( 'NONE',  ( 11.00000000000000000, 1.347111479062088405E-15, 108.4375000040967763 ) ) ;
#68879=DIRECTION ( 'NONE',  ( -0.000000000000000000, -0.000000000000000000, -1.000000000000000000 ) ) ;
#68888=( BOUNDED_CURVE ( )  B_SPLINE_CURVE ( 2, ( #55976, #4286, #44643, #49925, #44273, #3163, #61991, #10313, #72570 ),
 .UNSPECIFIED., .F., .F. ) 
 B_SPLINE_CURVE_WITH_KNOTS ( ( 3, 2, 2, 2, 3 ),
 ( 0.5294117647058821374, 0.5330882352941174185, 0.5367647058823528106, 0.5404411764705880916, 0.5441176470588233727 ),
 .UNSPECIFIED. ) 
 CURVE ( )  GEOMETRIC_REPRESENTATION_ITEM ( )  RATIONAL_B_SPLINE_CURVE ( ( 1.000000000000004663, 0.9238795325112821866, 1.000000000000000000, 0.9238795325112867385, 1.000000000000000000, 0.9238795325112867385, 1.000000000000000000, 0.9238795325112890700, 0.9999999999999976685 ) ) 
 REPRESENTATION_ITEM ( '' )  );
#68907=CARTESIAN_POINT ( 'NONE',  ( -7.204075437095967871, 7.204075437095967871, 107.9687500020483810 ) ) ;
#68919=CARTESIAN_POINT ( 'NONE',  ( -4.556349186104045934, 11.00000000000000000, 99.90625000409677625 ) ) ;
#68923=CARTESIAN_POINT ( 'NONE',  ( 7.204075437095968759, -7.204075437095966983, 94.09375000204838102 ) ) ;
#68935=CARTESIAN_POINT ( 'NONE',  ( 4.220049686691941027, -10.18810118749999738, 98.12500000204836681 ) ) ;
#68944=EDGE_CURVE ( 'NONE', #39397, #5227, #24585, .T. ) ;
#68947=CARTESIAN_POINT ( 'NONE',  ( 7.204075437095966983, 7.204075437095967871, 74.96875000204836681 ) ) ;
#68953=CARTESIAN_POINT ( 'NONE',  ( -11.00000000000000000, 0.000000000000000000, 100.1875000040967763 ) ) ;
#68963=EDGE_CURVE ( 'NONE', #44494, #70285, #7422, .T. ) ;
#68968=CARTESIAN_POINT ( 'NONE',  ( 1.871523826299183495E-15, -10.18810118749999916, 71.03125000204838102 ) ) ;
#68971=CARTESIAN_POINT ( 'NONE',  ( 11.00000000000000000, 1.347111479062088405E-15, 84.24999999999998579 ) ) ;
#68991=EDGE_CURVE ( 'NONE', #69514, #73904, #61398, .T. ) ;
#68998=CARTESIAN_POINT ( 'NONE',  ( 2.020667218593132706E-15, -11.00000000000000000, 72.06250000409677625 ) ) ;
#69011=( BOUNDED_CURVE ( )  B_SPLINE_CURVE ( 2, ( #49898, #62327, #67630, #4260, #16290, #27626, #32564, #63075, #57060 ),
 .UNSPECIFIED., .F., .F. ) 
 B_SPLINE_CURVE_WITH_KNOTS ( ( 3, 2, 2, 2, 3 ),
 ( 0.3823529411764705621, 0.3860294117647058987, 0.3897058823529411797, 0.3933823529411764608, 0.3970588235294117418 ),
 .UNSPECIFIED. ) 
 CURVE ( )  GEOMETRIC_REPRESENTATION_ITEM ( )  RATIONAL_B_SPLINE_CURVE ( ( 1.000000000000000000, 0.9238795325112867385, 1.000000000000000000, 0.9238795325112867385, 1.000000000000000000, 0.9238795325112867385, 1.000000000000000000, 0.9238795325112867385, 1.000000000000000000 ) ) 
 REPRESENTATION_ITEM ( '' )  );
#69016=( BOUNDED_CURVE ( )  B_SPLINE_CURVE ( 1, ( #17285, #62559 ),
 .UNSPECIFIED., .F., .F. ) 
 B_SPLINE_CURVE_WITH_KNOTS ( ( 2, 2 ),
 ( 0.000000000000000000, 1.000000000000000000 ),
 .UNSPECIFIED. ) 
 CURVE ( )  GEOMETRIC_REPRESENTATION_ITEM ( )  RATIONAL_B_SPLINE_CURVE ( ( 0.9660721264009082265, 0.9660721264009082265 ) ) 
 REPRESENTATION_ITEM ( '' )  );
#69017=CARTESIAN_POINT ( 'NONE',  ( -4.220049686691935698, 10.18810118749999916, 68.87500000204838102 ) ) ;
#69027=EDGE_LOOP ( 'NONE', ( #45058, #35972, #43626, #14862, #68023 ) ) ;
#69031=EDGE_CURVE ( 'NONE', #53323, #46063, #8727, .T. ) ;
#69053=VERTEX_POINT ( 'NONE', #54759 ) ;
#69054=ORIENTED_EDGE ( 'NONE', *, *, #59652, .T. ) ;
#69055=CARTESIAN_POINT ( 'NONE',  ( -4.220049686691935698, 10.18810118749999916, 89.87500000204836681 ) ) ;
#69058=CARTESIAN_POINT ( 'NONE',  ( -11.00000000000000000, 0.000000000000000000, 101.5000000000000000 ) ) ;
#69086=CARTESIAN_POINT ( 'NONE',  ( 11.00000000000000355, -4.556349186104045046, 91.84375000409677625 ) ) ;
#69105=( NAMED_UNIT ( * ) SI_UNIT ( $, .STERADIAN. ) SOLID_ANGLE_UNIT ( ) );
#69108=CARTESIAN_POINT ( 'NONE',  ( -7.204075437095965206, -7.204075437095968759, 98.21875000204838102 ) ) ;
#69116=CARTESIAN_POINT ( 'NONE',  ( 7.204075437095966983, 7.204075437095967871, 109.0937500020483810 ) ) ;
#69128=CARTESIAN_POINT ( 'NONE',  ( 7.204075437095966983, 7.204075437095967871, 104.9687500020483810 ) ) ;
#69142=CARTESIAN_POINT ( 'NONE',  ( -7.204075437095967871, 7.204075437095967871, 112.4687500020483810 ) ) ;
#69143=CARTESIAN_POINT ( 'NONE',  ( -10.99999999999994671, -4.556349186104105442, 103.0937499999999858 ) ) ;
#69155=CARTESIAN_POINT ( 'NONE',  ( -7.778174593052020747, -7.778174593052023411, 91.18749999999998579 ) ) ;
#69159=CARTESIAN_POINT ( 'NONE',  ( -6.735557395310442023E-16, 11.00000000000000000, 117.6250000000000000 ) ) ;
#69163=CYLINDRICAL_SURFACE ( 'NONE', #31255, 11.00000000000000000 ) ;
#69166=ORIENTED_EDGE ( 'NONE', *, *, #7336, .F. ) ;
#69170=CARTESIAN_POINT ( 'NONE',  ( 2.020667218593132706E-15, -11.00000000000000000, 112.5625000040967763 ) ) ;
#69192=CARTESIAN_POINT ( 'NONE',  ( 7.204075437095966983, 7.204075437095967871, 82.09375000204838102 ) ) ;
#69196=CARTESIAN_POINT ( 'NONE',  ( 10.18810118750000093, -4.220049686691933921, 115.1875000020483668 ) ) ;
#69204=CARTESIAN_POINT ( 'NONE',  ( 10.18810118750000093, -4.220049686691933033, 79.18750000204836681 ) ) ;
#69217=CARTESIAN_POINT ( 'NONE',  ( -7.204075437095967871, 7.204075437095967871, 71.96875000204836681 ) ) ;
#69259=CARTESIAN_POINT ( 'NONE',  ( -6.735557395310442023E-16, 11.00000000000000000, 84.81250000409676204 ) ) ;
#69274=ORIENTED_EDGE ( 'NONE', *, *, #52790, .F. ) ;
#69284=CARTESIAN_POINT ( 'NONE',  ( 7.204075437095968759, -7.204075437095966983, 104.2187500020483810 ) ) ;
#69295=CARTESIAN_POINT ( 'NONE',  ( -11.00000000000000000, 0.000000000000000000, 100.1875000040967763 ) ) ;
#69299=CARTESIAN_POINT ( 'NONE',  ( 1.871523826299183495E-15, -10.18810118749999916, 95.40625000204836681 ) ) ;
#69313=CARTESIAN_POINT ( 'NONE',  ( 10.18810118750000093, -4.220049686691933921, 89.31250000204838102 ) ) ;
#69322=CARTESIAN_POINT ( 'NONE',  ( -4.220049686691935698, 10.18810118749999916, 72.25000000204836681 ) ) ;
#69331=CARTESIAN_POINT ( 'NONE',  ( 4.556349186104052151, -10.99999999999999822, 88.65625000409680467 ) ) ;
#69338=CARTESIAN_POINT ( 'NONE',  ( -10.18810118749999916, 4.220049686691934809, 70.56250000204836681 ) ) ;
#69341=CARTESIAN_POINT ( 'NONE',  ( -11.00000000000000000, 4.556349186104045934, 83.40624999999998579 ) ) ;
#69346=EDGE_CURVE ( 'NONE', #47864, #1216, #2462, .T. ) ;
#69348=DIRECTION ( 'NONE',  ( -1.000000000000000000, 0.000000000000000000, 0.000000000000000000 ) ) ;
#69356=CARTESIAN_POINT ( 'NONE',  ( 11.00000000000000000, 1.347111479062088405E-15, 97.93750000409677625 ) ) ;
#69370=CARTESIAN_POINT ( 'NONE',  ( -6.735557395310442023E-16, 11.00000000000000000, 68.31250000409677625 ) ) ;
#69382=CARTESIAN_POINT ( 'NONE',  ( 10.18810118750000093, -4.220049686691933033, 110.6875000020483810 ) ) ;
#69385=ORIENTED_EDGE ( 'NONE', *, *, #10436, .T. ) ;
#69387=CARTESIAN_POINT ( 'NONE',  ( -10.18810118749999916, 4.220049686691934809, 70.56250000204836681 ) ) ;
#69399=EDGE_CURVE ( 'NONE', #33983, #67283, #30446, .T. ) ;
#69416=CARTESIAN_POINT ( 'NONE',  ( -11.00000000000010658, 4.556349186103942017, 79.09375000409676204 ) ) ;
#69418=VERTEX_POINT ( 'NONE', #52824 ) ;
#69423=CARTESIAN_POINT ( 'NONE',  ( -7.204075437095967871, 7.204075437095967871, 85.46875000204836681 ) ) ;
#69426=CARTESIAN_POINT ( 'NONE',  ( 11.00000000000000355, -4.556349186104045046, 103.6562499999999858 ) ) ;
#69454=CARTESIAN_POINT ( 'NONE',  ( 7.778174593052021635, 7.778174593052023411, 99.43749999999998579 ) ) ;
#69459=CARTESIAN_POINT ( 'NONE',  ( 11.00000000000000000, 1.347111479062088405E-15, 94.93750000409677625 ) ) ;
#69472=CARTESIAN_POINT ( 'NONE',  ( 0.000000000000000000, 0.000000000000000000, 118.0000000000000000 ) ) ;
#69482=CARTESIAN_POINT ( 'NONE',  ( 4.220049686691934809, 10.18810118749999916, 100.5625000020483668 ) ) ;
#69491=CARTESIAN_POINT ( 'NONE',  ( 10.18810118750000093, -4.220049686691933921, 105.8125000020483952 ) ) ;
#69493=ORIENTED_EDGE ( 'NONE', *, *, #44504, .F. ) ;
#69497=CARTESIAN_POINT ( 'NONE',  ( 4.556349186104052151, -10.99999999999999822, 76.65625000409676204 ) ) ;
#69500=CARTESIAN_POINT ( 'NONE',  ( -10.18810118749999916, 0.000000000000000000, 104.0312500020483810 ) ) ;
#69513=ORIENTED_EDGE ( 'NONE', *, *, #43108, .F. ) ;
#69514=VERTEX_POINT ( 'NONE', #47885 ) ;
#69515=CARTESIAN_POINT ( 'NONE',  ( -7.204075437095967871, 7.204075437095967871, 106.4687500020483810 ) ) ;
#69525=VECTOR ( 'NONE', #53761, 1000.000000000000000 ) ;
#69533=CARTESIAN_POINT ( 'NONE',  ( 11.00000000000000000, 1.347111479062088405E-15, 117.2500000000000000 ) ) ;
#69545=CARTESIAN_POINT ( 'NONE',  ( -4.556349186104047710, -10.99999999999999822, 112.4687500040967905 ) ) ;
#69559=ORIENTED_EDGE ( 'NONE', *, *, #18090, .T. ) ;
#69562=DIRECTION ( 'NONE',  ( -0.000000000000000000, -0.000000000000000000, -1.000000000000000000 ) ) ;
#69566=CARTESIAN_POINT ( 'NONE',  ( 1.871523826299183495E-15, -10.18810118749999916, 83.03125000204838102 ) ) ;
#69570=CARTESIAN_POINT ( 'NONE',  ( -10.18810118749999916, 4.220049686691934809, 114.4375000020483668 ) ) ;
#69579=CARTESIAN_POINT ( 'NONE',  ( -10.18810118749999738, -4.220049686691941915, 78.62500000204838102 ) ) ;
#69592=CARTESIAN_POINT ( 'NONE',  ( -7.204075437095965206, -7.204075437095968759, 70.84375000204836681 ) ) ;
#69606=ORIENTED_EDGE ( 'NONE', *, *, #59129, .F. ) ;
#69615=CARTESIAN_POINT ( 'NONE',  ( -4.556349186104045934, 11.00000000000000000, 74.40625000409677625 ) ) ;
#69616=EDGE_CURVE ( 'NONE', #73904, #5598, #33330, .T. ) ;
#69625=CARTESIAN_POINT ( 'NONE',  ( -4.556349186104045934, 11.00000000000000000, 80.21874999999997158 ) ) ;
#69630=CARTESIAN_POINT ( 'NONE',  ( 10.99999999999989342, 4.556349186104152515, 106.8437500000000000 ) ) ;
#69644=DIRECTION ( 'NONE',  ( 0.000000000000000000, 0.000000000000000000, 1.000000000000000000 ) ) ;
#69655=CARTESIAN_POINT ( 'NONE',  ( 7.204075437095968759, -7.204075437095966983, 102.7187500020483668 ) ) ;
#69672=CARTESIAN_POINT ( 'NONE',  ( 7.204075437095966983, 7.204075437095967871, 92.96875000204838102 ) ) ;
#69678=CARTESIAN_POINT ( 'NONE',  ( -6.238412754330611322E-16, 10.18810118749999916, 79.65625000204836681 ) ) ;
#69686=CARTESIAN_POINT ( 'NONE',  ( 10.18810118749999916, 1.247682550866122264E-15, 87.90625000204838102 ) ) ;
#69692=AXIS2_PLACEMENT_3D ( 'NONE', #73509, #27115, #17286 ) ;
#69698=CARTESIAN_POINT ( 'NONE',  ( -10.18810118749999916, 0.000000000000000000, 74.03125000204838102 ) ) ;
#69703=EDGE_CURVE ( 'NONE', #24157, #16043, #43420, .T. ) ;
#69714=CARTESIAN_POINT ( 'NONE',  ( 7.204075437095966983, 7.204075437095967871, 68.59375000204836681 ) ) ;
#69717=CARTESIAN_POINT ( 'NONE',  ( 11.00000000000000355, -4.556349186104045046, 81.15624999999997158 ) ) ;
#69720=DIRECTION ( 'NONE',  ( -1.000000000000000000, 0.000000000000000000, 0.000000000000000000 ) ) ;
#69721=ORIENTED_EDGE ( 'NONE', *, *, #3618, .T. ) ;
#69737=DIRECTION ( 'NONE',  ( -0.000000000000000000, -0.000000000000000000, -1.000000000000000000 ) ) ;
#69744=CARTESIAN_POINT ( 'NONE',  ( 4.220049686691934809, 10.18810118749999916, 116.6875000020483952 ) ) ;
#69756=CARTESIAN_POINT ( 'NONE',  ( 10.18810118749999916, 4.220049686691935698, 112.3750000020483810 ) ) ;
#69760=CARTESIAN_POINT ( 'NONE',  ( -10.18810118749999916, 0.000000000000000000, 67.65625000204836681 ) ) ;
#69783=VERTEX_POINT ( 'NONE', #48625 ) ;
#69795=CARTESIAN_POINT ( 'NONE',  ( 7.204075437095966983, 7.204075437095967871, 83.59375000204836681 ) ) ;
#69798=CARTESIAN_POINT ( 'NONE',  ( -11.00000000000000000, 0.000000000000000000, 103.0000000000000000 ) ) ;
#69830=CARTESIAN_POINT ( 'NONE',  ( 11.00000000000000355, -4.556349186104045046, 87.34375000409679046 ) ) ;
#69854=DIRECTION ( 'NONE',  ( -1.000000000000000000, 0.000000000000000000, 0.000000000000000000 ) ) ;
#69857=CARTESIAN_POINT ( 'NONE',  ( 10.18810118750000093, -4.220049686691933921, 94.18750000204836681 ) ) ;
#69863=CARTESIAN_POINT ( 'NONE',  ( -10.18810118749999738, -4.220049686691941915, 109.7500000020483810 ) ) ;
#69865=ORIENTED_EDGE ( 'NONE', *, *, #21008, .F. ) ;
#69871=CARTESIAN_POINT ( 'NONE',  ( 10.18810118749999916, 1.247682550866122264E-15, 101.7812500020483810 ) ) ;
#69873=EDGE_CURVE ( 'NONE', #70285, #25175, #69016, .T. ) ;
#69890=CARTESIAN_POINT ( 'NONE',  ( -7.204075437095967871, 7.204075437095967871, 103.4687500020483668 ) ) ;
#69909=CARTESIAN_POINT ( 'NONE',  ( -4.220049686691935698, 10.18810118749999916, 69.25000000204836681 ) ) ;
#69921=CARTESIAN_POINT ( 'NONE',  ( -4.556349186104045934, 11.00000000000000000, 104.4062500040967620 ) ) ;
#69938=CYLINDRICAL_SURFACE ( 'NONE', #55583, 11.00000000000000000 ) ;
#69941=CARTESIAN_POINT ( 'NONE',  ( 7.204075437095966983, 7.204075437095967871, 85.09375000204836681 ) ) ;
#69945=CARTESIAN_POINT ( 'NONE',  ( 4.220049686691934809, 10.18810118749999916, 111.0625000020483810 ) ) ;
#69947=CARTESIAN_POINT ( 'NONE',  ( 10.99999999999999467, 11.00000000000000355, 41.99999999999999289 ) ) ;
#69952=CARTESIAN_POINT ( 'NONE',  ( 4.220049686691934809, 10.18810118749999916, 78.06250000204836681 ) ) ;
#69954=VERTEX_POINT ( 'NONE', #36133 ) ;
#69967=CARTESIAN_POINT ( 'NONE',  ( -7.204075437095967871, 7.204075437095967871, 73.46875000204838102 ) ) ;
#69978=CARTESIAN_POINT ( 'NONE',  ( 11.00000000000000000, 4.556349186104045934, 93.53125000409676204 ) ) ;
#69991=( BOUNDED_CURVE ( )  B_SPLINE_CURVE ( 2, ( #49927, #20876, #8441, #55605, #65782, #49553, #21251, #3923, #31461, #3537, #48798, #66523, #71807, #14834, #4288, #20125, #43897, #26154, #9193, #15214, #31835, #26529, #25778, #73318, #66909, #43140, #54486, #38244, #44275, #67286, #37497, #14460, #54854, #15585, #38625, #3165, #61627, #27280, #50297, #21622, #52171, #34091, #68394, #68027, #11429, #57087, #10315, #5776, #17449, #56719, #69142, #39724, #135, #6146, #23111, #16692, #62725, #39356, #51045, #34466, #29153, #45379, #50664, #503, #44645, #5037, #11063, #5403, #74055, #28405, #67660, #27656, #15959, #45753, #51413, #11797, #62353, #10684, #74427, #21995, #63104, #28034, #22354, #22733, #73683, #38988, #68766, #17077, #40099, #16321, #61993, #33341, #57469, #28772, #33717, #51787, #46124, #40470, #56343, #4662, #45021, #63475, #34835, #57842, #35562, #46494, #17828, #65322, #64223, #58574, #46868, #1959, #64596, #24949, #69515, #58946, #18936, #47966, #52906, #24217, #47231, #52534, #59675, #872, #41942, #12893, #64950, #7252, #40841, #41215, #70259, #18571, #13627, #23858, #35199, #12164, #35929, #30263, #53280, #12531, #6882, #36665, #42306, #63850, #58216, #6517, #69890, #30627, #29524, #29893, #13260, #36296, #41581, #1605, #70616, #59315, #7620, #53649, #18202, #1240, #24589, #7986, #70981, #19296, #30992, #54014, #47594, #23482, #8349, #20031, #55140, #26058, #67197, #20786, #20406, #3826, #21160, #60781, #60404, #38532, #26823, #3445, #43422, #49079, #15495, #72092, #38155, #61533, #37785, #43044, #32502, #72855, #55514, #61156, #25688, #49836, #8731, #9488, #44183, #9856, #26434, #31744, #49460, #66063, #60031, #32884, #9106, #25319, #2324, #48335, #71343, #72479, #19665, #31365, #71715, #43806, #32120, #37030, #42677, #14745, #54393, #65689, #14370, #2700, #13989, #48708, #37403, #66821, #54764, #3073, #15123, #66435, #45661, #4201, #22270, #67937, #45293, #4946, #4569, #22641, #68305, #27190, #50207, #23028, #21900, #16231, #27567, #34374, #16603, #57374, #73227, #39640, #51324, #5683, #10597, #56632, #27945, #61901, #17360, #11705, #39268, #62637, #68676, #10970, #21533, #73592, #50953, #73964, #46035, #56252, #67569, #44556, #34005, #56999, #5313, #44930, #62268, #33625, #28315, #40012, #15866, #38898, #50575, #63014, #10225, #74332, #16985, #11339, #28683, #51696, #42, #69055, #40383, #63382, #33253, #55886, #29803, #13170, #53187, #6055, #30171, #24859, #58486, #23394, #40747, #52446, #12807, #6794, #47878, #1525, #52815, #36206, #53557, #18481, #18112, #70897, #59223, #17731, #41125, #46771, #18849, #1149, #70534, #19212, #70173, #784, #64867, #30541, #7535, #41856, #58124, #1873, #64133, #24128, #47141, #42217, #35111, #46409, #69423, #41492, #64508, #24503, #6433, #47508, #65229, #34746, #57750, #29061, #63757, #29435, #52082, #414, #12440, #12074, #23767, #35838, #58854, #7165, #69795, #35473, #60695, #2614, #25231, #21074, #49751, #43715, #55049, #3732, #26731, #37316, #2237, #19574, #31275, #66350, #60313, #72768, #32029, #31655, #15033, #32410, #71999, #14654, #42589, #25967, #37695, #54676, #8641, #44098, #2982, #49367, #13533, #48989, #54303, #66729, #9390, #38069, #72384, #36941, #61068, #71624, #20697, #55423, #9015, #36572, #65604, #8261, #3356, #20314, #48248, #59585, #43331, #13902, #7899, #26346, #30904, #53924, #59946, #71255, #25604, #19946, #48617, #42955, #65974, #14278, #15402, #33541, #4483, #56542, #16139, #15779, #33916, #4859, #32790, #28230, #39925, #27474, #16899, #62182, #22557, #28601, #45578, #38441, #27855, #62551, #68593, #21808, #67848, #39178, #73138, #51612, #22944, #50488, #10509, #50864, #44841, #73880, #74628, #50122, #73501, #51238, #11256, #22184, #45209, #68220, #16517, #10134, #21444, #74249, #39557, #61444, #33172, #10882, #34285, #56170, #44467, #62931, #67480, #38817, #56916, #61816, #5229, #57289, #5603, #67106, #4114, #9771, #55798, #27107, #11623, #58408, #58041, #6355, #68968, #40294, #13088, #11997, #29359, #69338, #24422, #12363, #47429, #41044, #40667, #52365, #12724, #30460, #17648, #18028, #331, #7453, #23312, #41414, #35398, #35757, #6714, #63295, #63670, #64052, #69714, #36123, #46324, #35029, #701, #29721, #23684, #64426, #46690, #58774, #59144, #64787, #17277, #34661, #57664, #52735, #53107 ),
 .UNSPECIFIED., .F., .F. ) 
 B_SPLINE_CURVE_WITH_KNOTS ( ( 3, 2, 2, 2, 2, 2, 2, 2, 2, 2, 2, 2, 2, 2, 2, 2, 2, 2, 2, 2, 2, 2, 2, 2, 2, 2, 2, 2, 2, 2, 2, 2, 2, 2, 2, 2, 2, 2, 2, 2, 2, 2, 2, 2, 2, 2, 2, 2, 2, 2, 2, 2, 2, 2, 2, 2, 2, 2, 2, 2, 2, 2, 2, 2, 2, 2, 2, 2, 2, 2, 2, 2, 2, 2, 2, 2, 2, 2, 2, 2, 2, 2, 2, 2, 2, 2, 2, 2, 2, 2, 2, 2, 2, 2, 2, 2, 2, 2, 2, 2, 2, 2, 2, 2, 2, 2, 2, 2, 2, 2, 2, 2, 2, 2, 2, 2, 2, 2, 2, 2, 2, 2, 2, 2, 2, 2, 2, 2, 2, 2, 2, 2, 2, 2, 2, 2, 2, 2, 2, 2, 2, 2, 2, 2, 2, 2, 2, 2, 2, 2, 2, 2, 2, 2, 2, 2, 2, 2, 2, 2, 2, 2, 2, 2, 2, 2, 2, 2, 2, 2, 2, 2, 2, 2, 2, 2, 2, 2, 2, 2, 2, 2, 2, 2, 2, 2, 2, 2, 2, 2, 2, 2, 2, 2, 2, 2, 2, 2, 2, 2, 2, 2, 2, 2, 2, 2, 2, 2, 2, 2, 2, 2, 2, 2, 2, 2, 2, 2, 2, 2, 2, 2, 2, 2, 2, 2, 2, 2, 2, 2, 2, 2, 2, 2, 2, 2, 2, 2, 2, 2, 2, 2, 2, 2, 2, 2, 2, 2, 2, 2, 2, 2, 2, 2, 2, 2, 2, 2, 2, 2, 2, 2, 2, 2, 2, 2, 2, 3 ),
 ( 0.000000000000000000, 0.003750026907760104986, 0.007500053815520209971, 0.01125008072328031496, 0.01500010763104041994, 0.01875013453880052666, 0.02250016144656062991, 0.02625018835432073316, 0.03000021526208083988, 0.03375024216984094660, 0.03750026907760105332, 0.04125029598536116004, 0.04500032289312125983, 0.04875034980088135961, 0.05250037670864146633, 0.05625040361640157305, 0.06000043052416167977, 0.06375045743192178649, 0.06750048433968189321, 0.07125051124744199993, 0.07500053815520210665, 0.07875056506296221337, 0.08250059197072232009, 0.08625061887848241293, 0.09000064578624251965, 0.09375067269400262637, 0.09750069960176271922, 0.1012507265095228259, 0.1050007534172829327, 0.1087507803250430394, 0.1125008072328031461, 0.1162508341405632528, 0.1200008610483233595, 0.1237508879560834663, 0.1275009148638435730, 0.1312509417716036519, 0.1350009686793637864, 0.1387509955871238654, 0.1425010224948839999, 0.1462510494026440788, 0.1500010763104042133, 0.1537511032181642923, 0.1575011301259244267, 0.1612511570336845057, 0.1650011839414446402, 0.1687512108492047191, 0.1725012377569648259, 0.1762512646647249326, 0.1800012915724850393, 0.1837513184802451460, 0.1875013453880052527, 0.1912513722957653595, 0.1950013992035254384, 0.1987514261112855729, 0.2025014530190456519, 0.2062514799268057863, 0.2100015068345658653, 0.2137515337423259998, 0.2175015606500860788, 0.2212515875578462132, 0.2250016144656062922, 0.2287516413733663989, 0.2325016682811265056, 0.2362516951888866124, 0.2400017220966467191, 0.2437517490044068258, 0.2475017759121669325, 0.2512518028199270392, 0.2550018297276871460, 0.2587518566354472527, 0.2625018835432073039, 0.2662519104509674661, 0.2700019373587275728, 0.2737519642664876796, 0.2775019911742477308, 0.2812520180820078930, 0.2850020449897679997, 0.2887520718975280509, 0.2925020988052881576, 0.2962521257130483199, 0.3000021526208084266, 0.3037521795285684778, 0.3075022064363285845, 0.3112522333440887468, 0.3150022602518488535, 0.3187522871596089047, 0.3225023140673690114, 0.3262523409751291181, 0.3300023678828892804, 0.3337523947906493316, 0.3375024216984094383, 0.3412524486061695450, 0.3450024755139296517, 0.3487525024216897584, 0.3525025293294498652, 0.3562525562372099719, 0.3600025831449700786, 0.3637526100527301853, 0.3675026369604902921, 0.3712526638682503988, 0.3750026907760105055, 0.3787527176837706122, 0.3825027445915307189, 0.3862527714992908257, 0.3900027984070508769, 0.3937528253148110391, 0.3975028522225711458, 0.4012528791303311970, 0.4050029060380913037, 0.4087529329458514660, 0.4125029598536115727, 0.4162529867613716239, 0.4200030136691317306, 0.4237530405768918929, 0.4275030674846519996, 0.4312530943924120508, 0.4350031213001721575, 0.4387531482079323197, 0.4425031751156924265, 0.4462532020234524777, 0.4500032289312125844, 0.4537532558389726911, 0.4575032827467327978, 0.4612533096544929045, 0.4650033365622530113, 0.4687533634700131180, 0.4725033903777732247, 0.4762534172855333314, 0.4800034441932934381, 0.4837534711010535449, 0.4875034980088136516, 0.4912535249165737583, 0.4950035518243338650, 0.4987535787320939717, 0.5025036056398540785, 0.5062536325476142407, 0.5100036594553742919, 0.5137536863631343431, 0.5175037132708945053, 0.5212537401786545566, 0.5250037670864146078, 0.5287537939941748810, 0.5325038209019349322, 0.5362538478096949834, 0.5400038747174551457, 0.5437539016252151969, 0.5475039285329753591, 0.5512539554407354103, 0.5550039823484954615, 0.5587540092562557348, 0.5625040361640157860, 0.5662540630717758372, 0.5700040899795359994, 0.5737541168872960506, 0.5775041437950561019, 0.5812541707028162641, 0.5850041976105763153, 0.5887542245183364775, 0.5925042514260966398, 0.5962542783338566910, 0.6000043052416168532, 0.6037543321493769044, 0.6075043590571369556, 0.6112543859648971178, 0.6150044128726571691, 0.6187544397804173313, 0.6225044666881774935, 0.6262544935959375447, 0.6300045205036977070, 0.6337545474114577582, 0.6375045743192178094, 0.6412546012269779716, 0.6450046281347380228, 0.6487546550424980740, 0.6525046819502582363, 0.6562547088580183985, 0.6600047357657785607, 0.6637547626735386119, 0.6675047895812986631, 0.6712548164890588254, 0.6750048433968188766, 0.6787548703045789278, 0.6825048972123390900, 0.6862549241200992522, 0.6900049510278593035, 0.6937549779356194657, 0.6975050048433795169, 0.7012550317511396791, 0.7050050586588997303, 0.7087550855666597815, 0.7125051124744199438, 0.7162551393821799950, 0.7200051662899401572, 0.7237551931977003195, 0.7275052201054603707, 0.7312552470132205329, 0.7350052739209805841, 0.7387553008287406353, 0.7425053277365007975, 0.7462553546442608488, 0.7500053815520210110, 0.7537554084597811732, 0.7575054353675412244, 0.7612554622753012756, 0.7650054891830614379, 0.7687555160908214891, 0.7725055429985816513, 0.7762555699063417025, 0.7800055968141017537, 0.7837556237218620270, 0.7875056506296220782, 0.7912556775373821294, 0.7950057044451422916, 0.7987557313529023428, 0.8025057582606623940, 0.8062557851684225563, 0.8100058120761826075, 0.8137558389839428807, 0.8175058658917029319, 0.8212558927994629832, 0.8250059197072231454, 0.8287559466149831966, 0.8325059735227432478, 0.8362560004305034100, 0.8400060273382634612, 0.8437560542460236235, 0.8475060811537837857, 0.8512561080615438369, 0.8550061349693039991, 0.8587561618770640504, 0.8625061887848241016, 0.8662562156925842638, 0.8700062426003443150, 0.8737562695081043662, 0.8775062964158646395, 0.8812563233236246907, 0.8850063502313848529, 0.8887563771391449041, 0.8925064040469049553, 0.8962564309546651176, 0.9000064578624251688, 0.9037564847701852200, 0.9075065116779453822, 0.9112565385857055444, 0.9150065654934655957, 0.9187565924012257579, 0.9225066193089858091, 0.9262566462167459713, 0.9300066731245060225, 0.9337567000322660737, 0.9375067269400262360, 0.9412567538477863982, 0.9450067807555464494, 0.9487568076633066116, 0.9525068345710666629, 0.9562568614788268251, 0.9600068883865868763, 0.9637569152943469275, 0.9675069422021070897, 0.9712569691098671409, 0.9750069960176273032, 0.9787570229253874654, 0.9825070498331475166, 0.9862570767409075678, 0.9900071036486677301, 0.9937571305564277813, 0.9975071574641879435, 1.000000000000000000 ),
 .UNSPECIFIED. ) 
 CURVE ( )  GEOMETRIC_REPRESENTATION_ITEM ( )  RATIONAL_B_SPLINE_CURVE ( ( 1.000000000000000000, 0.9238795325112867385, 1.000000000000000000, 0.9238795325112867385, 1.000000000000000000, 0.9238795325112867385, 1.000000000000000000, 0.9238795325112867385, 1.000000000000000000, 0.9238795325112867385, 1.000000000000000000, 0.9238795325112867385, 1.000000000000000000, 0.9238795325112867385, 1.000000000000000000, 0.9238795325112867385, 1.000000000000000000, 0.9238795325112867385, 1.000000000000000000, 0.9238795325112867385, 1.000000000000000000, 0.9238795325112867385, 1.000000000000000000, 0.9238795325112867385, 1.000000000000000000, 0.9238795325112867385, 1.000000000000000000, 0.9238795325112867385, 1.000000000000000000, 0.9238795325112867385, 1.000000000000000000, 0.9238795325112867385, 1.000000000000000000, 0.9238795325112867385, 1.000000000000000000, 0.9238795325112867385, 1.000000000000000000, 0.9238795325112867385, 1.000000000000000000, 0.9238795325112867385, 1.000000000000000000, 0.9238795325112867385, 1.000000000000000000, 0.9238795325112867385, 1.000000000000000000, 0.9238795325112867385, 1.000000000000000000, 0.9238795325112867385, 1.000000000000000000, 0.9238795325112867385, 1.000000000000000000, 0.9238795325112867385, 1.000000000000000000, 0.9238795325112867385, 1.000000000000000000, 0.9238795325112867385, 1.000000000000000000, 0.9238795325112867385, 1.000000000000000000, 0.9238795325112867385, 1.000000000000000000, 0.9238795325112867385, 1.000000000000000000, 0.9238795325112867385, 1.000000000000000000, 0.9238795325112867385, 1.000000000000000000, 0.9238795325112867385, 1.000000000000000000, 0.9238795325112867385, 1.000000000000000000, 0.9238795325112867385, 1.000000000000000000, 0.9238795325112867385, 1.000000000000000000, 0.9238795325112867385, 1.000000000000000000, 0.9238795325112867385, 1.000000000000000000, 0.9238795325112867385, 1.000000000000000000, 0.9238795325112867385, 1.000000000000000000, 0.9238795325112867385, 1.000000000000000000, 0.9238795325112867385, 1.000000000000000000, 0.9238795325112867385, 1.000000000000000000, 0.9238795325112867385, 1.000000000000000000, 0.9238795325112867385, 1.000000000000000000, 0.9238795325112867385, 1.000000000000000000, 0.9238795325112867385, 1.000000000000000000, 0.9238795325112867385, 1.000000000000000000, 0.9238795325112867385, 1.000000000000000000, 0.9238795325112867385, 1.000000000000000000, 0.9238795325112867385, 1.000000000000000000, 0.9238795325112867385, 1.000000000000000000, 0.9238795325112867385, 1.000000000000000000, 0.9238795325112867385, 1.000000000000000000, 0.9238795325112867385, 1.000000000000000000, 0.9238795325112867385, 1.000000000000000000, 0.9238795325112867385, 1.000000000000000000, 0.9238795325112867385, 1.000000000000000000, 0.9238795325112867385, 1.000000000000000000, 0.9238795325112867385, 1.000000000000000000, 0.9238795325112867385, 1.000000000000000000, 0.9238795325112867385, 1.000000000000000000, 0.9238795325112867385, 1.000000000000000000, 0.9238795325112867385, 1.000000000000000000, 0.9238795325112867385, 1.000000000000000000, 0.9238795325112867385, 1.000000000000000000, 0.9238795325112867385, 1.000000000000000000, 0.9238795325112867385, 1.000000000000000000, 0.9238795325112867385, 1.000000000000000000, 0.9238795325112867385, 1.000000000000000000, 0.9238795325112867385, 1.000000000000000000, 0.9238795325112867385, 1.000000000000000000, 0.9238795325112867385, 1.000000000000000000, 0.9238795325112867385, 1.000000000000000000, 0.9238795325112867385, 1.000000000000000000, 0.9238795325112867385, 1.000000000000000000, 0.9238795325112867385, 1.000000000000000000, 0.9238795325112867385, 1.000000000000000000, 0.9238795325112867385, 1.000000000000000000, 0.9238795325112867385, 1.000000000000000000, 0.9238795325112867385, 1.000000000000000000, 0.9238795325112867385, 1.000000000000000000, 0.9238795325112867385, 1.000000000000000000, 0.9238795325112867385, 1.000000000000000000, 0.9238795325112867385, 1.000000000000000000, 0.9238795325112867385, 1.000000000000000000, 0.9238795325112867385, 1.000000000000000000, 0.9238795325112867385, 1.000000000000000000, 0.9238795325112867385, 1.000000000000000000, 0.9238795325112867385, 1.000000000000000000, 0.9238795325112867385, 1.000000000000000000, 0.9238795325112867385, 1.000000000000000000, 0.9238795325112867385, 1.000000000000000000, 0.9238795325112867385, 1.000000000000000000, 0.9238795325112867385, 1.000000000000000000, 0.9238795325112867385, 1.000000000000000000, 0.9238795325112867385, 1.000000000000000000, 0.9238795325112867385, 1.000000000000000000, 0.9238795325112867385, 1.000000000000000000, 0.9238795325112867385, 1.000000000000000000, 0.9238795325112867385, 1.000000000000000000, 0.9238795325112867385, 1.000000000000000000, 0.9238795325112867385, 1.000000000000000000, 0.9238795325112867385, 1.000000000000000000, 0.9238795325112867385, 1.000000000000000000, 0.9238795325112867385, 1.000000000000000000, 0.9238795325112867385, 1.000000000000000000, 0.9238795325112867385, 1.000000000000000000, 0.9238795325112867385, 1.000000000000000000, 0.9238795325112867385, 1.000000000000000000, 0.9238795325112867385, 1.000000000000000000, 0.9238795325112867385, 1.000000000000000000, 0.9238795325112867385, 1.000000000000000000, 0.9238795325112867385, 1.000000000000000000, 0.9238795325112867385, 1.000000000000000000, 0.9238795325112867385, 1.000000000000000000, 0.9238795325112867385, 1.000000000000000000, 0.9238795325112867385, 1.000000000000000000, 0.9238795325112867385, 1.000000000000000000, 0.9238795325112867385, 1.000000000000000000, 0.9238795325112867385, 1.000000000000000000, 0.9238795325112867385, 1.000000000000000000, 0.9238795325112867385, 1.000000000000000000, 0.9238795325112867385, 1.000000000000000000, 0.9238795325112867385, 1.000000000000000000, 0.9238795325112867385, 1.000000000000000000, 0.9238795325112867385, 1.000000000000000000, 0.9238795325112867385, 1.000000000000000000, 0.9238795325112867385, 1.000000000000000000, 0.9238795325112867385, 1.000000000000000000, 0.9238795325112867385, 1.000000000000000000, 0.9238795325112867385, 1.000000000000000000, 0.9238795325112867385, 1.000000000000000000, 0.9238795325112867385, 1.000000000000000000, 0.9238795325112867385, 1.000000000000000000, 0.9238795325112867385, 1.000000000000000000, 0.9238795325112867385, 1.000000000000000000, 0.9238795325112867385, 1.000000000000000000, 0.9238795325112867385, 1.000000000000000000, 0.9238795325112867385, 1.000000000000000000, 0.9238795325112867385, 1.000000000000000000, 0.9238795325112867385, 1.000000000000000000, 0.9238795325112867385, 1.000000000000000000, 0.9238795325112867385, 1.000000000000000000, 0.9238795325112867385, 1.000000000000000000, 0.9238795325112867385, 1.000000000000000000, 0.9238795325112867385, 1.000000000000000000, 0.9238795325112867385, 1.000000000000000000, 0.9238795325112867385, 1.000000000000000000, 0.9238795325112867385, 1.000000000000000000, 0.9238795325112867385, 1.000000000000000000, 0.9238795325112867385, 1.000000000000000000, 0.9238795325112867385, 1.000000000000000000, 0.9238795325112867385, 1.000000000000000000, 0.9238795325112867385, 1.000000000000000000, 0.9238795325112867385, 1.000000000000000000, 0.9238795325112867385, 1.000000000000000000, 0.9238795325112867385, 1.000000000000000000, 0.9238795325112867385, 1.000000000000000000, 0.9238795325112867385, 1.000000000000000000, 0.9238795325112867385, 1.000000000000000000, 0.9238795325112867385, 1.000000000000000000, 0.9238795325112867385, 1.000000000000000000, 0.9238795325112867385, 1.000000000000000000, 0.9238795325112867385, 1.000000000000000000, 0.9238795325112867385, 1.000000000000000000, 0.9238795325112867385, 1.000000000000000000, 0.9238795325112867385, 1.000000000000000000, 0.9238795325112867385, 1.000000000000000000, 0.9238795325112867385, 1.000000000000000000, 0.9238795325112867385, 1.000000000000000000, 0.9238795325112867385, 1.000000000000000000, 0.9238795325112867385, 1.000000000000000000, 0.9238795325112867385, 1.000000000000000000, 0.9238795325112867385, 1.000000000000000000, 0.9238795325112867385, 1.000000000000000000, 0.9238795325112867385, 1.000000000000000000, 0.9238795325112867385, 1.000000000000000000, 0.9238795325112867385, 1.000000000000000000, 0.9238795325112867385, 1.000000000000000000, 0.9238795325112867385, 1.000000000000000000, 0.9238795325112867385, 1.000000000000000000, 0.9238795325112867385, 1.000000000000000000, 0.9238795325112867385, 1.000000000000000000, 0.9238795325112867385, 1.000000000000000000, 0.9238795325112867385, 1.000000000000000000, 0.9238795325112867385, 1.000000000000000000, 0.9238795325112867385, 1.000000000000000000, 0.9238795325112867385, 1.000000000000000000, 0.9238795325112867385, 1.000000000000000000, 0.9238795325112867385, 1.000000000000000000, 0.9238795325112867385, 1.000000000000000000, 0.9238795325112867385, 1.000000000000000000, 0.9238795325112867385, 1.000000000000000000, 0.9238795325112867385, 1.000000000000000000, 0.9238795325112867385, 1.000000000000000000, 0.9238795325112867385, 1.000000000000000000, 0.9238795325112867385, 1.000000000000000000, 0.9238795325112867385, 1.000000000000000000, 0.9238795325112867385, 1.000000000000000000, 0.9238795325112867385, 1.000000000000000000, 0.9238795325112867385, 1.000000000000000000, 0.9238795325112867385, 1.000000000000000000, 0.9238795325112867385, 1.000000000000000000, 0.9238795325112867385, 1.000000000000000000, 0.9238795325112867385, 1.000000000000000000, 0.9238795325112867385, 1.000000000000000000, 0.9238795325112867385, 1.000000000000000000, 0.9238795325112867385, 1.000000000000000000, 0.9238795325112867385, 1.000000000000000000, 0.9238795325112867385, 1.000000000000000000, 0.9238795325112867385, 1.000000000000000000, 0.9238795325112867385, 1.000000000000000000, 0.9238795325112867385, 1.000000000000000000, 0.9238795325112867385, 1.000000000000000000, 0.9238795325112867385, 1.000000000000000000, 0.9238795325112867385, 1.000000000000000000, 0.9238795325112867385, 1.000000000000000000, 0.9238795325112867385, 1.000000000000000000, 0.9238795325112867385, 1.000000000000000000, 0.9238795325112867385, 1.000000000000000000, 0.9238795325112867385, 1.000000000000000000, 0.9238795325112867385, 1.000000000000000000, 0.9238795325112867385, 1.000000000000000000, 0.9238795325112867385, 1.000000000000000000, 0.9238795325112867385, 1.000000000000000000, 0.9238795325112867385, 1.000000000000000000, 0.9238795325112867385, 1.000000000000000000, 0.9238795325112867385, 1.000000000000000000, 0.9238795325112867385, 1.000000000000000000, 0.9238795325112867385, 1.000000000000000000, 0.9238795325112867385, 1.000000000000000000, 0.9238795325112867385, 1.000000000000000000, 0.9238795325112867385, 1.000000000000000000, 0.9238795325112867385, 1.000000000000000000, 0.9238795325112867385, 1.000000000000000000, 0.9238795325112867385, 1.000000000000000000, 0.9238795325112867385, 1.000000000000000000, 0.9238795325112867385, 1.000000000000000000, 0.9238795325112867385, 1.000000000000000000, 0.9238795325112867385, 1.000000000000000000, 0.9238795325112867385, 1.000000000000000000, 0.9238795325112867385, 1.000000000000000000, 0.9238795325112867385, 1.000000000000000000, 0.9238795325112867385, 1.000000000000000000, 0.9238795325112867385, 1.000000000000000000, 0.9238795325112867385, 1.000000000000000000, 0.9238795325112867385, 1.000000000000000000, 0.9238795325112867385, 1.000000000000000000, 0.9238795325112867385, 1.000000000000000000, 0.9238795325112867385, 1.000000000000000000, 0.9238795325112867385, 1.000000000000000000, 0.9238795325112867385, 1.000000000000000000, 0.9238795325112867385, 1.000000000000000000, 0.9238795325112867385, 1.000000000000000000, 0.9238795325112867385, 1.000000000000000000, 0.9238795325112867385, 1.000000000000000000, 0.9238795325112867385, 1.000000000000000000, 0.9238795325112867385, 1.000000000000000000, 0.9238795325112867385, 1.000000000000000000, 0.9238795325112867385, 1.000000000000000000, 0.9238795325112867385, 1.000000000000000000, 0.9238795325112867385, 1.000000000000000000, 0.9238795325112867385, 1.000000000000000000, 0.9238795325112867385, 1.000000000000000000, 0.9493986726310960078, 0.9660721378631347278 ) ) 
 REPRESENTATION_ITEM ( '' )  );
#70002=CARTESIAN_POINT ( 'NONE',  ( 11.00000000000000000, 1.347111479062088405E-15, 90.25000000000000000 ) ) ;
#70005=CARTESIAN_POINT ( 'NONE',  ( -7.778174593052023411, 7.778174593052023411, 76.00000000409676204 ) ) ;
#70024=EDGE_LOOP ( 'NONE', ( #41175, #27555, #49394, #25603 ) ) ;
#70031=CARTESIAN_POINT ( 'NONE',  ( -7.268158626439248593, 8.014265980700427505, 117.6910954969439587 ) ) ;
#70032=CARTESIAN_POINT ( 'NONE',  ( -10.18810118749999916, 4.220049686691934809, 103.5625000020483668 ) ) ;
#70049=CARTESIAN_POINT ( 'NONE',  ( -7.204075437095965206, -7.204075437095968759, 96.71875000204838102 ) ) ;
#70053=FACE_OUTER_BOUND ( 'NONE', #38151, .T. ) ;
#70055=CARTESIAN_POINT ( 'NONE',  ( -7.204075437095965206, -7.204075437095968759, 77.21875000204836681 ) ) ;
#70065=CARTESIAN_POINT ( 'NONE',  ( 10.18810118749999916, 4.220049686691935698, 91.00000000204836681 ) ) ;
#70076=CARTESIAN_POINT ( 'NONE',  ( 7.204075437095966983, 7.204075437095967871, 73.46875000204838102 ) ) ;
#70096=CARTESIAN_POINT ( 'NONE',  ( 11.00000000000000000, 4.556349186104045934, 85.84374999999998579 ) ) ;
#70121=CARTESIAN_POINT ( 'NONE',  ( -11.00000000000001776, -4.556349186104032611, 116.5937499999999858 ) ) ;
#70123=CARTESIAN_POINT ( 'NONE',  ( -7.778174593052023411, 7.778174593052023411, 68.50000000409677625 ) ) ;
#70130=EDGE_CURVE ( 'NONE', #36433, #2613, #41031, .T. ) ;
#70135=CARTESIAN_POINT ( 'NONE',  ( 7.204075437095966983, 7.204075437095967871, 115.4687500020483810 ) ) ;
#70137=ORIENTED_EDGE ( 'NONE', *, *, #4386, .T. ) ;
#70139=CARTESIAN_POINT ( 'NONE',  ( -10.18810118749999916, 4.220049686691934809, 67.56250000204836681 ) ) ;
#70173=CARTESIAN_POINT ( 'NONE',  ( -6.238412754330611322E-16, 10.18810118749999916, 86.78125000204836681 ) ) ;
#70175=CARTESIAN_POINT ( 'NONE',  ( -6.735557395310442023E-16, 11.00000000000000000, 101.1249999999999858 ) ) ;
#70200=CARTESIAN_POINT ( 'NONE',  ( 10.99999999999994849, 4.556349186104097448, 99.34375000000000000 ) ) ;
#70201=DIRECTION ( 'NONE',  ( -1.000000000000000000, 0.000000000000000000, 0.000000000000000000 ) ) ;
#70206=CARTESIAN_POINT ( 'NONE',  ( -10.99999999999999822, -4.556349186104052151, 86.78125000409679046 ) ) ;
#70230=CARTESIAN_POINT ( 'NONE',  ( -10.18810118749999916, 0.000000000000000000, 93.53125000204836681 ) ) ;
#70237=CARTESIAN_POINT ( 'NONE',  ( 4.220049686691934809, 10.18810118749999916, 100.1875000020483668 ) ) ;
#70246=CARTESIAN_POINT ( 'NONE',  ( -10.18810118749999916, 0.000000000000000000, 101.0312500020483810 ) ) ;
#70259=CARTESIAN_POINT ( 'NONE',  ( -7.204075437095967871, 7.204075437095967871, 104.9687500020483810 ) ) ;
#70263=CARTESIAN_POINT ( 'NONE',  ( -11.00000000000000000, 0.000000000000000000, 68.68750000409676204 ) ) ;
#70277=CARTESIAN_POINT ( 'NONE',  ( -7.778174593052023411, 7.778174593052023411, 116.3125000000000000 ) ) ;
#70285=VERTEX_POINT ( 'NONE', #9602 ) ;
#70288=CARTESIAN_POINT ( 'NONE',  ( -11.00000000000000000, 0.000000000000000000, 103.1875000040967763 ) ) ;
#70293=CARTESIAN_POINT ( 'NONE',  ( 2.020667218593132706E-15, -11.00000000000000000, 108.0625000040967905 ) ) ;
#70307=CARTESIAN_POINT ( 'NONE',  ( 10.18810118749999916, 1.247682550866122264E-15, 80.40625000204838102 ) ) ;
#70311=CARTESIAN_POINT ( 'NONE',  ( 7.204075437095968759, -7.204075437095966983, 107.5937500020483810 ) ) ;
#70320=CARTESIAN_POINT ( 'NONE',  ( -10.18810118749999916, 0.000000000000000000, 80.03125000204836681 ) ) ;
#70332=CARTESIAN_POINT ( 'NONE',  ( 10.18810118749999916, 4.220049686691935698, 73.00000000204836681 ) ) ;
#70336=EDGE_CURVE ( 'NONE', #6126, #69954, #67018, .T. ) ;
#70338=FACE_OUTER_BOUND ( 'NONE', #73030, .T. ) ;
#70375=EDGE_CURVE ( 'NONE', #60482, #1123, #38153, .T. ) ;
#70376=ORIENTED_EDGE ( 'NONE', *, *, #65738, .F. ) ;
#70397=CARTESIAN_POINT ( 'NONE',  ( 7.204075437095968759, -7.204075437095966983, 101.2187500020483668 ) ) ;
#70408=CARTESIAN_POINT ( 'NONE',  ( -4.556349186104045934, 11.00000000000000000, 83.40625000409676204 ) ) ;
#70412=CARTESIAN_POINT ( 'NONE',  ( 4.220049686691934809, 10.18810118749999916, 93.06250000204838102 ) ) ;
#70415=CARTESIAN_POINT ( 'NONE',  ( 11.00000000000000000, 1.347111479062088405E-15, 118.0000000000000000 ) ) ;
#70416=DIRECTION ( 'NONE',  ( -1.000000000000000000, 0.000000000000000000, 0.000000000000000000 ) ) ;
#70417=CARTESIAN_POINT ( 'NONE',  ( 7.778174593052021635, 7.778174593052023411, 102.4374999999999858 ) ) ;
#70418=CARTESIAN_POINT ( 'NONE',  ( -6.238412754330611322E-16, 10.18810118749999916, 75.15625000204836681 ) ) ;
#70421=DIRECTION ( 'NONE',  ( 1.000000000000000000, 0.000000000000000000, 0.000000000000000000 ) ) ;
#70423=CYLINDRICAL_SURFACE ( 'NONE', #49781, 11.00000000000000000 ) ;
#70425=CARTESIAN_POINT ( 'NONE',  ( 4.220049686691934809, 10.18810118749999916, 91.18750000204836681 ) ) ;
#70426=ADVANCED_FACE ( 'NONE', ( #29179 ), #47255, .T. ) ;
#70436=CARTESIAN_POINT ( 'NONE',  ( -7.204075437095967871, 7.204075437095967871, 72.34375000204836681 ) ) ;
#70456=CARTESIAN_POINT ( 'NONE',  ( 4.556349186104051263, -10.99999999999999822, 76.46874999999998579 ) ) ;
#70483=CARTESIAN_POINT ( 'NONE',  ( 10.18810118749999916, 4.220049686691935698, 116.5000000020483810 ) ) ;
#70495=CARTESIAN_POINT ( 'NONE',  ( 4.220049686691941027, -10.18810118749999738, 115.0000000020483810 ) ) ;
#70519=DIRECTION ( 'NONE',  ( -1.000000000000000000, 0.000000000000000000, 0.000000000000000000 ) ) ;
#70534=CARTESIAN_POINT ( 'NONE',  ( -7.204075437095967871, 7.204075437095967871, 86.96875000204836681 ) ) ;
#70536=CARTESIAN_POINT ( 'NONE',  ( -4.556349186104047710, -10.99999999999999822, 94.28124999999997158 ) ) ;
#70537=CARTESIAN_POINT ( 'NONE',  ( 11.00000000000000000, 1.347111479062088405E-15, 105.2500000000000000 ) ) ;
#70561=CARTESIAN_POINT ( 'NONE',  ( -6.735557395310442023E-16, 11.00000000000000000, 104.3125000040967763 ) ) ;
#70564=CARTESIAN_POINT ( 'NONE',  ( -10.99999999999999822, -4.556349186104052151, 88.28125000409677625 ) ) ;
#70588=CARTESIAN_POINT ( 'NONE',  ( -4.220049686691937474, -10.18810118749999738, 90.81250000204838102 ) ) ;
#70593=CARTESIAN_POINT ( 'NONE',  ( 10.18810118749999916, 4.220049686691935698, 98.50000000204838102 ) ) ;
#70601=CARTESIAN_POINT ( 'NONE',  ( -4.220049686691937474, -10.18810118749999738, 95.31250000204838102 ) ) ;
#70616=CARTESIAN_POINT ( 'NONE',  ( 7.204075437095968759, -7.204075437095966983, 102.7187500020483668 ) ) ;
#70626=VERTEX_POINT ( 'NONE', #60054 ) ;
#70628=PLANE ( 'NONE',  #62649 ) ;
#70635=CARTESIAN_POINT ( 'NONE',  ( 4.556349186104045934, 11.00000000000000000, 116.0312499999999858 ) ) ;
#70646=CARTESIAN_POINT ( 'NONE',  ( -11.00000000000000000, 0.000000000000000000, 104.6875000040967763 ) ) ;
#70661=CARTESIAN_POINT ( 'NONE',  ( -11.00000000000010303, -4.556349186103947346, 67.28125000409676204 ) ) ;
#70665=DIRECTION ( 'NONE',  ( 1.000000000000000000, 2.168404344971008868E-16, 0.000000000000000000 ) ) ;
#70670=CARTESIAN_POINT ( 'NONE',  ( 0.000000000000000000, 0.000000000000000000, 118.0000000000000000 ) ) ;
#70671=CARTESIAN_POINT ( 'NONE',  ( -10.18810118749999916, 4.220049686691934809, 106.9375000020483810 ) ) ;
#70672=ORIENTED_EDGE ( 'NONE', *, *, #9377, .T. ) ;
#70678=CARTESIAN_POINT ( 'NONE',  ( 7.204075437095966983, 7.204075437095967871, 68.96875000204836681 ) ) ;
#70680=ORIENTED_EDGE ( 'NONE', *, *, #48717, .T. ) ;
#70681=CYLINDRICAL_SURFACE ( 'NONE', #60947, 11.00000000000000000 ) ;
#70689=CARTESIAN_POINT ( 'NONE',  ( 1.871523826299183495E-15, -10.18810118749999916, 116.4062500020483810 ) ) ;
#70693=EDGE_CURVE ( 'NONE', #22824, #17226, #47990, .T. ) ;
#70700=LINE ( 'NONE', #42760, #13898 ) ;
#70714=ORIENTED_EDGE ( 'NONE', *, *, #66443, .T. ) ;
#70748=ORIENTED_EDGE ( 'NONE', *, *, #48682, .F. ) ;
#70751=ADVANCED_FACE ( 'NONE', ( #49486 ), #27216, .T. ) ;
#70756=CARTESIAN_POINT ( 'NONE',  ( -10.18810118749999916, 0.000000000000000000, 100.6562500020483810 ) ) ;
#70773=CARTESIAN_POINT ( 'NONE',  ( 7.204075437095966983, 7.204075437095967871, 89.96875000204838102 ) ) ;
#70780=CARTESIAN_POINT ( 'NONE',  ( 1.871523826299183495E-15, -10.18810118749999916, 74.40625000204836681 ) ) ;
#70785=CARTESIAN_POINT ( 'NONE',  ( -10.18810118749999916, 0.000000000000000000, 87.15625000204838102 ) ) ;
#70813=DIRECTION ( 'NONE',  ( -1.000000000000000000, 0.000000000000000000, 0.000000000000000000 ) ) ;
#70819=CARTESIAN_POINT ( 'NONE',  ( -7.778174593052020747, -7.778174593052023411, 79.18750000000000000 ) ) ;
#70829=ADVANCED_FACE ( 'NONE', ( #67597 ), #38925, .T. ) ;
#70846=CARTESIAN_POINT ( 'NONE',  ( -7.204075437095967871, 7.204075437095967871, 85.84375000204836681 ) ) ;
#70847=CARTESIAN_POINT ( 'NONE',  ( -7.778174593052023411, 7.778174593052023411, 67.00000000409676204 ) ) ;
#70860=CARTESIAN_POINT ( 'NONE',  ( -10.18810118749999916, 4.220049686691934809, 114.4375000020483668 ) ) ;
#70888=CARTESIAN_POINT ( 'NONE',  ( -10.99999999999999822, -4.556349186104053040, 98.59375000000000000 ) ) ;
#70893=CARTESIAN_POINT ( 'NONE',  ( 11.00000000000000000, 1.347111479062088405E-15, 82.74999999999998579 ) ) ;
#70897=CARTESIAN_POINT ( 'NONE',  ( 4.220049686691941027, -10.18810118749999738, 87.62500000204836681 ) ) ;
#70899=CARTESIAN_POINT ( 'NONE',  ( 7.778174593052021635, 7.778174593052023411, 94.93750000000000000 ) ) ;
#70900=CARTESIAN_POINT ( 'NONE',  ( 11.00000000000000000, 1.347111479062088405E-15, 118.0000000000000000 ) ) ;
#70905=CARTESIAN_POINT ( 'NONE',  ( -7.778174593052023411, 7.778174593052023411, 78.81249999999998579 ) ) ;
#70919=CARTESIAN_POINT ( 'NONE',  ( -11.00000000000000000, 0.000000000000000000, 118.0000000000000000 ) ) ;
#70926=CARTESIAN_POINT ( 'NONE',  ( -11.00000000000000000, 4.556349186104045934, 70.09375000409676204 ) ) ;
#70928=CARTESIAN_POINT ( 'NONE',  ( -11.00000000000000000, 4.556349186104045934, 86.59375000409677625 ) ) ;
#70944=CARTESIAN_POINT ( 'NONE',  ( 11.00000000000000000, 1.347111479062088405E-15, 91.93750000409677625 ) ) ;
#70949=CARTESIAN_POINT ( 'NONE',  ( 1.871523826299183495E-15, -10.18810118749999916, 93.90625000204836681 ) ) ;
#70954=CARTESIAN_POINT ( 'NONE',  ( 10.18810118749999916, 4.220049686691935698, 100.0000000020483668 ) ) ;
#70964=CARTESIAN_POINT ( 'NONE',  ( -7.204075437095967871, 7.204075437095967871, 99.34375000204836681 ) ) ;
#70967=( BOUNDED_CURVE ( )  B_SPLINE_CURVE ( 2, ( #70982, #8350, #54394, #19297, #1960, #42307, #66436, #48336, #2701 ),
 .UNSPECIFIED., .F., .F. ) 
 B_SPLINE_CURVE_WITH_KNOTS ( ( 3, 2, 2, 2, 3 ),
 ( 0.02941176470588236988, 0.03308823529411766828, 0.03676470588235296322, 0.04044117647058825815, 0.04411764705882355309 ),
 .UNSPECIFIED. ) 
 CURVE ( )  GEOMETRIC_REPRESENTATION_ITEM ( )  RATIONAL_B_SPLINE_CURVE ( ( 0.9999999999999996669, 0.9238795325112870716, 1.000000000000000000, 0.9238795325112867385, 1.000000000000000000, 0.9238795325112867385, 1.000000000000000000, 0.9238795325112862944, 1.000000000000000444 ) ) 
 REPRESENTATION_ITEM ( '' )  );
#70970=ORIENTED_EDGE ( 'NONE', *, *, #68045, .F. ) ;
#70974=CARTESIAN_POINT ( 'NONE',  ( 11.00000000000000000, 1.347111479062088405E-15, 90.43750000409676204 ) ) ;
#70981=CARTESIAN_POINT ( 'NONE',  ( -7.204075437095967871, 7.204075437095967871, 101.9687500020483668 ) ) ;
#70982=CARTESIAN_POINT ( 'NONE',  ( -11.00000000000000000, 0.000000000000000000, 115.1875000040967763 ) ) ;
#70996=DIRECTION ( 'NONE',  ( -0.000000000000000000, -0.000000000000000000, -1.000000000000000000 ) ) ;
#70997=CARTESIAN_POINT ( 'NONE',  ( -10.99999999999999822, -4.556349186104052151, 112.0937499999999858 ) ) ;
#71006=VERTEX_POINT ( 'NONE', #51348 ) ;
#71010=CARTESIAN_POINT ( 'NONE',  ( -7.778174593052020747, -7.778174593052023411, 104.8750000040967763 ) ) ;
#71013=CARTESIAN_POINT ( 'NONE',  ( 4.556349186104045934, 11.00000000000000000, 95.21875000409677625 ) ) ;
#71016=LINE ( 'NONE', #42714, #44782 ) ;
#71030=CARTESIAN_POINT ( 'NONE',  ( 4.220049686691941027, -10.18810118749999738, 112.0000000020483668 ) ) ;
#71032=DIRECTION ( 'NONE',  ( -0.000000000000000000, -0.000000000000000000, -1.000000000000000000 ) ) ;
#71037=CARTESIAN_POINT ( 'NONE',  ( 4.220049686691941027, -10.18810118749999738, 68.50000000204838102 ) ) ;
#71048=CARTESIAN_POINT ( 'NONE',  ( 7.204075437095968759, -7.204075437095966983, 115.0937500020483810 ) ) ;
#71114=CARTESIAN_POINT ( 'NONE',  ( -10.18810118749999916, 4.220049686691934809, 93.06250000204839523 ) ) ;
#71115=CARTESIAN_POINT ( 'NONE',  ( -11.00000000000000000, 0.000000000000000000, 86.68750000409677625 ) ) ;
#71124=CARTESIAN_POINT ( 'NONE',  ( 4.556349186104045934, 11.00000000000000000, 83.21875000409680467 ) ) ;
#71128=CARTESIAN_POINT ( 'NONE',  ( 4.220049686691934809, 10.18810118749999916, 90.06250000204838102 ) ) ;
#71134=CARTESIAN_POINT ( 'NONE',  ( 7.204075437095968759, -7.204075437095966983, 76.09375000204838102 ) ) ;
#71143=CARTESIAN_POINT ( 'NONE',  ( -10.18810118749999916, 0.000000000000000000, 85.65625000204838102 ) ) ;
#71155=CARTESIAN_POINT ( 'NONE',  ( -10.18810118749999738, -4.220049686691941915, 71.12500000204836681 ) ) ;
#71170=( BOUNDED_CURVE ( )  B_SPLINE_CURVE ( 2, ( #27144, #44137, #10919, #33954, #67148, #16554, #15442, #10546, #44880 ),
 .UNSPECIFIED., .F., .F. ) 
 B_SPLINE_CURVE_WITH_KNOTS ( ( 3, 2, 2, 2, 3 ),
 ( 0.3529411764705882026, 0.3566176470588234837, 0.3602941176470587648, 0.3639705882352940458, 0.3676470588235293824 ),
 .UNSPECIFIED. ) 
 CURVE ( )  GEOMETRIC_REPRESENTATION_ITEM ( )  RATIONAL_B_SPLINE_CURVE ( ( 1.000000000000001110, 0.9238795325112856283, 1.000000000000000000, 0.9238795325112867385, 1.000000000000000000, 0.9238795325112867385, 1.000000000000000000, 0.9238795325112878487, 0.9999999999999988898 ) ) 
 REPRESENTATION_ITEM ( '' )  );
#71177=CARTESIAN_POINT ( 'NONE',  ( 11.00000000000000000, 4.556349186104045934, 75.34375000000000000 ) ) ;
#71187=CARTESIAN_POINT ( 'NONE',  ( -7.778174593052023411, 7.778174593052023411, 115.0000000040967905 ) ) ;
#71203=CARTESIAN_POINT ( 'NONE',  ( 4.220049686691934809, 10.18810118749999916, 88.56250000204836681 ) ) ;
#71204=CARTESIAN_POINT ( 'NONE',  ( -10.18810118749999738, -4.220049686691941915, 112.7500000020483810 ) ) ;
#71215=CARTESIAN_POINT ( 'NONE',  ( -7.204075437095967871, 7.204075437095967871, 105.3437500020483810 ) ) ;
#71219=DIRECTION ( 'NONE',  ( -0.000000000000000000, -0.000000000000000000, -1.000000000000000000 ) ) ;
#71226=STYLED_ITEM('',(#74706),#17043);
#71244=CARTESIAN_POINT ( 'NONE',  ( 4.556349186104045934, 11.00000000000000000, 72.53124999999998579 ) ) ;
#71255=CARTESIAN_POINT ( 'NONE',  ( -10.18810118749999916, 4.220049686691934809, 78.06250000204836681 ) ) ;
#71257=CARTESIAN_POINT ( 'NONE',  ( 7.778174593052023411, -7.778174593052021635, 97.56250000000000000 ) ) ;
#71264=DIRECTION ( 'NONE',  ( -0.8660266317069091890, 0.4999978731656731235, 2.046673486196596759E-06 ) ) ;
#71268=CIRCLE ( 'NONE', #64093, 10.49999999999998224 ) ;
#71272=LINE ( 'NONE', #66745, #2212 ) ;
#71285=CARTESIAN_POINT ( 'NONE',  ( 11.00000000000000000, 1.347111479062088405E-15, 103.9375000040967763 ) ) ;
#71288=CARTESIAN_POINT ( 'NONE',  ( 11.00000000000000000, 4.556349186104045934, 80.03125000409677625 ) ) ;
#71303=ADVANCED_FACE ( 'NONE', ( #52843 ), #53950, .T. ) ;
#71314=CARTESIAN_POINT ( 'NONE',  ( -6.238412754330611322E-16, 10.18810118749999916, 90.15625000204838102 ) ) ;
#71319=CARTESIAN_POINT ( 'NONE',  ( -10.18810118749999916, 4.220049686691934809, 103.5625000020483668 ) ) ;
#71327=CARTESIAN_POINT ( 'NONE',  ( -4.220049686691937474, -10.18810118749999738, 99.81250000204838102 ) ) ;
#71329=AXIS2_PLACEMENT_3D ( 'NONE', #11648, #69737, #12020 ) ;
#71339=CARTESIAN_POINT ( 'NONE',  ( 10.99999999999989342, 4.556349186104152515, 84.34375000000001421 ) ) ;
#71341=EDGE_LOOP ( 'NONE', ( #63817, #19253, #66061, #27922 ) ) ;
#71343=CARTESIAN_POINT ( 'NONE',  ( -7.204075437095967871, 7.204075437095967871, 97.46875000204838102 ) ) ;
#71353=CARTESIAN_POINT ( 'NONE',  ( -4.556349186104045934, 11.00000000000000000, 74.21875000000000000 ) ) ;
#71359=CARTESIAN_POINT ( 'NONE',  ( 7.778174593052023411, -7.778174593052021635, 115.5625000000000000 ) ) ;
#71371=CARTESIAN_POINT ( 'NONE',  ( 11.00000000000000355, -4.556349186104045046, 106.8437500040967763 ) ) ;
#71372=DIRECTION ( 'NONE',  ( 0.7071067811865401342, -0.000000000000000000, 0.7071067811865549002 ) ) ;
#71375=CARTESIAN_POINT ( 'NONE',  ( 2.020667218593132706E-15, -11.00000000000000000, 107.8750000000000000 ) ) ;
#71377=CARTESIAN_POINT ( 'NONE',  ( 4.556349186104045934, 11.00000000000000000, 87.53125000000000000 ) ) ;
#71395=CARTESIAN_POINT ( 'NONE',  ( 4.220049686691941027, -10.18810118749999738, 110.5000000020483810 ) ) ;
#71399=DIRECTION ( 'NONE',  ( -1.000000000000000000, 0.000000000000000000, 0.000000000000000000 ) ) ;
#71402=FACE_OUTER_BOUND ( 'NONE', #4834, .T. ) ;
#71403=CARTESIAN_POINT ( 'NONE',  ( -10.18810118749999738, -4.220049686691941915, 74.12500000204836681 ) ) ;
#71405=( BOUNDED_CURVE ( )  B_SPLINE_CURVE ( 2, ( #10727, #29203, #10361, #182, #4706, #33385, #62767, #28819, #33760 ),
 .UNSPECIFIED., .F., .F. ) 
 B_SPLINE_CURVE_WITH_KNOTS ( ( 3, 2, 2, 2, 3 ),
 ( 0.2647058823529410687, 0.2683823529411763498, 0.2720588235294116863, 0.2757352941176470229, 0.2794117647058823040 ),
 .UNSPECIFIED. ) 
 CURVE ( )  GEOMETRIC_REPRESENTATION_ITEM ( )  RATIONAL_B_SPLINE_CURVE ( ( 1.000000000000002220, 0.9238795325112844070, 1.000000000000000000, 0.9238795325112867385, 1.000000000000000000, 0.9238795325112867385, 1.000000000000000000, 0.9238795325112878487, 0.9999999999999988898 ) ) 
 REPRESENTATION_ITEM ( '' )  );
#71417=CARTESIAN_POINT ( 'NONE',  ( 4.220049686691941027, -10.18810118749999738, 68.12500000204838102 ) ) ;
#71454=CARTESIAN_POINT ( 'NONE',  ( -11.00000000000000000, 0.000000000000000000, 112.1875000040967763 ) ) ;
#71465=DIRECTION ( 'NONE',  ( 1.000000000000000000, 3.154042683594195121E-16, 0.000000000000000000 ) ) ;
#71469=DIRECTION ( 'NONE',  ( -0.000000000000000000, -0.000000000000000000, -1.000000000000000000 ) ) ;
#71472=CARTESIAN_POINT ( 'NONE',  ( -7.778174593052020747, -7.778174593052023411, 104.8750000040967763 ) ) ;
#71475=CARTESIAN_POINT ( 'NONE',  ( -4.556349186104045934, 11.00000000000000000, 81.90625000409676204 ) ) ;
#71480=CARTESIAN_POINT ( 'NONE',  ( -10.18810118749999738, -4.220049686691941915, 93.25000000204838102 ) ) ;
#71491=VECTOR ( 'NONE', #49417, 1000.000000000000000 ) ;
#71496=CARTESIAN_POINT ( 'NONE',  ( -10.18810118749999916, 4.220049686691934809, 87.43750000204838102 ) ) ;
#71502=CARTESIAN_POINT ( 'NONE',  ( -10.18810118749999738, -4.220049686691941915, 74.12500000204836681 ) ) ;
#71507=DIRECTION ( 'NONE',  ( -0.000000000000000000, -0.000000000000000000, -1.000000000000000000 ) ) ;
#71511=CARTESIAN_POINT ( 'NONE',  ( 7.204075437095968759, -7.204075437095966983, 86.21875000204836681 ) ) ;
#71521=CARTESIAN_POINT ( 'NONE',  ( -4.220049686691937474, -10.18810118749999738, 69.81250000204835260 ) ) ;
#71544=CARTESIAN_POINT ( 'NONE',  ( -7.778174593052020747, -7.778174593052023411, 77.68749999999998579 ) ) ;
#71572=CARTESIAN_POINT ( 'NONE',  ( -6.238412754330611322E-16, 10.18810118749999916, 88.65625000204838102 ) ) ;
#71573=CARTESIAN_POINT ( 'NONE',  ( 4.220049686691934809, 10.18810118749999916, 110.6875000020483952 ) ) ;
#71576=CARTESIAN_POINT ( 'NONE',  ( 11.00000000000000000, 1.347111479062088405E-15, 106.7500000000000000 ) ) ;
#71586=CARTESIAN_POINT ( 'NONE',  ( -10.18810118749999916, 0.000000000000000000, 105.5312500020483810 ) ) ;
#71609=AXIS2_PLACEMENT_3D ( 'NONE', #3183, #30734, #54502 ) ;
#71619=CARTESIAN_POINT ( 'NONE',  ( -6.735557395310442023E-16, 11.00000000000000000, 83.12499999999998579 ) ) ;
#71624=CARTESIAN_POINT ( 'NONE',  ( -10.18810118749999738, -4.220049686691941915, 79.75000000204838102 ) ) ;
#71627=CARTESIAN_POINT ( 'NONE',  ( -7.778174593052023411, 7.778174593052023411, 95.31250000000000000 ) ) ;
#71628=CARTESIAN_POINT ( 'NONE',  ( 7.778174593052023411, -7.778174593052021635, 105.0624999999999858 ) ) ;
#71657=CARTESIAN_POINT ( 'NONE',  ( 4.556349186104051263, -10.99999999999999822, 81.15625000409676204 ) ) ;
#71674=CARTESIAN_POINT ( 'NONE',  ( -10.18810118749999916, 0.000000000000000000, 79.65625000204836681 ) ) ;
#71682=CARTESIAN_POINT ( 'NONE',  ( -7.204075437095967871, 7.204075437095967871, 85.84375000204836681 ) ) ;
#71683=ORIENTED_EDGE ( 'NONE', *, *, #16197, .T. ) ;
#71688=CARTESIAN_POINT ( 'NONE',  ( -10.18810118749999916, 4.220049686691934809, 99.06250000204836681 ) ) ;
#71691=ORIENTED_EDGE ( 'NONE', *, *, #50371, .F. ) ;
#71694=VECTOR ( 'NONE', #20746, 1000.000000000000000 ) ;
#71696=CARTESIAN_POINT ( 'NONE',  ( -6.238412754330611322E-16, 10.18810118749999916, 96.15625000204838102 ) ) ;
#71698=CARTESIAN_POINT ( 'NONE',  ( 0.000000000000000000, 0.000000000000000000, 118.0000000000000000 ) ) ;
#71704=DIRECTION ( 'NONE',  ( 1.000000000000000000, 1.224646799147353207E-16, -0.000000000000000000 ) ) ;
#71715=CARTESIAN_POINT ( 'NONE',  ( 7.204075437095966983, 7.204075437095967871, 97.09375000204836681 ) ) ;
#71725=CARTESIAN_POINT ( 'NONE',  ( 11.00000000000010658, 4.556349186103942017, 73.84374999999997158 ) ) ;
#71730=CARTESIAN_POINT ( 'NONE',  ( 11.00000000000000000, 1.347111479062088405E-15, 85.75000000000000000 ) ) ;
#71732=CARTESIAN_POINT ( 'NONE',  ( -11.00000000000000000, 0.000000000000000000, 91.18750000409677625 ) ) ;
#71733=CARTESIAN_POINT ( 'NONE',  ( -7.778174593052020747, -7.778174593052023411, 113.6875000000000000 ) ) ;
#71740=DIRECTION ( 'NONE',  ( 0.000000000000000000, 0.000000000000000000, -1.000000000000000000 ) ) ;
#71745=CARTESIAN_POINT ( 'NONE',  ( -11.00000000000000000, 4.556349186104045934, 98.59375000409677625 ) ) ;
#71747=CARTESIAN_POINT ( 'NONE',  ( 4.556349186104052151, -10.99999999999999822, 106.6562500040967905 ) ) ;
#71752=CARTESIAN_POINT ( 'NONE',  ( 7.778174593052021635, 7.778174593052023411, 87.43749999999998579 ) ) ;
#71771=CARTESIAN_POINT ( 'NONE',  ( 7.204075437095966983, 7.204075437095967871, 103.4687500020483668 ) ) ;
#71778=CARTESIAN_POINT ( 'NONE',  ( -6.238412754330611322E-16, 10.18810118749999916, 73.65625000204836681 ) ) ;
#71781=CARTESIAN_POINT ( 'NONE',  ( -10.18810118749999916, 0.000000000000000000, 117.1562500020483810 ) ) ;
#71790=CARTESIAN_POINT ( 'NONE',  ( 10.18810118750000093, -4.220049686691933921, 68.31250000204838102 ) ) ;
#71807=CARTESIAN_POINT ( 'NONE',  ( 1.871523826299183495E-15, -10.18810118749999916, 116.0312500020483810 ) ) ;
#71854=ORIENTED_EDGE ( 'NONE', *, *, #10436, .F. ) ;
#71856=CARTESIAN_POINT ( 'NONE',  ( 1.871523826299183495E-15, -10.18810118749999916, 98.03125000204838102 ) ) ;
#71866=CARTESIAN_POINT ( 'NONE',  ( 11.00000000000000000, 1.347111479062088405E-15, 76.74999999999998579 ) ) ;
#71867=CARTESIAN_POINT ( 'NONE',  ( -11.00000000000000000, 0.000000000000000000, 83.68750000409677625 ) ) ;
#71871=CARTESIAN_POINT ( 'NONE',  ( 10.18810118749999916, 4.220049686691935698, 88.37500000204838102 ) ) ;
#71886=CARTESIAN_POINT ( 'NONE',  ( -7.204075437095965206, -7.204075437095968759, 84.34375000204836681 ) ) ;
#71921=CARTESIAN_POINT ( 'NONE',  ( -11.00000000000000000, 4.556349186104045934, 78.90624999999998579 ) ) ;
#71931=CARTESIAN_POINT ( 'NONE',  ( -7.778174593052020747, -7.778174593052023411, 113.8750000040967763 ) ) ;
#71946=ORIENTED_EDGE ( 'NONE', *, *, #12875, .F. ) ;
#71947=CARTESIAN_POINT ( 'NONE',  ( 10.18810118749999916, 1.247682550866122264E-15, 85.28125000204836681 ) ) ;
#71948=CARTESIAN_POINT ( 'NONE',  ( -10.18810118749999916, 4.220049686691934809, 111.0625000020483810 ) ) ;
#71960=CARTESIAN_POINT ( 'NONE',  ( 7.204075437095968759, -7.204075437095966983, 109.0937500020483810 ) ) ;
#71989=CARTESIAN_POINT ( 'NONE',  ( 11.00000000000000000, 1.347111479062088405E-15, 118.0000000000000000 ) ) ;
#71991=EDGE_CURVE ( 'NONE', #2612, #49272, #21221, .T. ) ;
#71995=CARTESIAN_POINT ( 'NONE',  ( 7.778174593052021635, 7.778174593052023411, 82.93750000000000000 ) ) ;
#71999=CARTESIAN_POINT ( 'NONE',  ( 1.871523826299183495E-15, -10.18810118749999916, 81.53125000204838102 ) ) ;
#72002=CARTESIAN_POINT ( 'NONE',  ( 2.020667218593132706E-15, -11.00000000000000000, 92.87499999999998579 ) ) ;
#72009=VECTOR ( 'NONE', #52852, 1000.000000000000000 ) ;
#72030=CARTESIAN_POINT ( 'NONE',  ( -10.99999999999999822, -4.556349186104052151, 82.28125000409677625 ) ) ;
#72046=LINE ( 'NONE', #20363, #71694 ) ;
#72047=CARTESIAN_POINT ( 'NONE',  ( 7.204075437095966983, 7.204075437095967871, 77.59375000204838102 ) ) ;
#72056=CARTESIAN_POINT ( 'NONE',  ( -10.18810118749999916, 0.000000000000000000, 87.53125000204836681 ) ) ;
#72058=CARTESIAN_POINT ( 'NONE',  ( -10.99999999999968203, -4.556349186104368343, 89.78125000409681888 ) ) ;
#72062=CARTESIAN_POINT ( 'NONE',  ( -10.18810118749999916, 0.000000000000000000, 93.15625000204836681 ) ) ;
#72070=CARTESIAN_POINT ( 'NONE',  ( -10.18810118749999916, 0.000000000000000000, 96.53125000204838102 ) ) ;
#72071=ADVANCED_FACE ( 'NONE', ( #26202 ), #42075, .T. ) ;
#72073=AXIS2_PLACEMENT_3D ( 'NONE', #8279, #31289, #30918 ) ;
#72092=CARTESIAN_POINT ( 'NONE',  ( 10.18810118750000093, -4.220049686691933033, 99.81250000204838102 ) ) ;
#72103=ORIENTED_EDGE ( 'NONE', *, *, #1411, .F. ) ;
#72105=ADVANCED_FACE ( 'NONE', ( #30764 ), #8125, .T. ) ;
#72112=CARTESIAN_POINT ( 'NONE',  ( 4.556349186104045934, 11.00000000000000000, 113.0312499999999858 ) ) ;
#72116=CARTESIAN_POINT ( 'NONE',  ( 2.020667218593132706E-15, -11.00000000000000000, 101.8750000000000000 ) ) ;
#72124=CARTESIAN_POINT ( 'NONE',  ( -6.735557395310442023E-16, 11.00000000000000000, 99.81250000409677625 ) ) ;
#72125=LINE ( 'NONE', #38569, #61231 ) ;
#72127=CARTESIAN_POINT ( 'NONE',  ( 5.471491410962281421, 9.542682104092435225, 117.5000000000000711 ) ) ;
#72146=CARTESIAN_POINT ( 'NONE',  ( 11.00000000000010658, 4.556349186103942017, 69.34374999999998579 ) ) ;
#72147=CARTESIAN_POINT ( 'NONE',  ( 10.18810118749999916, 4.220049686691935698, 106.3750000020483668 ) ) ;
#72153=CARTESIAN_POINT ( 'NONE',  ( 10.18810118749999916, 1.247682550866122264E-15, 71.78125000204838102 ) ) ;
#72165=CARTESIAN_POINT ( 'NONE',  ( 1.871523826299183495E-15, -10.18810118749999916, 113.4062500020483810 ) ) ;
#72191=CARTESIAN_POINT ( 'NONE',  ( -11.00000000000000000, 0.000000000000000000, 113.6875000040967763 ) ) ;
#72221=LINE ( 'NONE', #15996, #4802 ) ;
#72223=LINE ( 'NONE', #20538, #5835 ) ;
#72225=VERTEX_POINT ( 'NONE', #9996 ) ;
#72230=CARTESIAN_POINT ( 'NONE',  ( 11.00000000000000000, 1.347111479062088405E-15, 94.74999999999998579 ) ) ;
#72234=CARTESIAN_POINT ( 'NONE',  ( 7.204075437095968759, -7.204075437095966983, 95.21875000204838102 ) ) ;
#72235=DIRECTION ( 'NONE',  ( -0.000000000000000000, -0.000000000000000000, -1.000000000000000000 ) ) ;
#72250=CARTESIAN_POINT ( 'NONE',  ( 1.871523826299183495E-15, -10.18810118749999916, 87.90625000204838102 ) ) ;
#72258=CARTESIAN_POINT ( 'NONE',  ( -11.00000000000000000, 0.000000000000000000, 85.18750000409677625 ) ) ;
#72265=CARTESIAN_POINT ( 'NONE',  ( 10.18810118749999916, 1.247682550866122264E-15, 81.90625000204838102 ) ) ;
#72296=LINE ( 'NONE', #3273, #20156 ) ;
#72301=CARTESIAN_POINT ( 'NONE',  ( 7.778174593052021635, 7.778174593052023411, 69.43749999999998579 ) ) ;
#72312=CARTESIAN_POINT ( 'NONE',  ( -11.00000000000000000, 0.000000000000000000, 113.6875000040967763 ) ) ;
#72328=CARTESIAN_POINT ( 'NONE',  ( -7.204075437095965206, -7.204075437095968759, 89.21875000204838102 ) ) ;
#72329=CARTESIAN_POINT ( 'NONE',  ( -4.220049686691935698, 10.18810118749999916, 110.8750000020483810 ) ) ;
#72338=CIRCLE ( 'NONE', #39803, 34.85072926314708752 ) ;
#72340=CARTESIAN_POINT ( 'NONE',  ( 4.556349186104045934, 11.00000000000000000, 113.0312500000000000 ) ) ;
#72344=CARTESIAN_POINT ( 'NONE',  ( 7.204075437095966983, 7.204075437095967871, 109.4687500020483810 ) ) ;
#72360=LINE ( 'NONE', #38416, #35820 ) ;
#72379=ORIENTED_EDGE ( 'NONE', *, *, #53175, .T. ) ;
#72382=EDGE_LOOP ( 'NONE', ( #62169, #52759, #51798, #160, #12490 ) ) ;
#72384=CARTESIAN_POINT ( 'NONE',  ( 1.871523826299183495E-15, -10.18810118749999916, 80.03125000204836681 ) ) ;
#72387=CARTESIAN_POINT ( 'NONE',  ( -10.99999999999999822, -4.556349186104052151, 91.09375000000001421 ) ) ;
#72418=CARTESIAN_POINT ( 'NONE',  ( 7.778174593052023411, -7.778174593052021635, 79.75000000409676204 ) ) ;
#72438=CARTESIAN_POINT ( 'NONE',  ( 4.220049686691934809, 10.18810118749999916, 77.68750000204838102 ) ) ;
#72448=CARTESIAN_POINT ( 'NONE',  ( 10.18810118750000093, -4.220049686691933921, 86.68750000204836681 ) ) ;
#72453=CARTESIAN_POINT ( 'NONE',  ( 10.18810118749999916, 1.247682550866122264E-15, 98.40625000204838102 ) ) ;
#72461=CARTESIAN_POINT ( 'NONE',  ( 7.204075437095968759, -7.204075437095966983, 94.09375000204838102 ) ) ;
#72479=CARTESIAN_POINT ( 'NONE',  ( -4.220049686691935698, 10.18810118749999916, 97.37500000204839523 ) ) ;
#72495=CARTESIAN_POINT ( 'NONE',  ( -7.778174593052023411, 7.778174593052023411, 111.8125000000000000 ) ) ;
#72512=CARTESIAN_POINT ( 'NONE',  ( 7.778174593052021635, 7.778174593052023411, 96.62500000409676204 ) ) ;
#72520=EDGE_CURVE ( 'NONE', #30135, #56146, #72046, .T. ) ;
#72536=CARTESIAN_POINT ( 'NONE',  ( -10.18810118749999916, 0.000000000000000000, 102.5312500020483810 ) ) ;
#72546=VERTEX_POINT ( 'NONE', #26782 ) ;
#72547=CARTESIAN_POINT ( 'NONE',  ( -7.204075437095967871, 7.204075437095967871, 110.9687500020483810 ) ) ;
#72555=CARTESIAN_POINT ( 'NONE',  ( 1.871523826299183495E-15, -10.18810118749999916, 107.4062500020483668 ) ) ;
#72557=B_SPLINE_CURVE_WITH_KNOTS ( 'NONE', 1,
 ( #41674, #30351 ),
 .UNSPECIFIED., .F., .F.,
 ( 2, 2 ),
 ( 0.000000000000000000, 1.000000000000000000 ),
 .UNSPECIFIED. ) ;
#72567=CARTESIAN_POINT ( 'NONE',  ( 11.00000000000000000, 1.347111479062088405E-15, 114.2499999999999858 ) ) ;
#72570=CARTESIAN_POINT ( 'NONE',  ( 11.00000000000000000, 1.347111479062088405E-15, 90.25000000000000000 ) ) ;
#72571=VERTEX_POINT ( 'NONE', #38488 ) ;
#72581=ORIENTED_EDGE ( 'NONE', *, *, #46321, .F. ) ;
#72593=LINE ( 'NONE', #67309, #13210 ) ;
#72616=CARTESIAN_POINT ( 'NONE',  ( 2.020667218593132706E-15, -11.00000000000000000, 82.37499999999998579 ) ) ;
#72622=CARTESIAN_POINT ( 'NONE',  ( -7.204075437095967871, 7.204075437095967871, 91.46875000204838102 ) ) ;
#72636=CARTESIAN_POINT ( 'NONE',  ( 1.871523826299183495E-15, -10.18810118749999916, 81.90625000204838102 ) ) ;
#72643=FACE_OUTER_BOUND ( 'NONE', #18339, .T. ) ;
#72648=VERTEX_POINT ( 'NONE', #3406 ) ;
#72651=CARTESIAN_POINT ( 'NONE',  ( -10.18810118749999738, -4.220049686691941915, 84.25000000204838102 ) ) ;
#72652=ADVANCED_FACE ( 'NONE', ( #60362 ), #38115, .T. ) ;
#72677=CARTESIAN_POINT ( 'NONE',  ( 10.99999999999989697, -4.556349186104149851, 93.15625000000001421 ) ) ;
#72686=CARTESIAN_POINT ( 'NONE',  ( -11.00000000000000000, 4.556349186104045934, 72.90624999999997158 ) ) ;
#72690=VERTEX_POINT ( 'NONE', #39229 ) ;
#72695=CARTESIAN_POINT ( 'NONE',  ( 11.00000000000000355, -4.556349186104045046, 109.8437500040967763 ) ) ;
#72713=CARTESIAN_POINT ( 'NONE',  ( 10.18810118750000093, -4.220049686691933921, 114.8125000020483668 ) ) ;
#72716=LINE ( 'NONE', #67428, #61259 ) ;
#72717=CARTESIAN_POINT ( 'NONE',  ( -4.556349186104048599, -10.99999999999999822, 106.2812500000000000 ) ) ;
#72727=CARTESIAN_POINT ( 'NONE',  ( 10.18810118750000093, -4.220049686691933033, 101.6875000020483810 ) ) ;
#72729=VERTEX_POINT ( 'NONE', #67526 ) ;
#72745=ORIENTED_EDGE ( 'NONE', *, *, #14446, .F. ) ;
#72751=( BOUNDED_CURVE ( )  B_SPLINE_CURVE ( 2, ( #55622, #44663, #20893, #67676, #39005, #33733, #61643, #4678, #43915 ),
 .UNSPECIFIED., .F., .F. ) 
 B_SPLINE_CURVE_WITH_KNOTS ( ( 3, 2, 2, 2, 3 ),
 ( 0.1764705882352942123, 0.1801470588235294934, 0.1838235294117648300, 0.1875000000000001110, 0.1911764705882353921 ),
 .UNSPECIFIED. ) 
 CURVE ( )  GEOMETRIC_REPRESENTATION_ITEM ( )  RATIONAL_B_SPLINE_CURVE ( ( 0.9999999999999982236, 0.9238795325112885148, 1.000000000000000000, 0.9238795325112867385, 1.000000000000000000, 0.9238795325112867385, 1.000000000000000000, 0.9238795325112844070, 1.000000000000002220 ) ) 
 REPRESENTATION_ITEM ( '' )  );
#72768=CARTESIAN_POINT ( 'NONE',  ( 10.18810118749999916, 4.220049686691935698, 82.00000000204838102 ) ) ;
#72770=FACE_OUTER_BOUND ( 'NONE', #30903, .T. ) ;
#72771=CARTESIAN_POINT ( 'NONE',  ( -7.778174593052020747, -7.778174593052023411, 86.68749999999998579 ) ) ;
#72784=CARTESIAN_POINT ( 'NONE',  ( 11.00000000000000000, 1.347111479062088405E-15, 99.43750000409677625 ) ) ;
#72794=CARTESIAN_POINT ( 'NONE',  ( 4.556349186104045934, 11.00000000000000000, 111.7187500040967905 ) ) ;
#72798=CARTESIAN_POINT ( 'NONE',  ( 2.020667218593132706E-15, -11.00000000000000000, 79.56250000409677625 ) ) ;
#72816=CARTESIAN_POINT ( 'NONE',  ( 1.871523826299183495E-15, -10.18810118749999916, 75.53125000204836681 ) ) ;
#72823=CARTESIAN_POINT ( 'NONE',  ( -10.18810118749999738, -4.220049686691941915, 87.62500000204836681 ) ) ;
#72825=CARTESIAN_POINT ( 'NONE',  ( -4.556349186104048599, -10.99999999999999822, 89.96875000409677625 ) ) ;
#72828=CARTESIAN_POINT ( 'NONE',  ( -6.238412754330611322E-16, 10.18810118749999916, 94.28125000204836681 ) ) ;
#72836=CARTESIAN_POINT ( 'NONE',  ( 4.220049686691934809, 10.18810118749999916, 91.56250000204836681 ) ) ;
#72855=CARTESIAN_POINT ( 'NONE',  ( -10.18810118749999738, -4.220049686691941915, 99.25000000204838102 ) ) ;
#72858=CARTESIAN_POINT ( 'NONE',  ( -10.99999999999999822, -4.556349186104052151, 109.0937500000000000 ) ) ;
#72866=CARTESIAN_POINT ( 'NONE',  ( 0.000000000000000000, 0.000000000000000000, 118.0000000000000000 ) ) ;
#72883=VERTEX_POINT ( 'NONE', #16948 ) ;
#72886=CARTESIAN_POINT ( 'NONE',  ( -4.556349186104047710, -10.99999999999999822, 98.96875000409676204 ) ) ;
#72889=CARTESIAN_POINT ( 'NONE',  ( -11.00000000000000533, 11.00000000000000000, 20.00000000000000000 ) ) ;
#72907=CARTESIAN_POINT ( 'NONE',  ( -4.220049686691937474, -10.18810118749999738, 101.3125000020483810 ) ) ;
#72911=CARTESIAN_POINT ( 'NONE',  ( -11.00000000000000000, 0.000000000000000000, 78.99999999999998579 ) ) ;
#72914=CARTESIAN_POINT ( 'NONE',  ( -10.68301270189220098, 0.000000000000000000, 117.8169872981077617 ) ) ;
#72917=CARTESIAN_POINT ( 'NONE',  ( -10.18810118749999916, 4.220049686691934809, 114.0625000020483668 ) ) ;
#72925=CARTESIAN_POINT ( 'NONE',  ( 7.204075437095966983, 7.204075437095967871, 112.4687500020483810 ) ) ;
#72934=CARTESIAN_POINT ( 'NONE',  ( 7.204075437095966983, 7.204075437095967871, 68.96875000204836681 ) ) ;
#72955=CARTESIAN_POINT ( 'NONE',  ( 7.778174593052021635, 7.778174593052023411, 87.62500000409677625 ) ) ;
#72957=CARTESIAN_POINT ( 'NONE',  ( -7.778174593052020747, -7.778174593052023411, 77.68749999999998579 ) ) ;
#72963=CARTESIAN_POINT ( 'NONE',  ( 4.556349186104052151, -10.99999999999999822, 110.9687500000000000 ) ) ;
#72973=CARTESIAN_POINT ( 'NONE',  ( 11.00000000000000000, 1.347111479062088405E-15, 82.74999999999998579 ) ) ;
#72994=CARTESIAN_POINT ( 'NONE',  ( 10.18810118749999916, 1.247682550866122264E-15, 86.40625000204838102 ) ) ;
#72995=CARTESIAN_POINT ( 'NONE',  ( -10.99999999999989342, 4.556349186104152515, 93.90625000000000000 ) ) ;
#73006=CARTESIAN_POINT ( 'NONE',  ( 10.18810118749999916, 4.220049686691935698, 80.87500000204836681 ) ) ;
#73020=CARTESIAN_POINT ( 'NONE',  ( 7.204075437095968759, -7.204075437095966983, 80.21875000204836681 ) ) ;
#73030=EDGE_LOOP ( 'NONE', ( #61804, #20695, #41659, #19711, #38859 ) ) ;
#73033=CARTESIAN_POINT ( 'NONE',  ( 7.778174593052023411, -7.778174593052021635, 73.75000000409676204 ) ) ;
#73045=CARTESIAN_POINT ( 'NONE',  ( 11.00000000000000000, 1.347111479062088405E-15, 93.24999999999998579 ) ) ;
#73053=CARTESIAN_POINT ( 'NONE',  ( 4.556349186104051263, -10.99999999999999822, 71.96874999999997158 ) ) ;
#73074=CARTESIAN_POINT ( 'NONE',  ( 7.778174593052021635, 7.778174593052023411, 81.43750000000000000 ) ) ;
#73081=CARTESIAN_POINT ( 'NONE',  ( -10.18810118749999916, 4.220049686691934809, 109.5625000020483810 ) ) ;
#73096=CARTESIAN_POINT ( 'NONE',  ( -4.220049686691937474, -10.18810118749999738, 102.8125000020483952 ) ) ;
#73118=CARTESIAN_POINT ( 'NONE',  ( 7.204075437095968759, -7.204075437095966983, 80.59375000204838102 ) ) ;
#73125=EDGE_LOOP ( 'NONE', ( #65647, #50555, #45338, #53106, #49763 ) ) ;
#73138=CARTESIAN_POINT ( 'NONE',  ( -10.18810118749999916, 0.000000000000000000, 75.15625000204836681 ) ) ;
#73141=CARTESIAN_POINT ( 'NONE',  ( 11.00000000000000000, 1.347111479062088405E-15, 88.75000000000000000 ) ) ;
#73145=CARTESIAN_POINT ( 'NONE',  ( 2.020667218593132706E-15, -11.00000000000000000, 83.87499999999998579 ) ) ;
#73146=DIRECTION ( 'NONE',  ( 0.000000000000000000, 0.000000000000000000, 1.000000000000000000 ) ) ;
#73168=CARTESIAN_POINT ( 'NONE',  ( 11.00000000000000000, 1.347111479062088405E-15, 81.43750000409677625 ) ) ;
#73170=CARTESIAN_POINT ( 'NONE',  ( -11.00000000000000000, 0.000000000000000000, 74.68750000409676204 ) ) ;
#73188=CARTESIAN_POINT ( 'NONE',  ( 4.220049686691934809, 10.18810118749999916, 74.68750000204836681 ) ) ;
#73196=CARTESIAN_POINT ( 'NONE',  ( -10.18810118749999916, 0.000000000000000000, 81.53125000204838102 ) ) ;
#73200=CARTESIAN_POINT ( 'NONE',  ( 0.000000000000000000, 0.000000000000000000, 118.0000000000000000 ) ) ;
#73201=CARTESIAN_POINT ( 'NONE',  ( 7.778174593052021635, 7.778174593052023411, 105.4374999999999858 ) ) ;
#73211=CARTESIAN_POINT ( 'NONE',  ( 7.204075437095968759, -7.204075437095966983, 91.09375000204838102 ) ) ;
#73227=CARTESIAN_POINT ( 'NONE',  ( 7.204075437095968759, -7.204075437095966983, 93.71875000204838102 ) ) ;
#73230=CARTESIAN_POINT ( 'NONE',  ( 11.00000000000000000, 1.347111479062088405E-15, 105.2500000000000000 ) ) ;
#73238=AXIS2_PLACEMENT_3D ( 'NONE', #22483, #39852, #69644 ) ;
#73239=CYLINDRICAL_SURFACE ( 'NONE', #30146, 11.00000000000000000 ) ;
#73260=CARTESIAN_POINT ( 'NONE',  ( -11.00000000000000000, 0.000000000000000000, 95.68750000409677625 ) ) ;
#73282=CARTESIAN_POINT ( 'NONE',  ( -7.204075437095967871, 7.204075437095967871, 103.8437500020483810 ) ) ;
#73293=CARTESIAN_POINT ( 'NONE',  ( -4.220049686691935698, 10.18810118749999916, 113.8750000020483668 ) ) ;
#73300=CARTESIAN_POINT ( 'NONE',  ( 2.020667218593132706E-15, -11.00000000000000000, 103.5625000040967763 ) ) ;
#73301=( BOUNDED_CURVE ( )  B_SPLINE_CURVE ( 2, ( #73045, #72677, #31937, #54960, #20980, #67011, #15688, #15310, #16424 ),
 .UNSPECIFIED., .F., .F. ) 
 B_SPLINE_CURVE_WITH_KNOTS ( ( 3, 2, 2, 2, 3 ),
 ( 0.4852941176470589313, 0.4889705882352942123, 0.4926470588235295489, 0.4963235294117648300, 0.5000000000000001110 ),
 .UNSPECIFIED. ) 
 CURVE ( )  GEOMETRIC_REPRESENTATION_ITEM ( )  RATIONAL_B_SPLINE_CURVE ( ( 0.9999999999999976685, 0.9238795325112890700, 1.000000000000000000, 0.9238795325112867385, 1.000000000000000000, 0.9238795325112867385, 1.000000000000000000, 0.9238795325112844070, 1.000000000000002220 ) ) 
 REPRESENTATION_ITEM ( '' )  );
#73303=CARTESIAN_POINT ( 'NONE',  ( 4.220049686691941027, -10.18810118749999738, 112.0000000020483668 ) ) ;
#73318=CARTESIAN_POINT ( 'NONE',  ( 10.18810118749999916, 4.220049686691935698, 115.0000000020483810 ) ) ;
#73361=CARTESIAN_POINT ( 'NONE',  ( 11.00000000000000355, -4.556349186104044158, 82.65625000000000000 ) ) ;
#73367=CARTESIAN_POINT ( 'NONE',  ( 7.204075437095966983, 7.204075437095967871, 89.59375000204838102 ) ) ;
#73377=CARTESIAN_POINT ( 'NONE',  ( -4.220049686691937474, -10.18810118749999738, 80.31250000204836681 ) ) ;
#73389=ORIENTED_EDGE ( 'NONE', *, *, #66141, .T. ) ;
#73391=CARTESIAN_POINT ( 'NONE',  ( 1.871523826299183495E-15, -10.18810118749999916, 78.53125000204836681 ) ) ;
#73425=CARTESIAN_POINT ( 'NONE',  ( -11.00000000000000000, 0.000000000000000000, 72.99999999999998579 ) ) ;
#73443=CARTESIAN_POINT ( 'NONE',  ( -11.00000000000000000, 0.000000000000000000, 81.99999999999998579 ) ) ;
#73451=CARTESIAN_POINT ( 'NONE',  ( -7.204075437095967871, 7.204075437095967871, 109.4687500020483810 ) ) ;
#73464=CARTESIAN_POINT ( 'NONE',  ( 7.204075437095968759, -7.204075437095966983, 100.0937500020483668 ) ) ;
#73483=CARTESIAN_POINT ( 'NONE',  ( -10.18810118749999738, -4.220049686691941915, 83.12500000204835260 ) ) ;
#73496=ORIENTED_EDGE ( 'NONE', *, *, #21911, .T. ) ;
#73501=CARTESIAN_POINT ( 'NONE',  ( 7.204075437095968759, -7.204075437095966983, 74.21875000204836681 ) ) ;
#73504=CARTESIAN_POINT ( 'NONE',  ( 11.00000000000000355, -4.556349186104045046, 88.65625000000000000 ) ) ;
#73509=CARTESIAN_POINT ( 'NONE',  ( 0.000000000000000000, 0.000000000000000000, 118.0000000000000000 ) ) ;
#73533=CARTESIAN_POINT ( 'NONE',  ( 2.020667218593132706E-15, -11.00000000000000000, 75.06250000409676204 ) ) ;
#73552=CARTESIAN_POINT ( 'NONE',  ( 10.18810118750000093, -4.220049686691933921, 71.31250000204836681 ) ) ;
#73562=CARTESIAN_POINT ( 'NONE',  ( -6.238412754330611322E-16, 10.18810118749999916, 81.15625000204838102 ) ) ;
#73564=EDGE_CURVE ( 'NONE', #39873, #10672, #54861, .T. ) ;
#73567=EDGE_CURVE ( 'NONE', #2929, #22034, #47020, .T. ) ;
#73574=CARTESIAN_POINT ( 'NONE',  ( 7.204075437095966983, 7.204075437095967871, 91.46875000204838102 ) ) ;
#73592=CARTESIAN_POINT ( 'NONE',  ( 10.18810118750000093, -4.220049686691933033, 92.31250000204838102 ) ) ;
#73595=CARTESIAN_POINT ( 'NONE',  ( -7.778174593052023411, 7.778174593052023411, 107.3124999999999858 ) ) ;
#73622=CARTESIAN_POINT ( 'NONE',  ( 11.00000000000000000, 1.347111479062088405E-15, 88.75000000000000000 ) ) ;
#73625=VERTEX_POINT ( 'NONE', #36820 ) ;
#73628=CARTESIAN_POINT ( 'NONE',  ( 11.00000000000000000, 4.556349186104045934, 92.03125000409677625 ) ) ;
#73649=CARTESIAN_POINT ( 'NONE',  ( -4.220049686691937474, -10.18810118749999738, 99.81250000204838102 ) ) ;
#73658=CARTESIAN_POINT ( 'NONE',  ( -6.238412754330611322E-16, 10.18810118749999916, 115.2812500020483810 ) ) ;
#73667=CARTESIAN_POINT ( 'NONE',  ( 7.204075437095968759, -7.204075437095966983, 110.5937500020483810 ) ) ;
#73682=ORIENTED_EDGE ( 'NONE', *, *, #19184, .F. ) ;
#73683=CARTESIAN_POINT ( 'NONE',  ( -6.238412754330611322E-16, 10.18810118749999916, 109.2812500020483668 ) ) ;
#73696=CARTESIAN_POINT ( 'NONE',  ( 10.99999999999989697, -4.556349186104149851, 91.65625000000001421 ) ) ;
#73730=VERTEX_POINT ( 'NONE', #66222 ) ;
#73732=CARTESIAN_POINT ( 'NONE',  ( 7.204075437095966983, 7.204075437095967871, 86.59375000204836681 ) ) ;
#73736=CARTESIAN_POINT ( 'NONE',  ( 7.778174593052021635, 7.778174593052023411, 112.9375000000000000 ) ) ;
#73745=CARTESIAN_POINT ( 'NONE',  ( -7.204075437095967871, 7.204075437095967871, 82.84375000204838102 ) ) ;
#73758=CARTESIAN_POINT ( 'NONE',  ( 7.204075437095968759, -7.204075437095966983, 77.21875000204836681 ) ) ;
#73793=CARTESIAN_POINT ( 'NONE',  ( -10.99999999999999822, -4.556349186104052151, 70.09374999999998579 ) ) ;
#73798=AXIS2_PLACEMENT_3D ( 'NONE', #74205, #6306, #47013 ) ;
#73813=CARTESIAN_POINT ( 'NONE',  ( -6.735557395310442023E-16, 11.00000000000000000, 81.62499999999998579 ) ) ;
#73820=CARTESIAN_POINT ( 'NONE',  ( -10.18810118749999916, 4.220049686691934809, 105.0625000020483810 ) ) ;
#73829=ORIENTED_EDGE ( 'NONE', *, *, #24932, .F. ) ;
#73836=CARTESIAN_POINT ( 'NONE',  ( -6.238412754330611322E-16, 10.18810118749999916, 99.15625000204838102 ) ) ;
#73841=PLANE ( 'NONE',  #4577 ) ;
#73849=( BOUNDED_CURVE ( )  B_SPLINE_CURVE ( 2, ( #14835, #3538, #54855, #26530, #36754, #15215, #55606, #60871, #3924 ),
 .UNSPECIFIED., .F., .F. ) 
 B_SPLINE_CURVE_WITH_KNOTS ( ( 3, 2, 2, 2, 3 ),
 ( 0.6323529411764704511, 0.6360294117647057321, 0.6397058823529409022, 0.6433823529411762943, 0.6470588235294115753 ),
 .UNSPECIFIED. ) 
 CURVE ( )  GEOMETRIC_REPRESENTATION_ITEM ( )  RATIONAL_B_SPLINE_CURVE ( ( 1.000000000000002220, 0.9238795325112844070, 1.000000000000000000, 0.9238795325112867385, 1.000000000000000000, 0.9238795325112867385, 1.000000000000000000, 0.9238795325112912904, 0.9999999999999954481 ) ) 
 REPRESENTATION_ITEM ( '' )  );
#73858=CARTESIAN_POINT ( 'NONE',  ( 10.18810118749999916, 4.220049686691935698, 80.87500000204836681 ) ) ;
#73873=EDGE_LOOP ( 'NONE', ( #39151, #16742, #56556, #17084 ) ) ;
#73879=ORIENTED_EDGE ( 'NONE', *, *, #56856, .T. ) ;
#73880=CARTESIAN_POINT ( 'NONE',  ( 10.18810118749999916, 4.220049686691935698, 74.50000000204838102 ) ) ;
#73883=CARTESIAN_POINT ( 'NONE',  ( -10.99999999999999822, -4.556349186104052151, 89.59374999999997158 ) ) ;
#73888=CARTESIAN_POINT ( 'NONE',  ( 11.00000000000000000, 1.347111479062088405E-15, 78.24999999999998579 ) ) ;
#73904=VERTEX_POINT ( 'NONE', #68097 ) ;
#73909=CARTESIAN_POINT ( 'NONE',  ( 4.556349186104045934, 11.00000000000000000, 75.71875000409677625 ) ) ;
#73926=CARTESIAN_POINT ( 'NONE',  ( 7.204075437095966983, 7.204075437095967871, 68.59375000204836681 ) ) ;
#73932=CARTESIAN_POINT ( 'NONE',  ( -4.556349186104048599, -10.99999999999999822, 79.46875000409677625 ) ) ;
#73935=CARTESIAN_POINT ( 'NONE',  ( 7.204075437095968759, -7.204075437095966983, 82.09375000204838102 ) ) ;
#73964=CARTESIAN_POINT ( 'NONE',  ( 4.220049686691941027, -10.18810118749999738, 92.12500000204836681 ) ) ;
#73967=CARTESIAN_POINT ( 'NONE',  ( -10.99999999999999822, -4.556349186104052151, 106.0937500000000142 ) ) ;
#73969=CARTESIAN_POINT ( 'NONE',  ( 11.00000000000000000, 1.347111479062088405E-15, 87.25000000000000000 ) ) ;
#73970=DIRECTION ( 'NONE',  ( 1.000000000000000000, 0.000000000000000000, -0.000000000000000000 ) ) ;
#73986=CARTESIAN_POINT ( 'NONE',  ( -11.00000000000000000, 0.000000000000000000, 86.50000000000000000 ) ) ;
#73998=CARTESIAN_POINT ( 'NONE',  ( -7.778174593052020747, -7.778174593052023411, 91.37500000409677625 ) ) ;
#74011=ORIENTED_EDGE ( 'NONE', *, *, #25573, .T. ) ;
#74013=CARTESIAN_POINT ( 'NONE',  ( -11.00000000000000000, 0.000000000000000000, 113.6875000040967763 ) ) ;
#74019=CARTESIAN_POINT ( 'NONE',  ( -6.238412754330611322E-16, 10.18810118749999916, 100.6562500020483810 ) ) ;
#74026=CARTESIAN_POINT ( 'NONE',  ( -10.18810118749999738, -4.220049686691941915, 114.2500000020483952 ) ) ;
#74033=CARTESIAN_POINT ( 'NONE',  ( -10.99999999999984013, -4.556349186104210247, 103.2812500040967905 ) ) ;
#74035=CARTESIAN_POINT ( 'NONE',  ( 1.871523826299183495E-15, -10.18810118749999916, 110.4062500020483668 ) ) ;
#74055=CARTESIAN_POINT ( 'NONE',  ( -6.238412754330611322E-16, 10.18810118749999916, 110.7812500020483668 ) ) ;
#74056=CARTESIAN_POINT ( 'NONE',  ( -6.735557395310442023E-16, 11.00000000000000000, 96.81250000409677625 ) ) ;
#74064=DIRECTION ( 'NONE',  ( -1.000000000000000000, 0.000000000000000000, 0.000000000000000000 ) ) ;
#74077=CARTESIAN_POINT ( 'NONE',  ( 2.020667218593132706E-15, -11.00000000000000000, 82.56250000409677625 ) ) ;
#74083=CARTESIAN_POINT ( 'NONE',  ( -4.556349186104045934, 11.00000000000000000, 110.4062500040967620 ) ) ;
#74106=CARTESIAN_POINT ( 'NONE',  ( 10.18810118749999916, 4.220049686691935698, 91.00000000204836681 ) ) ;
#74111=CARTESIAN_POINT ( 'NONE',  ( -10.18810118749999916, 0.000000000000000000, 116.0312500020483810 ) ) ;
#74118=CARTESIAN_POINT ( 'NONE',  ( -4.220049686691935698, 10.18810118749999916, 85.75000000204838102 ) ) ;
#74127=DIRECTION ( 'NONE',  ( -0.000000000000000000, -0.000000000000000000, -1.000000000000000000 ) ) ;
#74131=CARTESIAN_POINT ( 'NONE',  ( 10.18810118750000093, -4.220049686691933921, 77.31250000204836681 ) ) ;
#74133=EDGE_CURVE ( 'NONE', #36393, #30135, #35885, .T. ) ;
#74150=CARTESIAN_POINT ( 'NONE',  ( 7.778174593052021635, 7.778174593052023411, 74.12500000409677625 ) ) ;
#74171=CARTESIAN_POINT ( 'NONE',  ( 7.778174593052023411, -7.778174593052021635, 112.7500000040967763 ) ) ;
#74188=ORIENTED_EDGE ( 'NONE', *, *, #47538, .F. ) ;
#74190=CARTESIAN_POINT ( 'NONE',  ( 10.18810118750000093, -4.220049686691933921, 104.3125000020483810 ) ) ;
#74205=CARTESIAN_POINT ( 'NONE',  ( 0.000000000000000000, 0.000000000000000000, 118.0000000000000000 ) ) ;
#74209=CARTESIAN_POINT ( 'NONE',  ( 10.18810118749999916, 1.247682550866122264E-15, 98.78125000204838102 ) ) ;
#74222=CARTESIAN_POINT ( 'NONE',  ( -10.18810118749999916, 4.220049686691934809, 96.06250000204836681 ) ) ;
#74226=PRODUCT_DEFINITION_CONTEXT ( 'detailed design', #57833, 'design' ) ;
#74231=CARTESIAN_POINT ( 'NONE',  ( 1.871523826299183495E-15, -10.18810118749999916, 83.40625000204838102 ) ) ;
#74244=VERTEX_POINT ( 'NONE', #45818 ) ;
#74249=CARTESIAN_POINT ( 'NONE',  ( -4.220049686691935698, 10.18810118749999916, 73.37500000204838102 ) ) ;
#74252=CARTESIAN_POINT ( 'NONE',  ( -11.00000000000000000, 4.556349186104045934, 80.40624999999997158 ) ) ;
#74257=FACE_OUTER_BOUND ( 'NONE', #36664, .T. ) ;
#74260=AXIS2_PLACEMENT_3D ( 'NONE', #67712, #72235, #21671 ) ;
#74278=CARTESIAN_POINT ( 'NONE',  ( -6.735557395310442023E-16, 11.00000000000000000, 77.31250000409677625 ) ) ;
#74297=CARTESIAN_POINT ( 'NONE',  ( 7.204075437095966983, 7.204075437095967871, 71.59375000204836681 ) ) ;
#74332=CARTESIAN_POINT ( 'NONE',  ( -4.220049686691937474, -10.18810118749999738, 90.43750000204838102 ) ) ;
#74335=CARTESIAN_POINT ( 'NONE',  ( -6.735557395310442023E-16, 11.00000000000000000, 107.1250000000000000 ) ) ;
#74339=CARTESIAN_POINT ( 'NONE',  ( 7.778174593052021635, 7.778174593052023411, 113.1250000040967763 ) ) ;
#74362=ADVANCED_FACE ( 'NONE', ( #36359 ), #70681, .T. ) ;
#74365=CARTESIAN_POINT ( 'NONE',  ( -10.99999999999999822, -4.556349186104052151, 89.78125000409679046 ) ) ;
#74377=CARTESIAN_POINT ( 'NONE',  ( 7.778174593052021635, 7.778174593052023411, 102.6250000040967763 ) ) ;
#74390=CARTESIAN_POINT ( 'NONE',  ( 7.204075437095968759, -7.204075437095966983, 97.09375000204836681 ) ) ;
#74399=CARTESIAN_POINT ( 'NONE',  ( 4.220049686691941027, -10.18810118749999738, 110.1250000020483810 ) ) ;
#74409=( BOUNDED_CURVE ( )  B_SPLINE_CURVE ( 2, ( #71576, #21021, #66301, #32361, #3681, #72717, #44045, #5177, #22131 ),
 .UNSPECIFIED., .F., .F. ) 
 B_SPLINE_CURVE_WITH_KNOTS ( ( 3, 2, 2, 2, 3 ),
 ( 0.2205882352941175295, 0.2242647058823528383, 0.2279411764705881194, 0.2316176470588234282, 0.2352941176470587092 ),
 .UNSPECIFIED. ) 
 CURVE ( )  GEOMETRIC_REPRESENTATION_ITEM ( )  RATIONAL_B_SPLINE_CURVE ( ( 1.000000000000002220, 0.9238795325112844070, 1.000000000000000000, 0.9238795325112867385, 1.000000000000000000, 0.9238795325112867385, 1.000000000000000000, 0.9238795325112890700, 0.9999999999999976685 ) ) 
 REPRESENTATION_ITEM ( '' )  );
#74410=CARTESIAN_POINT ( 'NONE',  ( 4.220049686691934809, 10.18810118749999916, 103.5625000020483668 ) ) ;
#74414=ORIENTED_EDGE ( 'NONE', *, *, #31650, .T. ) ;
#74427=CARTESIAN_POINT ( 'NONE',  ( -7.204075437095965206, -7.204075437095968759, 109.8437500020483810 ) ) ;
#74447=DIRECTION ( 'NONE',  ( 0.000000000000000000, 0.000000000000000000, -1.000000000000000000 ) ) ;
#74451=CARTESIAN_POINT ( 'NONE',  ( -7.778174593052023411, 7.778174593052023411, 113.5000000040967763 ) ) ;
#74474=CARTESIAN_POINT ( 'NONE',  ( -6.238412754330611322E-16, 10.18810118749999916, 85.28125000204836681 ) ) ;
#74479=CARTESIAN_POINT ( 'NONE',  ( -7.778174593052023411, 7.778174593052023411, 113.3125000000000000 ) ) ;
#74480=CARTESIAN_POINT ( 'NONE',  ( 10.18810118750000093, -4.220049686691933921, 113.6875000020483952 ) ) ;
#74488=CARTESIAN_POINT ( 'NONE',  ( 4.220049686691941027, -10.18810118749999738, 77.50000000204839523 ) ) ;
#74490=ORIENTED_EDGE ( 'NONE', *, *, #60667, .T. ) ;
#74499=CARTESIAN_POINT ( 'NONE',  ( -7.204075437095967871, 7.204075437095967871, 79.46875000204836681 ) ) ;
#74514=ADVANCED_FACE ( 'NONE', ( #35995 ), #14551, .T. ) ;
#74536=CARTESIAN_POINT ( 'NONE',  ( 11.00000000000010836, -4.556349186103939353, 90.15625000000000000 ) ) ;
#74545=VERTEX_POINT ( 'NONE', #3915 ) ;
#74568=CARTESIAN_POINT ( 'NONE',  ( 7.204075437095966983, 7.204075437095967871, 106.0937500020483810 ) ) ;
#74582=EDGE_CURVE ( 'NONE', #12782, #32089, #39349, .T. ) ;
#74584=CARTESIAN_POINT ( 'NONE',  ( -6.238412754330611322E-16, 10.18810118749999916, 96.15625000204838102 ) ) ;
#74596=CARTESIAN_POINT ( 'NONE',  ( -7.778174593052023411, 7.778174593052023411, 89.50000000409677625 ) ) ;
#74598=CARTESIAN_POINT ( 'NONE',  ( -6.238412754330611322E-16, 10.18810118749999916, 92.78125000204836681 ) ) ;
#74602=ORIENTED_EDGE ( 'NONE', *, *, #41335, .F. ) ;
#74608=CARTESIAN_POINT ( 'NONE',  ( -6.238412754330611322E-16, 10.18810118749999916, 79.65625000204836681 ) ) ;
#74628=CARTESIAN_POINT ( 'NONE',  ( 10.18810118749999916, 1.247682550866122264E-15, 74.40625000204836681 ) ) ;
#74631=CARTESIAN_POINT ( 'NONE',  ( 11.00000000000000000, 4.556349186104045934, 81.34375000000000000 ) ) ;
#74634=CARTESIAN_POINT ( 'NONE',  ( 0.000000000000000000, 0.000000000000000000, 118.0000000000000000 ) ) ;
#74635=ORIENTED_EDGE ( 'NONE', *, *, #33466, .T. ) ;
#74700=COLOUR_RGB('Black',0.12,0.14,0.17);
#74701=FILL_AREA_STYLE_COLOUR('',#74700);
#74702=FILL_AREA_STYLE('',(#74701));
#74703=SURFACE_STYLE_FILL_AREA(#74702);
#74704=SURFACE_SIDE_STYLE('',(#74703));
#74705=SURFACE_STYLE_USAGE(.BOTH.,#74704);
#74706=PRESENTATION_STYLE_ASSIGNMENT((#74705));
ENDSEC;
END-ISO-10303-21;
